ISO-10303-21;
HEADER;
/* Generated by software containing ST-Developer
 * from STEP Tools, Inc. (www.steptools.com) 
 */

FILE_DESCRIPTION(
/* description */ (''),
/* implementation_level */ '2;1');

FILE_NAME(
/* name */ 'Socket head screw M4x24.step',
/* time_stamp */ '2026-11-15T17:46:57-08:00',
/* author */ (''),
/* organization */ (''),
/* preprocessor_version */ 'ST-DEVELOPER v20.2',
/* originating_system */ 'Autodesk Translation Framework v15.17.0.0',
/* authorisation */ '');

FILE_SCHEMA (('AUTOMOTIVE_DESIGN { 1 0 10303 214 3 1 1 }'));
ENDSEC;

DATA;
#10=MECHANICAL_DESIGN_GEOMETRIC_PRESENTATION_REPRESENTATION('',(#384),#12963);
#171=B_SPLINE_SURFACE_WITH_KNOTS('',3,3,((#9802,#9803,#9804,#9805,#9806,
#9807,#9808,#9809,#9810,#9811,#9812,#9813,#9814,#9815,#9816,#9817,#9818,
#9819,#9820,#9821,#9822,#9823,#9824,#9825,#9826,#9827,#9828,#9829,#9830,
#9831,#9832,#9833,#9834,#9835,#9836,#9837,#9838,#9839,#9840,#9841,#9842,
#9843,#9844,#9845,#9846,#9847,#9848,#9849,#9850,#9851,#9852,#9853,#9854,
#9855,#9856,#9857,#9858,#9859,#9860,#9861,#9862,#9863,#9864,#9865,#9866,
#9867,#9868,#9869,#9870,#9871,#9872,#9873,#9874,#9875,#9876,#9877,#9878,
#9879,#9880,#9881,#9882,#9883,#9884,#9885,#9886,#9887,#9888,#9889,#9890,
#9891,#9892,#9893,#9894,#9895,#9896,#9897,#9898,#9899,#9900,#9901,#9902,
#9903,#9904,#9905,#9906,#9907,#9908,#9909,#9910,#9911,#9912,#9913,#9914,
#9915,#9916,#9917,#9918,#9919,#9920,#9921,#9922,#9923,#9924,#9925,#9926,
#9927,#9928,#9929,#9930,#9931,#9932,#9933,#9934,#9935,#9936,#9937,#9938,
#9939,#9940,#9941,#9942,#9943,#9944,#9945,#9946,#9947,#9948,#9949,#9950,
#9951,#9952,#9953,#9954,#9955,#9956,#9957,#9958,#9959,#9960,#9961,#9962,
#9963,#9964,#9965,#9966,#9967,#9968,#9969,#9970,#9971,#9972,#9973,#9974,
#9975,#9976,#9977,#9978,#9979,#9980,#9981,#9982,#9983,#9984,#9985,#9986,
#9987,#9988,#9989,#9990,#9991,#9992,#9993,#9994,#9995,#9996,#9997,#9998,
#9999,#10000,#10001,#10002,#10003,#10004,#10005,#10006,#10007,#10008,#10009,
#10010,#10011,#10012,#10013,#10014,#10015,#10016,#10017,#10018,#10019,#10020,
#10021,#10022),(#10023,#10024,#10025,#10026,#10027,#10028,#10029,#10030,
#10031,#10032,#10033,#10034,#10035,#10036,#10037,#10038,#10039,#10040,#10041,
#10042,#10043,#10044,#10045,#10046,#10047,#10048,#10049,#10050,#10051,#10052,
#10053,#10054,#10055,#10056,#10057,#10058,#10059,#10060,#10061,#10062,#10063,
#10064,#10065,#10066,#10067,#10068,#10069,#10070,#10071,#10072,#10073,#10074,
#10075,#10076,#10077,#10078,#10079,#10080,#10081,#10082,#10083,#10084,#10085,
#10086,#10087,#10088,#10089,#10090,#10091,#10092,#10093,#10094,#10095,#10096,
#10097,#10098,#10099,#10100,#10101,#10102,#10103,#10104,#10105,#10106,#10107,
#10108,#10109,#10110,#10111,#10112,#10113,#10114,#10115,#10116,#10117,#10118,
#10119,#10120,#10121,#10122,#10123,#10124,#10125,#10126,#10127,#10128,#10129,
#10130,#10131,#10132,#10133,#10134,#10135,#10136,#10137,#10138,#10139,#10140,
#10141,#10142,#10143,#10144,#10145,#10146,#10147,#10148,#10149,#10150,#10151,
#10152,#10153,#10154,#10155,#10156,#10157,#10158,#10159,#10160,#10161,#10162,
#10163,#10164,#10165,#10166,#10167,#10168,#10169,#10170,#10171,#10172,#10173,
#10174,#10175,#10176,#10177,#10178,#10179,#10180,#10181,#10182,#10183,#10184,
#10185,#10186,#10187,#10188,#10189,#10190,#10191,#10192,#10193,#10194,#10195,
#10196,#10197,#10198,#10199,#10200,#10201,#10202,#10203,#10204,#10205,#10206,
#10207,#10208,#10209,#10210,#10211,#10212,#10213,#10214,#10215,#10216,#10217,
#10218,#10219,#10220,#10221,#10222,#10223,#10224,#10225,#10226,#10227,#10228,
#10229,#10230,#10231,#10232,#10233,#10234,#10235,#10236,#10237,#10238,#10239,
#10240,#10241,#10242,#10243),(#10244,#10245,#10246,#10247,#10248,#10249,
#10250,#10251,#10252,#10253,#10254,#10255,#10256,#10257,#10258,#10259,#10260,
#10261,#10262,#10263,#10264,#10265,#10266,#10267,#10268,#10269,#10270,#10271,
#10272,#10273,#10274,#10275,#10276,#10277,#10278,#10279,#10280,#10281,#10282,
#10283,#10284,#10285,#10286,#10287,#10288,#10289,#10290,#10291,#10292,#10293,
#10294,#10295,#10296,#10297,#10298,#10299,#10300,#10301,#10302,#10303,#10304,
#10305,#10306,#10307,#10308,#10309,#10310,#10311,#10312,#10313,#10314,#10315,
#10316,#10317,#10318,#10319,#10320,#10321,#10322,#10323,#10324,#10325,#10326,
#10327,#10328,#10329,#10330,#10331,#10332,#10333,#10334,#10335,#10336,#10337,
#10338,#10339,#10340,#10341,#10342,#10343,#10344,#10345,#10346,#10347,#10348,
#10349,#10350,#10351,#10352,#10353,#10354,#10355,#10356,#10357,#10358,#10359,
#10360,#10361,#10362,#10363,#10364,#10365,#10366,#10367,#10368,#10369,#10370,
#10371,#10372,#10373,#10374,#10375,#10376,#10377,#10378,#10379,#10380,#10381,
#10382,#10383,#10384,#10385,#10386,#10387,#10388,#10389,#10390,#10391,#10392,
#10393,#10394,#10395,#10396,#10397,#10398,#10399,#10400,#10401,#10402,#10403,
#10404,#10405,#10406,#10407,#10408,#10409,#10410,#10411,#10412,#10413,#10414,
#10415,#10416,#10417,#10418,#10419,#10420,#10421,#10422,#10423,#10424,#10425,
#10426,#10427,#10428,#10429,#10430,#10431,#10432,#10433,#10434,#10435,#10436,
#10437,#10438,#10439,#10440,#10441,#10442,#10443,#10444,#10445,#10446,#10447,
#10448,#10449,#10450,#10451,#10452,#10453,#10454,#10455,#10456,#10457,#10458,
#10459,#10460,#10461,#10462,#10463,#10464),(#10465,#10466,#10467,#10468,
#10469,#10470,#10471,#10472,#10473,#10474,#10475,#10476,#10477,#10478,#10479,
#10480,#10481,#10482,#10483,#10484,#10485,#10486,#10487,#10488,#10489,#10490,
#10491,#10492,#10493,#10494,#10495,#10496,#10497,#10498,#10499,#10500,#10501,
#10502,#10503,#10504,#10505,#10506,#10507,#10508,#10509,#10510,#10511,#10512,
#10513,#10514,#10515,#10516,#10517,#10518,#10519,#10520,#10521,#10522,#10523,
#10524,#10525,#10526,#10527,#10528,#10529,#10530,#10531,#10532,#10533,#10534,
#10535,#10536,#10537,#10538,#10539,#10540,#10541,#10542,#10543,#10544,#10545,
#10546,#10547,#10548,#10549,#10550,#10551,#10552,#10553,#10554,#10555,#10556,
#10557,#10558,#10559,#10560,#10561,#10562,#10563,#10564,#10565,#10566,#10567,
#10568,#10569,#10570,#10571,#10572,#10573,#10574,#10575,#10576,#10577,#10578,
#10579,#10580,#10581,#10582,#10583,#10584,#10585,#10586,#10587,#10588,#10589,
#10590,#10591,#10592,#10593,#10594,#10595,#10596,#10597,#10598,#10599,#10600,
#10601,#10602,#10603,#10604,#10605,#10606,#10607,#10608,#10609,#10610,#10611,
#10612,#10613,#10614,#10615,#10616,#10617,#10618,#10619,#10620,#10621,#10622,
#10623,#10624,#10625,#10626,#10627,#10628,#10629,#10630,#10631,#10632,#10633,
#10634,#10635,#10636,#10637,#10638,#10639,#10640,#10641,#10642,#10643,#10644,
#10645,#10646,#10647,#10648,#10649,#10650,#10651,#10652,#10653,#10654,#10655,
#10656,#10657,#10658,#10659,#10660,#10661,#10662,#10663,#10664,#10665,#10666,
#10667,#10668,#10669,#10670,#10671,#10672,#10673,#10674,#10675,#10676,#10677,
#10678,#10679,#10680,#10681,#10682,#10683,#10684,#10685)),.UNSPECIFIED.,
 .F.,.F.,.F.,(4,4),(4,1,1,1,1,1,1,1,1,1,1,1,1,1,1,1,1,1,1,1,1,1,1,1,1,1,
1,1,1,1,1,1,1,1,1,1,1,1,1,1,1,1,1,1,1,1,1,1,1,1,1,1,1,1,1,1,1,1,1,1,1,1,
1,1,1,1,1,1,1,1,1,1,1,1,1,1,1,1,1,1,1,1,1,1,1,1,1,1,1,1,1,1,1,1,1,1,1,1,
1,1,1,1,1,1,1,1,1,1,1,1,1,1,1,1,1,1,1,1,1,1,1,1,1,1,1,1,1,1,1,1,1,1,1,1,
1,1,1,1,1,1,1,1,1,1,1,1,1,1,1,1,1,1,1,1,1,1,1,1,1,1,1,1,1,1,1,1,1,1,1,1,
1,1,1,1,1,1,1,1,1,1,1,1,1,1,1,1,1,1,1,1,1,1,1,1,1,1,1,1,1,1,1,1,1,1,1,1,
1,1,1,1,1,1,1,1,1,1,1,1,4),(0.,0.0460148164544132),(8.31058692273996,9.30824121805847,
10.305895513377,11.3035498086955,12.301204104014,13.2988583993325,14.296512694651,
15.2941669899695,16.291821285288,17.2894755806066,18.2871298759251,19.2847841712436,
20.2824384665621,21.2800927618806,22.2777470571991,23.2754013525176,24.2730556478361,
25.2707099431546,26.2683642384732,27.2660185337917,28.2636728291102,29.2613271244287,
30.2589814197472,31.2566357150657,32.2542900103842,33.2519443057027,34.2495986010213,
35.2472528963398,36.2449071916583,37.2425614869768,38.2402157822953,39.2378700776138,
40.2355243729323,41.2331786682508,42.2308329635693,43.2284872588879,44.2261415542064,
45.2237958495249,46.2214501448434,47.2191044401619,48.2167587354804,49.2144130307989,
50.2120673261174,51.209721621436,52.2073759167545,53.205030212073,54.2026845073915,
55.20033880271,56.1979930980285,57.195647393347,58.1933016886655,59.190955983984,
60.1886102793026,61.1862645746211,62.1839188699396,63.1815731652581,64.1792274605766,
65.1768817558951,66.1745360512136,67.1721903465321,68.1698446418506,69.1674989371692,
70.1651532324877,71.1628075278062,72.1604618231247,73.1581161184432,74.1557704137617,
75.1534247090802,76.1510790043987,77.1487332997173,78.1463875950358,79.1440418903543,
80.1416961856728,81.1393504809913,82.1370047763098,83.1346590716283,84.1323133669468,
85.1299676622653,86.1276219575839,87.1252762529024,88.1229305482209,89.1205848435394,
90.1182391388579,91.1158934341764,92.1135477294949,93.1112020248134,94.1088563201319,
95.1065106154505,96.104164910769,97.1018192060875,98.099473501406,99.0971277967245,
100.094782092043,101.092436387362,102.09009068268,103.087744977999,104.085399273317,
105.083053568636,106.080707863954,107.078362159273,108.076016454591,109.07367074991,
110.071325045228,111.068979340547,112.066633635865,113.064287931184,114.061942226502,
115.059596521821,116.057250817139,117.054905112458,118.052559407776,119.050213703095,
120.047867998413,121.045522293732,122.04317658905,123.040830884369,124.038485179687,
125.036139475006,126.033793770324,127.031448065643,128.029102360961,129.02675665628,
130.024410951598,131.022065246917,132.019719542235,133.017373837554,134.015028132872,
135.012682428191,136.010336723509,137.007991018828,138.005645314146,139.003299609465,
140.000953904783,140.998608200102,141.99626249542,142.993916790739,143.991571086058,
144.989225381376,145.986879676695,146.984533972013,147.982188267332,148.97984256265,
149.977496857969,150.975151153287,151.972805448606,152.970459743924,153.968114039243,
154.965768334561,155.96342262988,156.961076925198,157.958731220517,158.956385515835,
159.954039811154,160.951694106472,161.949348401791,162.947002697109,163.944656992428,
164.942311287746,165.939965583065,166.937619878383,167.935274173702,168.93292846902,
169.930582764339,170.928237059657,171.925891354976,172.923545650294,173.921199945613,
174.918854240931,175.91650853625,176.914162831568,177.911817126887,178.909471422205,
179.907125717524,180.904780012842,181.902434308161,182.900088603479,183.897742898798,
184.895397194116,185.893051489435,186.890705784754,187.888360080072,188.886014375391,
189.883668670709,190.881322966028,191.878977261346,192.876631556665,193.874285851983,
194.871940147302,195.86959444262,196.867248737939,197.864903033257,198.862557328576,
199.860211623894,200.857865919213,201.855520214531,202.85317450985,203.850828805168,
204.848483100487,205.846137395805,206.843791691124,207.841445986442,208.839100281761,
209.836754577079,210.834408872398,211.832063167716,212.829717463035,213.827371758353,
214.825026053672,215.82268034899,216.820334644309,217.817988939627,218.815643234946,
219.813297530264,220.810951825583,221.808606120901,222.80626041622,223.803914711538,
224.801569006857,225.799223302175),.UNSPECIFIED.);
#172=B_SPLINE_SURFACE_WITH_KNOTS('',3,3,((#10819,#10820,#10821,#10822,#10823,
#10824,#10825,#10826,#10827,#10828,#10829,#10830,#10831,#10832,#10833,#10834,
#10835,#10836,#10837,#10838,#10839,#10840,#10841,#10842,#10843,#10844,#10845,
#10846,#10847,#10848,#10849,#10850,#10851,#10852,#10853,#10854,#10855,#10856,
#10857,#10858,#10859,#10860,#10861,#10862,#10863,#10864,#10865,#10866,#10867,
#10868,#10869,#10870,#10871,#10872,#10873,#10874,#10875,#10876,#10877,#10878,
#10879,#10880,#10881,#10882,#10883,#10884,#10885,#10886,#10887,#10888,#10889,
#10890,#10891,#10892,#10893,#10894,#10895,#10896,#10897,#10898,#10899,#10900,
#10901,#10902,#10903,#10904,#10905,#10906,#10907,#10908,#10909,#10910,#10911,
#10912,#10913,#10914,#10915,#10916,#10917,#10918,#10919,#10920,#10921,#10922,
#10923,#10924,#10925,#10926,#10927,#10928,#10929,#10930,#10931,#10932,#10933,
#10934,#10935,#10936,#10937,#10938,#10939,#10940,#10941,#10942,#10943,#10944,
#10945,#10946,#10947,#10948,#10949,#10950,#10951,#10952,#10953,#10954,#10955,
#10956,#10957,#10958,#10959,#10960,#10961,#10962,#10963,#10964,#10965,#10966,
#10967,#10968,#10969,#10970,#10971,#10972,#10973,#10974,#10975,#10976,#10977,
#10978,#10979,#10980,#10981,#10982,#10983,#10984,#10985,#10986,#10987,#10988,
#10989,#10990,#10991,#10992,#10993,#10994,#10995,#10996,#10997,#10998,#10999,
#11000,#11001,#11002,#11003,#11004,#11005,#11006,#11007,#11008,#11009,#11010,
#11011,#11012,#11013,#11014,#11015,#11016,#11017,#11018,#11019,#11020,#11021,
#11022,#11023,#11024,#11025,#11026,#11027,#11028,#11029,#11030,#11031,#11032,
#11033,#11034,#11035,#11036,#11037,#11038,#11039),(#11040,#11041,#11042,
#11043,#11044,#11045,#11046,#11047,#11048,#11049,#11050,#11051,#11052,#11053,
#11054,#11055,#11056,#11057,#11058,#11059,#11060,#11061,#11062,#11063,#11064,
#11065,#11066,#11067,#11068,#11069,#11070,#11071,#11072,#11073,#11074,#11075,
#11076,#11077,#11078,#11079,#11080,#11081,#11082,#11083,#11084,#11085,#11086,
#11087,#11088,#11089,#11090,#11091,#11092,#11093,#11094,#11095,#11096,#11097,
#11098,#11099,#11100,#11101,#11102,#11103,#11104,#11105,#11106,#11107,#11108,
#11109,#11110,#11111,#11112,#11113,#11114,#11115,#11116,#11117,#11118,#11119,
#11120,#11121,#11122,#11123,#11124,#11125,#11126,#11127,#11128,#11129,#11130,
#11131,#11132,#11133,#11134,#11135,#11136,#11137,#11138,#11139,#11140,#11141,
#11142,#11143,#11144,#11145,#11146,#11147,#11148,#11149,#11150,#11151,#11152,
#11153,#11154,#11155,#11156,#11157,#11158,#11159,#11160,#11161,#11162,#11163,
#11164,#11165,#11166,#11167,#11168,#11169,#11170,#11171,#11172,#11173,#11174,
#11175,#11176,#11177,#11178,#11179,#11180,#11181,#11182,#11183,#11184,#11185,
#11186,#11187,#11188,#11189,#11190,#11191,#11192,#11193,#11194,#11195,#11196,
#11197,#11198,#11199,#11200,#11201,#11202,#11203,#11204,#11205,#11206,#11207,
#11208,#11209,#11210,#11211,#11212,#11213,#11214,#11215,#11216,#11217,#11218,
#11219,#11220,#11221,#11222,#11223,#11224,#11225,#11226,#11227,#11228,#11229,
#11230,#11231,#11232,#11233,#11234,#11235,#11236,#11237,#11238,#11239,#11240,
#11241,#11242,#11243,#11244,#11245,#11246,#11247,#11248,#11249,#11250,#11251,
#11252,#11253,#11254,#11255,#11256,#11257,#11258,#11259,#11260),(#11261,
#11262,#11263,#11264,#11265,#11266,#11267,#11268,#11269,#11270,#11271,#11272,
#11273,#11274,#11275,#11276,#11277,#11278,#11279,#11280,#11281,#11282,#11283,
#11284,#11285,#11286,#11287,#11288,#11289,#11290,#11291,#11292,#11293,#11294,
#11295,#11296,#11297,#11298,#11299,#11300,#11301,#11302,#11303,#11304,#11305,
#11306,#11307,#11308,#11309,#11310,#11311,#11312,#11313,#11314,#11315,#11316,
#11317,#11318,#11319,#11320,#11321,#11322,#11323,#11324,#11325,#11326,#11327,
#11328,#11329,#11330,#11331,#11332,#11333,#11334,#11335,#11336,#11337,#11338,
#11339,#11340,#11341,#11342,#11343,#11344,#11345,#11346,#11347,#11348,#11349,
#11350,#11351,#11352,#11353,#11354,#11355,#11356,#11357,#11358,#11359,#11360,
#11361,#11362,#11363,#11364,#11365,#11366,#11367,#11368,#11369,#11370,#11371,
#11372,#11373,#11374,#11375,#11376,#11377,#11378,#11379,#11380,#11381,#11382,
#11383,#11384,#11385,#11386,#11387,#11388,#11389,#11390,#11391,#11392,#11393,
#11394,#11395,#11396,#11397,#11398,#11399,#11400,#11401,#11402,#11403,#11404,
#11405,#11406,#11407,#11408,#11409,#11410,#11411,#11412,#11413,#11414,#11415,
#11416,#11417,#11418,#11419,#11420,#11421,#11422,#11423,#11424,#11425,#11426,
#11427,#11428,#11429,#11430,#11431,#11432,#11433,#11434,#11435,#11436,#11437,
#11438,#11439,#11440,#11441,#11442,#11443,#11444,#11445,#11446,#11447,#11448,
#11449,#11450,#11451,#11452,#11453,#11454,#11455,#11456,#11457,#11458,#11459,
#11460,#11461,#11462,#11463,#11464,#11465,#11466,#11467,#11468,#11469,#11470,
#11471,#11472,#11473,#11474,#11475,#11476,#11477,#11478,#11479,#11480,#11481),
(#11482,#11483,#11484,#11485,#11486,#11487,#11488,#11489,#11490,#11491,
#11492,#11493,#11494,#11495,#11496,#11497,#11498,#11499,#11500,#11501,#11502,
#11503,#11504,#11505,#11506,#11507,#11508,#11509,#11510,#11511,#11512,#11513,
#11514,#11515,#11516,#11517,#11518,#11519,#11520,#11521,#11522,#11523,#11524,
#11525,#11526,#11527,#11528,#11529,#11530,#11531,#11532,#11533,#11534,#11535,
#11536,#11537,#11538,#11539,#11540,#11541,#11542,#11543,#11544,#11545,#11546,
#11547,#11548,#11549,#11550,#11551,#11552,#11553,#11554,#11555,#11556,#11557,
#11558,#11559,#11560,#11561,#11562,#11563,#11564,#11565,#11566,#11567,#11568,
#11569,#11570,#11571,#11572,#11573,#11574,#11575,#11576,#11577,#11578,#11579,
#11580,#11581,#11582,#11583,#11584,#11585,#11586,#11587,#11588,#11589,#11590,
#11591,#11592,#11593,#11594,#11595,#11596,#11597,#11598,#11599,#11600,#11601,
#11602,#11603,#11604,#11605,#11606,#11607,#11608,#11609,#11610,#11611,#11612,
#11613,#11614,#11615,#11616,#11617,#11618,#11619,#11620,#11621,#11622,#11623,
#11624,#11625,#11626,#11627,#11628,#11629,#11630,#11631,#11632,#11633,#11634,
#11635,#11636,#11637,#11638,#11639,#11640,#11641,#11642,#11643,#11644,#11645,
#11646,#11647,#11648,#11649,#11650,#11651,#11652,#11653,#11654,#11655,#11656,
#11657,#11658,#11659,#11660,#11661,#11662,#11663,#11664,#11665,#11666,#11667,
#11668,#11669,#11670,#11671,#11672,#11673,#11674,#11675,#11676,#11677,#11678,
#11679,#11680,#11681,#11682,#11683,#11684,#11685,#11686,#11687,#11688,#11689,
#11690,#11691,#11692,#11693,#11694,#11695,#11696,#11697,#11698,#11699,#11700,
#11701,#11702)),.UNSPECIFIED.,.F.,.F.,.F.,(4,4),(4,1,1,1,1,1,1,1,1,1,1,
1,1,1,1,1,1,1,1,1,1,1,1,1,1,1,1,1,1,1,1,1,1,1,1,1,1,1,1,1,1,1,1,1,1,1,1,
1,1,1,1,1,1,1,1,1,1,1,1,1,1,1,1,1,1,1,1,1,1,1,1,1,1,1,1,1,1,1,1,1,1,1,1,
1,1,1,1,1,1,1,1,1,1,1,1,1,1,1,1,1,1,1,1,1,1,1,1,1,1,1,1,1,1,1,1,1,1,1,1,
1,1,1,1,1,1,1,1,1,1,1,1,1,1,1,1,1,1,1,1,1,1,1,1,1,1,1,1,1,1,1,1,1,1,1,1,
1,1,1,1,1,1,1,1,1,1,1,1,1,1,1,1,1,1,1,1,1,1,1,1,1,1,1,1,1,1,1,1,1,1,1,1,
1,1,1,1,1,1,1,1,1,1,1,1,1,1,1,1,1,1,1,1,1,1,1,1,1,1,1,4),(0.,0.0460148164544132),
(11.6154215191109,12.6130758144294,13.6107301097479,14.6083844050664,15.6060387003849,
16.6036929957034,17.601347291022,18.5990015863405,19.596655881659,20.5943101769775,
21.591964472296,22.5896187676145,23.587273062933,24.5849273582515,25.58258165357,
26.5802359488886,27.5778902442071,28.5755445395256,29.5731988348441,30.5708531301626,
31.5685074254811,32.5661617207996,33.5638160161181,34.5614703114366,35.5591246067551,
36.5567789020737,37.5544331973922,38.5520874927107,39.5497417880292,40.5473960833477,
41.5450503786662,42.5427046739847,43.5403589693032,44.5380132646217,45.5356675599403,
46.5333218552588,47.5309761505773,48.5286304458958,49.5262847412143,50.5239390365328,
51.5215933318513,52.5192476271698,53.5169019224883,54.5145562178069,55.5122105131254,
56.5098648084439,57.5075191037624,58.5051733990809,59.5028276943994,60.5004819897179,
61.4981362850364,62.4957905803549,63.4934448756734,64.491099170992,65.4887534663105,
66.486407761629,67.4840620569475,68.481716352266,69.4793706475845,70.477024942903,
71.4746792382215,72.4723335335401,73.4699878288586,74.4676421241771,75.4652964194956,
76.4629507148141,77.4606050101326,78.4582593054511,79.4559136007696,80.4535678960881,
81.4512221914066,82.4488764867252,83.4465307820437,84.4441850773622,85.4418393726807,
86.4394936679992,87.4371479633177,88.4348022586362,89.4324565539547,90.4301108492732,
91.4277651445918,92.4254194399103,93.4230737352288,94.4207280305473,95.4183823258658,
96.4160366211843,97.4136909165028,98.4113452118213,99.4089995071398,100.406653802458,
101.404308097777,102.401962393095,103.399616688414,104.397270983732,105.394925279051,
106.392579574369,107.390233869688,108.387888165006,109.385542460325,110.383196755643,
111.380851050962,112.37850534628,113.376159641599,114.373813936918,115.371468232236,
116.369122527555,117.366776822873,118.364431118192,119.36208541351,120.359739708829,
121.357394004147,122.355048299466,123.352702594784,124.350356890103,125.348011185421,
126.34566548074,127.343319776058,128.340974071377,129.338628366695,130.336282662014,
131.333936957332,132.331591252651,133.329245547969,134.326899843288,135.324554138606,
136.322208433925,137.319862729243,138.317517024562,139.31517131988,140.312825615199,
141.310479910517,142.308134205836,143.305788501154,144.303442796473,145.301097091791,
146.29875138711,147.296405682428,148.294059977747,149.291714273065,150.289368568384,
151.287022863702,152.284677159021,153.282331454339,154.279985749658,155.277640044976,
156.275294340295,157.272948635613,158.270602930932,159.268257226251,160.265911521569,
161.263565816888,162.261220112206,163.258874407525,164.256528702843,165.254182998162,
166.25183729348,167.249491588799,168.247145884117,169.244800179436,170.242454474754,
171.240108770073,172.237763065391,173.23541736071,174.233071656028,175.230725951347,
176.228380246665,177.226034541984,178.223688837302,179.221343132621,180.218997427939,
181.216651723258,182.214306018576,183.211960313895,184.209614609213,185.207268904532,
186.20492319985,187.202577495169,188.200231790487,189.197886085806,190.195540381124,
191.193194676443,192.190848971761,193.18850326708,194.186157562398,195.183811857717,
196.181466153035,197.179120448354,198.176774743672,199.174429038991,200.172083334309,
201.169737629628,202.167391924946,203.165046220265,204.162700515584,205.160354810902,
206.158009106221,207.155663401539,208.153317696858,209.150971992176,210.148626287495,
211.146280582813,212.143934878132,213.14158917345,214.139243468769,215.136897764087,
216.134552059406,217.132206354724,218.129860650043,219.127514945361,220.12516924068,
221.122823535998,222.120477831317,223.118132126635,224.115786421954,225.113440717272,
226.111095012591,227.108749307909,228.106403603228,229.104057898546),
 .UNSPECIFIED.);
#175=B_SPLINE_CURVE_WITH_KNOTS('',3,(#7263,#7264,#7265,#7266,#7267,#7268,
#7269,#7270,#7271,#7272),.UNSPECIFIED.,.F.,.F.,(4,3,3,4),(-4.0925417488383,
-3.99061718127404,-2.99296288595553,-2.06514013327811),.UNSPECIFIED.);
#176=B_SPLINE_CURVE_WITH_KNOTS('',3,(#7275,#7276,#7277,#7278,#7279,#7280,
#7281),.UNSPECIFIED.,.F.,.F.,(4,3,4),(0.,0.997654295318505,1.11419103802989),
 .UNSPECIFIED.);
#177=B_SPLINE_CURVE_WITH_KNOTS('',3,(#7286,#7287,#7288,#7289,#7290,#7291,
#7292,#7293,#7294,#7295,#7296,#7297,#7298,#7299,#7300,#7301,#7302,#7303,
#7304,#7305,#7306,#7307),.UNSPECIFIED.,.F.,.F.,(4,3,3,3,3,3,3,4),(-10.3757270560179,
-9.97654295318511,-8.9788886578666,-7.98123436254809,-6.98358006722958,
-5.98592577191107,-4.98827147659255,-4.0925417488383),.UNSPECIFIED.);
#178=B_SPLINE_CURVE_WITH_KNOTS('',3,(#7308,#7309,#7310,#7311,#7312,#7313,
#7314,#7315,#7316,#7317,#7318,#7319,#7320,#7321,#7322,#7323,#7324,#7325,
#7326,#7327,#7328,#7329),.UNSPECIFIED.,.F.,.F.,(4,3,3,3,3,3,3,4),(1.11419103802989,
1.99530859063702,2.99296288595553,3.99061718127404,4.98827147659255,5.98592577191106,
6.98358006722958,7.39737634520948),.UNSPECIFIED.);
#179=B_SPLINE_CURVE_WITH_KNOTS('',3,(#7334,#7335,#7336,#7337,#7338,#7339,
#7340,#7341,#7342,#7343,#7344,#7345,#7346,#7347,#7348,#7349,#7350,#7351,
#7352,#7353,#7354,#7355),.UNSPECIFIED.,.F.,.F.,(4,3,3,3,3,3,3,4),(-16.6589123631975,
-15.9624687250962,-14.9648144297777,-13.9671601344592,-12.9695058391406,
-11.9718515438221,-10.9741972485036,-10.3757270560179),.UNSPECIFIED.);
#180=B_SPLINE_CURVE_WITH_KNOTS('',3,(#7356,#7357,#7358,#7359,#7360,#7361,
#7362,#7363,#7364,#7365,#7366,#7367,#7368,#7369,#7370,#7371,#7372,#7373,
#7374,#7375,#7376,#7377),.UNSPECIFIED.,.F.,.F.,(4,3,3,3,3,3,3,4),(7.39737634520948,
7.98123436254809,8.97888865786661,9.97654295318512,10.9741972485036,11.9718515438221,
12.9695058391407,13.6805616523891),.UNSPECIFIED.);
#181=B_SPLINE_CURVE_WITH_KNOTS('',3,(#7382,#7383,#7384,#7385,#7386,#7387,
#7388,#7389,#7390,#7391,#7392,#7393,#7394,#7395,#7396,#7397,#7398,#7399,
#7400,#7401,#7402,#7403),.UNSPECIFIED.,.F.,.F.,(4,3,3,3,3,3,3,4),(-22.9420976703771,
-21.9483944970072,-20.9507402016887,-19.9530859063702,-18.9554316110517,
-17.9577773157332,-16.9601230204147,-16.6589123631975),.UNSPECIFIED.);
#182=B_SPLINE_CURVE_WITH_KNOTS('',3,(#7404,#7405,#7406,#7407,#7408,#7409,
#7410,#7411,#7412,#7413,#7414,#7415,#7416,#7417,#7418,#7419,#7420,#7421,
#7422,#7423,#7424,#7425,#7426,#7427,#7428),.UNSPECIFIED.,.F.,.F.,(4,3,3,
3,3,3,3,3,4),(13.6805616523891,13.9671601344592,14.9648144297777,15.9624687250962,
16.9601230204147,17.9577773157332,18.9554316110517,19.9530859063702,19.9637469595687),
 .UNSPECIFIED.);
#183=B_SPLINE_CURVE_WITH_KNOTS('',3,(#7433,#7434,#7435,#7436,#7437,#7438,
#7439,#7440,#7441,#7442,#7443,#7444,#7445,#7446,#7447,#7448,#7449,#7450,
#7451,#7452,#7453,#7454),.UNSPECIFIED.,.F.,.F.,(4,3,3,3,3,3,3,4),(-29.2252829775566,
-28.9319745642368,-27.9343202689183,-26.9366659735998,-25.9390116782813,
-24.9413573829628,-23.9437030876443,-22.9420976703771),.UNSPECIFIED.);
#184=B_SPLINE_CURVE_WITH_KNOTS('',3,(#7455,#7456,#7457,#7458,#7459,#7460,
#7461,#7462,#7463,#7464,#7465,#7466,#7467,#7468,#7469,#7470,#7471,#7472,
#7473,#7474,#7475,#7476),.UNSPECIFIED.,.F.,.F.,(4,3,3,3,3,3,3,4),(19.9637469595687,
20.9507402016887,21.9483944970072,22.9460487923258,23.9437030876443,24.9413573829628,
25.9390116782813,26.2469322667482),.UNSPECIFIED.);
#185=B_SPLINE_CURVE_WITH_KNOTS('',3,(#7481,#7482,#7483,#7484,#7485,#7486,
#7487,#7488,#7489,#7490,#7491,#7492,#7493,#7494,#7495,#7496,#7497,#7498,
#7499,#7500,#7501,#7502),.UNSPECIFIED.,.F.,.F.,(4,3,3,3,3,3,3,4),(-35.5084682847362,
-34.9179003361479,-33.9202460408294,-32.9225917455109,-31.9249374501923,
-30.9272831548738,-29.9296288595553,-29.2252829775566),.UNSPECIFIED.);
#186=B_SPLINE_CURVE_WITH_KNOTS('',3,(#7503,#7504,#7505,#7506,#7507,#7508,
#7509,#7510,#7511,#7512,#7513,#7514,#7515,#7516,#7517,#7518,#7519,#7520,
#7521,#7522,#7523,#7524),.UNSPECIFIED.,.F.,.F.,(4,3,3,3,3,3,3,4),(26.2469322667482,
26.9366659735998,27.9343202689183,28.9319745642368,29.9296288595553,30.9272831548739,
31.9249374501924,32.5301175739278),.UNSPECIFIED.);
#187=B_SPLINE_CURVE_WITH_KNOTS('',3,(#7529,#7530,#7531,#7532,#7533,#7534,
#7535,#7536,#7537,#7538,#7539,#7540,#7541,#7542,#7543,#7544,#7545,#7546,
#7547,#7548,#7549,#7550),.UNSPECIFIED.,.F.,.F.,(4,3,3,3,3,3,3,4),(-41.7916535919158,
-40.903826108059,-39.9061718127404,-38.9085175174219,-37.9108632221034,
-36.9132089267849,-35.9155546314664,-35.5084682847362),.UNSPECIFIED.);
#188=B_SPLINE_CURVE_WITH_KNOTS('',3,(#7551,#7552,#7553,#7554,#7555,#7556,
#7557,#7558,#7559,#7560,#7561,#7562,#7563,#7564,#7565,#7566,#7567,#7568,
#7569,#7570,#7571,#7572),.UNSPECIFIED.,.F.,.F.,(4,3,3,3,3,3,3,4),(32.5301175739278,
32.9225917455109,33.9202460408294,34.9179003361479,35.9155546314664,36.9132089267849,
37.9108632221034,38.8133028811074),.UNSPECIFIED.);
#189=B_SPLINE_CURVE_WITH_KNOTS('',3,(#7577,#7578,#7579,#7580,#7581,#7582,
#7583,#7584,#7585,#7586,#7587,#7588,#7589,#7590,#7591,#7592,#7593,#7594,
#7595,#7596,#7597,#7598,#7599,#7600,#7601),.UNSPECIFIED.,.F.,.F.,(4,3,3,
3,3,3,3,3,4),(-48.0748388990954,-47.8874061752885,-46.88975187997,-45.8920975846515,
-44.894443289333,-43.8967889940145,-42.899134698696,-41.9014804033775,-41.7916535919158),
 .UNSPECIFIED.);
#190=B_SPLINE_CURVE_WITH_KNOTS('',3,(#7602,#7603,#7604,#7605,#7606,#7607,
#7608,#7609,#7610,#7611,#7612,#7613,#7614,#7615,#7616,#7617,#7618,#7619,
#7620,#7621,#7622,#7623,#7624,#7625,#7626),.UNSPECIFIED.,.F.,.F.,(4,3,3,
3,3,3,3,3,4),(38.8133028811074,38.908517517422,39.9061718127405,40.903826108059,
41.9014804033775,42.899134698696,43.8967889940145,44.894443289333,45.096488188287),
 .UNSPECIFIED.);
#191=B_SPLINE_CURVE_WITH_KNOTS('',3,(#7631,#7632,#7633,#7634,#7635,#7636,
#7637,#7638,#7639,#7640,#7641,#7642,#7643,#7644,#7645,#7646,#7647,#7648,
#7649,#7650,#7651,#7652),.UNSPECIFIED.,.F.,.F.,(4,3,3,3,3,3,3,4),(-54.358024206275,
-53.8733319471996,-52.8756776518811,-51.8780233565626,-50.8803690612441,
-49.8827147659256,-48.885060470607,-48.0748388990954),.UNSPECIFIED.);
#192=B_SPLINE_CURVE_WITH_KNOTS('',3,(#7653,#7654,#7655,#7656,#7657,#7658,
#7659,#7660,#7661,#7662,#7663,#7664,#7665,#7666,#7667,#7668,#7669,#7670,
#7671,#7672,#7673,#7674),.UNSPECIFIED.,.F.,.F.,(4,3,3,3,3,3,3,4),(45.096488188287,
45.8920975846515,46.8897518799701,47.8874061752886,48.8850604706071,49.8827147659256,
50.8803690612441,51.3796734954666),.UNSPECIFIED.);
#193=B_SPLINE_CURVE_WITH_KNOTS('',3,(#7679,#7680,#7681,#7682,#7683,#7684,
#7685,#7686,#7687,#7688,#7689,#7690,#7691,#7692,#7693,#7694,#7695,#7696,
#7697,#7698,#7699,#7700),.UNSPECIFIED.,.F.,.F.,(4,3,3,3,3,3,3,4),(-60.6412095134546,
-59.8592577191107,-58.8616034237921,-57.8639491284736,-56.8662948331551,
-55.8686405378366,-54.8709862425181,-54.358024206275),.UNSPECIFIED.);
#194=B_SPLINE_CURVE_WITH_KNOTS('',3,(#7701,#7702,#7703,#7704,#7705,#7706,
#7707,#7708,#7709,#7710,#7711,#7712,#7713,#7714,#7715,#7716,#7717,#7718,
#7719,#7720,#7721,#7722),.UNSPECIFIED.,.F.,.F.,(4,3,3,3,3,3,3,4),(51.3796734954666,
51.8780233565626,52.8756776518811,53.8733319471996,54.8709862425181,55.8686405378366,
56.8662948331552,57.6628588026462),.UNSPECIFIED.);
#195=B_SPLINE_CURVE_WITH_KNOTS('',3,(#7727,#7728,#7729,#7730,#7731,#7732,
#7733,#7734,#7735,#7736,#7737,#7738,#7739,#7740,#7741,#7742,#7743,#7744,
#7745,#7746,#7747,#7748,#7749,#7750,#7751),.UNSPECIFIED.,.F.,.F.,(4,3,3,
3,3,3,3,3,4),(-66.9243948206342,-66.8428377863402,-65.8451834910217,-64.8475291957032,
-63.8498749003847,-62.8522206050662,-61.8545663097477,-60.8569120144292,
-60.6412095134546),.UNSPECIFIED.);
#196=B_SPLINE_CURVE_WITH_KNOTS('',3,(#7752,#7753,#7754,#7755,#7756,#7757,
#7758,#7759,#7760,#7761,#7762,#7763,#7764,#7765,#7766,#7767,#7768,#7769,
#7770,#7771,#7772,#7773,#7774,#7775,#7776),.UNSPECIFIED.,.F.,.F.,(4,3,3,
3,3,3,3,3,4),(57.6628588026462,57.8639491284737,58.8616034237922,59.8592577191107,
60.8569120144292,61.8545663097477,62.8522206050662,63.8498749003847,63.9460441098258),
 .UNSPECIFIED.);
#197=B_SPLINE_CURVE_WITH_KNOTS('',3,(#7781,#7782,#7783,#7784,#7785,#7786,
#7787,#7788,#7789,#7790,#7791,#7792,#7793,#7794,#7795,#7796,#7797,#7798,
#7799,#7800,#7801,#7802),.UNSPECIFIED.,.F.,.F.,(4,3,3,3,3,3,3,4),(-73.2075801278138,
-72.8287635582513,-71.8311092629328,-70.8334549676143,-69.8358006722958,
-68.8381463769772,-67.8404920816587,-66.9243948206342),.UNSPECIFIED.);
#198=B_SPLINE_CURVE_WITH_KNOTS('',3,(#7803,#7804,#7805,#7806,#7807,#7808,
#7809,#7810,#7811,#7812,#7813,#7814,#7815,#7816,#7817,#7818,#7819,#7820,
#7821,#7822,#7823,#7824),.UNSPECIFIED.,.F.,.F.,(4,3,3,3,3,3,3,4),(63.9460441098258,
64.8475291957032,65.8451834910218,66.8428377863403,67.8404920816588,68.8381463769773,
69.8358006722958,70.2292294170054),.UNSPECIFIED.);
#199=B_SPLINE_CURVE_WITH_KNOTS('',3,(#7829,#7830,#7831,#7832,#7833,#7834,
#7835,#7836,#7837,#7838,#7839,#7840,#7841,#7842,#7843,#7844,#7845,#7846,
#7847,#7848,#7849,#7850),.UNSPECIFIED.,.F.,.F.,(4,3,3,3,3,3,3,4),(-79.4907654349934,
-78.8146893301624,-77.8170350348439,-76.8193807395253,-75.8217264442068,
-74.8240721488883,-73.8264178535698,-73.2075801278138),.UNSPECIFIED.);
#200=B_SPLINE_CURVE_WITH_KNOTS('',3,(#7851,#7852,#7853,#7854,#7855,#7856,
#7857,#7858,#7859,#7860,#7861,#7862,#7863,#7864,#7865,#7866,#7867,#7868,
#7869,#7870,#7871,#7872),.UNSPECIFIED.,.F.,.F.,(4,3,3,3,3,3,3,4),(70.2292294170054,
70.8334549676143,71.8311092629328,72.8287635582514,73.8264178535699,74.8240721488884,
75.8217264442069,76.512414724185),.UNSPECIFIED.);
#201=B_SPLINE_CURVE_WITH_KNOTS('',3,(#7877,#7878,#7879,#7880,#7881,#7882,
#7883,#7884,#7885,#7886,#7887,#7888,#7889,#7890,#7891,#7892,#7893,#7894,
#7895,#7896,#7897,#7898),.UNSPECIFIED.,.F.,.F.,(4,3,3,3,3,3,3,4),(-85.773950742173,
-84.8006151020734,-83.8029608067549,-82.8053065114364,-81.8076522161179,
-80.8099979207994,-79.8123436254809,-79.4907654349934),.UNSPECIFIED.);
#202=B_SPLINE_CURVE_WITH_KNOTS('',3,(#7899,#7900,#7901,#7902,#7903,#7904,
#7905,#7906,#7907,#7908,#7909,#7910,#7911,#7912,#7913,#7914,#7915,#7916,
#7917,#7918,#7919,#7920),.UNSPECIFIED.,.F.,.F.,(4,3,3,3,3,3,3,4),(76.512414724185,
76.8193807395254,77.8170350348439,78.8146893301624,79.8123436254809,80.8099979207994,
81.8076522161179,82.7956000313646),.UNSPECIFIED.);
#203=B_SPLINE_CURVE_WITH_KNOTS('',3,(#7925,#7926,#7927,#7928,#7929,#7930,
#7931,#7932,#7933,#7934,#7935,#7936,#7937,#7938,#7939,#7940,#7941,#7942,
#7943,#7944,#7945,#7946,#7947,#7948,#7949),.UNSPECIFIED.,.F.,.F.,(4,3,3,
3,3,3,3,3,4),(-92.0571360493526,-91.784195169303,-90.7865408739845,-89.788886578666,
-88.7912322833475,-87.793577988029,-86.7959236927104,-85.7982693973919,
-85.773950742173),.UNSPECIFIED.);
#204=B_SPLINE_CURVE_WITH_KNOTS('',3,(#7950,#7951,#7952,#7953,#7954,#7955,
#7956,#7957,#7958,#7959,#7960,#7961,#7962,#7963,#7964,#7965,#7966,#7967,
#7968,#7969,#7970,#7971,#7972,#7973,#7974),.UNSPECIFIED.,.F.,.F.,(4,3,3,
3,3,3,3,3,4),(82.7956000313646,82.8053065114364,83.802960806755,84.8006151020735,
85.798269397392,86.7959236927105,87.793577988029,88.7912322833475,89.0787853385442),
 .UNSPECIFIED.);
#205=B_SPLINE_CURVE_WITH_KNOTS('',3,(#7979,#7980,#7981,#7982,#7983,#7984,
#7985,#7986,#7987,#7988,#7989,#7990,#7991,#7992,#7993,#7994,#7995,#7996,
#7997,#7998,#7999,#8000),.UNSPECIFIED.,.F.,.F.,(4,3,3,3,3,3,3,4),(-98.3403213565322,
-97.7701209412141,-96.7724666458956,-95.7748123505771,-94.7771580552585,
-93.77950375994,-92.7818494646215,-92.0571360493526),.UNSPECIFIED.);
#206=B_SPLINE_CURVE_WITH_KNOTS('',3,(#8001,#8002,#8003,#8004,#8005,#8006,
#8007,#8008,#8009,#8010,#8011,#8012,#8013,#8014,#8015,#8016,#8017,#8018,
#8019,#8020,#8021,#8022),.UNSPECIFIED.,.F.,.F.,(4,3,3,3,3,3,3,4),(89.0787853385442,
89.7888865786661,90.7865408739846,91.7841951693031,92.7818494646216,93.7795037599401,
94.7771580552586,95.3619706457238),.UNSPECIFIED.);
#207=B_SPLINE_CURVE_WITH_KNOTS('',3,(#8027,#8028,#8029,#8030,#8031,#8032,
#8033,#8034,#8035,#8036,#8037,#8038,#8039,#8040,#8041,#8042,#8043,#8044,
#8045,#8046,#8047,#8048),.UNSPECIFIED.,.F.,.F.,(4,3,3,3,3,3,3,4),(-104.623506663712,
-103.756046713125,-102.758392417807,-101.760738122488,-100.76308382717,
-99.7654295318511,-98.7677752365326,-98.3403213565322),.UNSPECIFIED.);
#208=B_SPLINE_CURVE_WITH_KNOTS('',3,(#8049,#8050,#8051,#8052,#8053,#8054,
#8055,#8056,#8057,#8058,#8059,#8060,#8061,#8062,#8063,#8064,#8065,#8066,
#8067,#8068,#8069,#8070),.UNSPECIFIED.,.F.,.F.,(4,3,3,3,3,3,3,4),(95.3619706457238,
95.7748123505771,96.7724666458956,97.7701209412141,98.7677752365326,99.7654295318512,
100.76308382717,101.645155952903),.UNSPECIFIED.);
#209=B_SPLINE_CURVE_WITH_KNOTS('',3,(#8075,#8076,#8077,#8078,#8079,#8080,
#8081,#8082,#8083,#8084,#8085,#8086,#8087,#8088,#8089,#8090,#8091,#8092,
#8093,#8094,#8095,#8096,#8097,#8098,#8099),.UNSPECIFIED.,.F.,.F.,(4,3,3,
3,3,3,3,3,4),(-110.906691970891,-110.739626780355,-109.741972485036,-108.744318189718,
-107.746663894399,-106.749009599081,-105.751355303762,-104.753701008444,
-104.623506663712),.UNSPECIFIED.);
#210=B_SPLINE_CURVE_WITH_KNOTS('',3,(#8100,#8101,#8102,#8103,#8104,#8105,
#8106,#8107,#8108,#8109,#8110,#8111,#8112,#8113,#8114,#8115,#8116,#8117,
#8118,#8119,#8120,#8121,#8122,#8123,#8124),.UNSPECIFIED.,.F.,.F.,(4,3,3,
3,3,3,3,3,4),(101.645155952903,101.760738122488,102.758392417807,103.756046713125,
104.753701008444,105.751355303762,106.749009599081,107.746663894399,107.928341260083),
 .UNSPECIFIED.);
#211=B_SPLINE_CURVE_WITH_KNOTS('',3,(#8129,#8130,#8131,#8132,#8133,#8134,
#8135,#8136,#8137,#8138,#8139,#8140,#8141,#8142,#8143,#8144,#8145,#8146,
#8147,#8148,#8149,#8150),.UNSPECIFIED.,.F.,.F.,(4,3,3,3,3,3,3,4),(-117.189877278071,
-116.725552552266,-115.727898256947,-114.730243961629,-113.73258966631,
-112.734935370992,-111.737281075673,-110.906691970891),.UNSPECIFIED.);
#212=B_SPLINE_CURVE_WITH_KNOTS('',3,(#8151,#8152,#8153,#8154,#8155,#8156,
#8157,#8158,#8159,#8160,#8161,#8162,#8163,#8164,#8165,#8166,#8167,#8168,
#8169,#8170,#8171,#8172),.UNSPECIFIED.,.F.,.F.,(4,3,3,3,3,3,3,4),(107.928341260083,
108.744318189718,109.741972485036,110.739626780355,111.737281075673,112.734935370992,
113.73258966631,114.211526567263),.UNSPECIFIED.);
#213=B_SPLINE_CURVE_WITH_KNOTS('',3,(#8177,#8178,#8179,#8180,#8181,#8182,
#8183,#8184,#8185,#8186,#8187,#8188,#8189,#8190,#8191,#8192,#8193,#8194,
#8195,#8196,#8197,#8198),.UNSPECIFIED.,.F.,.F.,(4,3,3,3,3,3,3,4),(-123.473062585251,
-122.711478324177,-121.713824028858,-120.71616973354,-119.718515438221,
-118.720861142903,-117.723206847584,-117.189877278071),.UNSPECIFIED.);
#214=B_SPLINE_CURVE_WITH_KNOTS('',3,(#8199,#8200,#8201,#8202,#8203,#8204,
#8205,#8206,#8207,#8208,#8209,#8210,#8211,#8212,#8213,#8214,#8215,#8216,
#8217,#8218,#8219,#8220),.UNSPECIFIED.,.F.,.F.,(4,3,3,3,3,3,3,4),(114.211526567263,
114.730243961629,115.727898256947,116.725552552266,117.723206847584,118.720861142903,
119.718515438221,120.494711874442),.UNSPECIFIED.);
#215=B_SPLINE_CURVE_WITH_KNOTS('',3,(#8225,#8226,#8227,#8228,#8229,#8230,
#8231,#8232,#8233,#8234,#8235,#8236,#8237,#8238,#8239,#8240,#8241,#8242,
#8243,#8244,#8245,#8246,#8247,#8248,#8249),.UNSPECIFIED.,.F.,.F.,(4,3,3,
3,3,3,3,3,4),(-129.75624789243,-129.695058391406,-128.697404096088,-127.699749800769,
-126.702095505451,-125.704441210132,-124.706786914814,-123.709132619495,
-123.473062585251),.UNSPECIFIED.);
#216=B_SPLINE_CURVE_WITH_KNOTS('',3,(#8250,#8251,#8252,#8253,#8254,#8255,
#8256,#8257,#8258,#8259,#8260,#8261,#8262,#8263,#8264,#8265,#8266,#8267,
#8268,#8269,#8270,#8271,#8272,#8273,#8274),.UNSPECIFIED.,.F.,.F.,(4,3,3,
3,3,3,3,3,4),(120.494711874442,120.71616973354,121.713824028858,122.711478324177,
123.709132619495,124.706786914814,125.704441210132,126.702095505451,126.777897181622),
 .UNSPECIFIED.);
#217=B_SPLINE_CURVE_WITH_KNOTS('',3,(#8279,#8280,#8281,#8282,#8283,#8284,
#8285,#8286,#8287,#8288,#8289,#8290,#8291,#8292,#8293,#8294,#8295,#8296,
#8297,#8298,#8299,#8300),.UNSPECIFIED.,.F.,.F.,(4,3,3,3,3,3,3,4),(-136.03943319961,
-135.680984163318,-134.683329867999,-133.68567557268,-132.688021277362,
-131.690366982043,-130.692712686725,-129.75624789243),.UNSPECIFIED.);
#218=B_SPLINE_CURVE_WITH_KNOTS('',3,(#8301,#8302,#8303,#8304,#8305,#8306,
#8307,#8308,#8309,#8310,#8311,#8312,#8313,#8314,#8315,#8316,#8317,#8318,
#8319,#8320,#8321,#8322),.UNSPECIFIED.,.F.,.F.,(4,3,3,3,3,3,3,4),(126.777897181622,
127.699749800769,128.697404096088,129.695058391406,130.692712686725,131.690366982044,
132.688021277362,133.061082488801),.UNSPECIFIED.);
#219=B_SPLINE_CURVE_WITH_KNOTS('',3,(#8327,#8328,#8329,#8330,#8331,#8332,
#8333,#8334,#8335,#8336,#8337,#8338,#8339,#8340,#8341,#8342,#8343,#8344,
#8345,#8346,#8347,#8348),.UNSPECIFIED.,.F.,.F.,(4,3,3,3,3,3,3,4),(-142.322618506789,
-141.666909935229,-140.66925563991,-139.671601344592,-138.673947049273,
-137.676292753955,-136.678638458636,-136.03943319961),.UNSPECIFIED.);
#220=B_SPLINE_CURVE_WITH_KNOTS('',3,(#8349,#8350,#8351,#8352,#8353,#8354,
#8355,#8356,#8357,#8358,#8359,#8360,#8361,#8362,#8363,#8364,#8365,#8366,
#8367,#8368,#8369,#8370),.UNSPECIFIED.,.F.,.F.,(4,3,3,3,3,3,3,4),(133.061082488801,
133.685675572681,134.683329867999,135.680984163318,136.678638458636,137.676292753955,
138.673947049273,139.344267795981),.UNSPECIFIED.);
#221=B_SPLINE_CURVE_WITH_KNOTS('',3,(#8375,#8376,#8377,#8378,#8379,#8380,
#8381,#8382,#8383,#8384,#8385,#8386,#8387,#8388,#8389,#8390,#8391,#8392,
#8393,#8394,#8395,#8396),.UNSPECIFIED.,.F.,.F.,(4,3,3,3,3,3,3,4),(-148.605803813969,
-147.65283570714,-146.655181411821,-145.657527116503,-144.659872821184,
-143.662218525866,-142.664564230547,-142.322618506789),.UNSPECIFIED.);
#222=B_SPLINE_CURVE_WITH_KNOTS('',3,(#8397,#8398,#8399,#8400,#8401,#8402,
#8403,#8404,#8405,#8406,#8407,#8408,#8409,#8410,#8411,#8412,#8413,#8414,
#8415,#8416,#8417,#8418),.UNSPECIFIED.,.F.,.F.,(4,3,3,3,3,3,3,4),(139.344267795981,
139.671601344592,140.66925563991,141.666909935229,142.664564230547,143.662218525866,
144.659872821184,145.62745310316),.UNSPECIFIED.);
#223=B_SPLINE_CURVE_WITH_KNOTS('',3,(#8423,#8424,#8425,#8426,#8427,#8428,
#8429,#8430,#8431,#8432,#8433,#8434,#8435,#8436,#8437,#8438,#8439,#8440,
#8441,#8442,#8443,#8444,#8445,#8446,#8447),.UNSPECIFIED.,.F.,.F.,(4,3,3,
3,3,3,3,3,4),(-154.888989121148,-154.636415774369,-153.638761479051,-152.641107183732,
-151.643452888414,-150.645798593095,-149.648144297777,-148.650490002458,
-148.605803813969),.UNSPECIFIED.);
#224=B_SPLINE_CURVE_WITH_KNOTS('',3,(#8448,#8449,#8450,#8451,#8452,#8453,
#8454,#8455,#8456,#8457,#8458,#8459,#8460,#8461,#8462,#8463,#8464,#8465,
#8466,#8467,#8468,#8469,#8470,#8471,#8472),.UNSPECIFIED.,.F.,.F.,(4,3,3,
3,3,3,3,3,4),(145.62745310316,145.657527116503,146.655181411821,147.65283570714,
148.650490002458,149.648144297777,150.645798593095,151.643452888414,151.91063841034),
 .UNSPECIFIED.);
#225=B_SPLINE_CURVE_WITH_KNOTS('',3,(#8477,#8478,#8479,#8480,#8481,#8482,
#8483,#8484,#8485,#8486,#8487,#8488,#8489,#8490,#8491,#8492,#8493,#8494,
#8495,#8496,#8497,#8498),.UNSPECIFIED.,.F.,.F.,(4,3,3,3,3,3,3,4),(-161.172174428328,
-160.62234154628,-159.624687250962,-158.627032955643,-157.629378660325,
-156.631724365006,-155.634070069688,-154.888989121148),.UNSPECIFIED.);
#226=B_SPLINE_CURVE_WITH_KNOTS('',3,(#8499,#8500,#8501,#8502,#8503,#8504,
#8505,#8506,#8507,#8508,#8509,#8510,#8511,#8512,#8513,#8514,#8515,#8516,
#8517,#8518,#8519,#8520),.UNSPECIFIED.,.F.,.F.,(4,3,3,3,3,3,3,4),(151.91063841034,
152.641107183732,153.638761479051,154.636415774369,155.634070069688,156.631724365006,
157.629378660325,158.19382371752),.UNSPECIFIED.);
#227=B_SPLINE_CURVE_WITH_KNOTS('',3,(#8525,#8526,#8527,#8528,#8529,#8530,
#8531,#8532,#8533,#8534,#8535,#8536,#8537,#8538,#8539,#8540,#8541,#8542,
#8543,#8544,#8545,#8546),.UNSPECIFIED.,.F.,.F.,(4,3,3,3,3,3,3,4),(-167.455359735508,
-166.608267318191,-165.610613022873,-164.612958727554,-163.615304432236,
-162.617650136917,-161.619995841599,-161.172174428328),.UNSPECIFIED.);
#228=B_SPLINE_CURVE_WITH_KNOTS('',3,(#8547,#8548,#8549,#8550,#8551,#8552,
#8553,#8554,#8555,#8556,#8557,#8558,#8559,#8560,#8561,#8562,#8563,#8564,
#8565,#8566,#8567,#8568),.UNSPECIFIED.,.F.,.F.,(4,3,3,3,3,3,3,4),(158.19382371752,
158.627032955643,159.624687250962,160.62234154628,161.619995841599,162.617650136917,
163.615304432236,164.477009024699),.UNSPECIFIED.);
#229=B_SPLINE_CURVE_WITH_KNOTS('',3,(#8573,#8574,#8575,#8576,#8577,#8578,
#8579,#8580,#8581,#8582,#8583,#8584,#8585,#8586,#8587,#8588,#8589,#8590,
#8591,#8592,#8593,#8594,#8595,#8596,#8597),.UNSPECIFIED.,.F.,.F.,(4,3,3,
3,3,3,3,3,4),(-173.738545042687,-173.591847385421,-172.594193090102,-171.596538794784,
-170.598884499465,-169.601230204147,-168.603575908828,-167.60592161351,
-167.455359735508),.UNSPECIFIED.);
#230=B_SPLINE_CURVE_WITH_KNOTS('',3,(#8598,#8599,#8600,#8601,#8602,#8603,
#8604,#8605,#8606,#8607,#8608,#8609,#8610,#8611,#8612,#8613,#8614,#8615,
#8616,#8617,#8618,#8619,#8620,#8621,#8622),.UNSPECIFIED.,.F.,.F.,(4,3,3,
3,3,3,3,3,4),(164.477009024699,164.612958727554,165.610613022873,166.608267318191,
167.60592161351,168.603575908828,169.601230204147,170.598884499465,170.760194331879),
 .UNSPECIFIED.);
#231=B_SPLINE_CURVE_WITH_KNOTS('',3,(#8627,#8628,#8629,#8630,#8631,#8632,
#8633,#8634,#8635,#8636,#8637,#8638,#8639,#8640,#8641,#8642,#8643,#8644,
#8645,#8646,#8647,#8648),.UNSPECIFIED.,.F.,.F.,(4,3,3,3,3,3,3,4),(-180.021730349867,
-179.577773157332,-178.580118862013,-177.582464566695,-176.584810271376,
-175.587155976058,-174.589501680739,-173.738545042687),.UNSPECIFIED.);
#232=B_SPLINE_CURVE_WITH_KNOTS('',3,(#8649,#8650,#8651,#8652,#8653,#8654,
#8655,#8656,#8657,#8658,#8659,#8660,#8661,#8662,#8663,#8664,#8665,#8666,
#8667,#8668,#8669,#8670),.UNSPECIFIED.,.F.,.F.,(4,3,3,3,3,3,3,4),(170.760194331879,
171.596538794784,172.594193090102,173.591847385421,174.58950168074,175.587155976058,
176.584810271377,177.043379639058),.UNSPECIFIED.);
#233=B_SPLINE_CURVE_WITH_KNOTS('',3,(#8675,#8676,#8677,#8678,#8679,#8680,
#8681,#8682,#8683,#8684,#8685,#8686,#8687,#8688,#8689,#8690,#8691,#8692,
#8693,#8694,#8695,#8696),.UNSPECIFIED.,.F.,.F.,(4,3,3,3,3,3,3,4),(-186.304915657046,
-185.563698929243,-184.566044633925,-183.568390338606,-182.570736043288,
-181.573081747969,-180.575427452651,-180.021730349867),.UNSPECIFIED.);
#234=B_SPLINE_CURVE_WITH_KNOTS('',3,(#8697,#8698,#8699,#8700,#8701,#8702,
#8703,#8704,#8705,#8706,#8707,#8708,#8709,#8710,#8711,#8712,#8713,#8714,
#8715,#8716,#8717,#8718),.UNSPECIFIED.,.F.,.F.,(4,3,3,3,3,3,3,4),(177.043379639058,
177.582464566695,178.580118862014,179.577773157332,180.575427452651,181.573081747969,
182.570736043288,183.326564946238),.UNSPECIFIED.);
#235=B_SPLINE_CURVE_WITH_KNOTS('',3,(#8723,#8724,#8725,#8726,#8727,#8728,
#8729,#8730,#8731,#8732,#8733,#8734,#8735,#8736,#8737,#8738,#8739,#8740,
#8741,#8742,#8743,#8744,#8745,#8746,#8747),.UNSPECIFIED.,.F.,.F.,(4,3,3,
3,3,3,3,3,4),(-192.588100964226,-192.547278996473,-191.549624701154,-190.551970405836,
-189.554316110517,-188.556661815199,-187.55900751988,-186.561353224562,
-186.304915657046),.UNSPECIFIED.);
#236=B_SPLINE_CURVE_WITH_KNOTS('',3,(#8748,#8749,#8750,#8751,#8752,#8753,
#8754,#8755,#8756,#8757,#8758,#8759,#8760,#8761,#8762,#8763,#8764,#8765,
#8766,#8767,#8768,#8769,#8770,#8771,#8772),.UNSPECIFIED.,.F.,.F.,(4,3,3,
3,3,3,3,3,4),(183.326564946238,183.568390338606,184.566044633925,185.563698929243,
186.561353224562,187.55900751988,188.556661815199,189.554316110517,189.609750253417),
 .UNSPECIFIED.);
#237=B_SPLINE_CURVE_WITH_KNOTS('',3,(#8777,#8778,#8779,#8780,#8781,#8782,
#8783,#8784,#8785,#8786,#8787,#8788,#8789,#8790,#8791,#8792,#8793,#8794,
#8795,#8796,#8797,#8798),.UNSPECIFIED.,.F.,.F.,(4,3,3,3,3,3,3,4),(-198.871286271405,
-198.533204768384,-197.535550473065,-196.537896177747,-195.540241882428,
-194.54258758711,-193.544933291791,-192.588100964226),.UNSPECIFIED.);
#238=B_SPLINE_CURVE_WITH_KNOTS('',3,(#8799,#8800,#8801,#8802,#8803,#8804,
#8805,#8806,#8807,#8808,#8809,#8810,#8811,#8812,#8813,#8814,#8815,#8816,
#8817,#8818,#8819,#8820),.UNSPECIFIED.,.F.,.F.,(4,3,3,3,3,3,3,4),(189.609750253417,
190.551970405836,191.549624701154,192.547278996473,193.544933291791,194.54258758711,
195.540241882428,195.892935560597),.UNSPECIFIED.);
#239=B_SPLINE_CURVE_WITH_KNOTS('',3,(#8825,#8826,#8827,#8828,#8829,#8830,
#8831,#8832,#8833,#8834,#8835,#8836,#8837,#8838,#8839,#8840,#8841,#8842,
#8843,#8844,#8845,#8846),.UNSPECIFIED.,.F.,.F.,(4,3,3,3,3,3,3,4),(-205.154471578585,
-204.519130540295,-203.521476244976,-202.523821949658,-201.526167654339,
-200.528513359021,-199.530859063702,-198.871286271405),.UNSPECIFIED.);
#240=B_SPLINE_CURVE_WITH_KNOTS('',3,(#8847,#8848,#8849,#8850,#8851,#8852,
#8853,#8854,#8855,#8856,#8857,#8858,#8859,#8860,#8861,#8862,#8863,#8864,
#8865,#8866,#8867,#8868),.UNSPECIFIED.,.F.,.F.,(4,3,3,3,3,3,3,4),(195.892935560597,
196.537896177747,197.535550473065,198.533204768384,199.530859063702,200.528513359021,
201.526167654339,202.176120867777),.UNSPECIFIED.);
#241=B_SPLINE_CURVE_WITH_KNOTS('',3,(#8873,#8874,#8875,#8876,#8877,#8878,
#8879,#8880,#8881,#8882,#8883,#8884,#8885,#8886,#8887,#8888,#8889,#8890,
#8891,#8892,#8893,#8894),.UNSPECIFIED.,.F.,.F.,(4,3,3,3,3,3,3,4),(-211.437656885764,
-210.505056312206,-209.507402016887,-208.509747721569,-207.51209342625,
-206.514439130932,-205.516784835613,-205.154471578585),.UNSPECIFIED.);
#242=B_SPLINE_CURVE_WITH_KNOTS('',3,(#8895,#8896,#8897,#8898,#8899,#8900,
#8901,#8902,#8903,#8904,#8905,#8906,#8907,#8908,#8909,#8910,#8911,#8912,
#8913,#8914,#8915,#8916),.UNSPECIFIED.,.F.,.F.,(4,3,3,3,3,3,3,4),(202.176120867777,
202.523821949658,203.521476244976,204.519130540295,205.516784835613,206.514439130932,
207.51209342625,208.459306174956),.UNSPECIFIED.);
#243=B_SPLINE_CURVE_WITH_KNOTS('',3,(#8923,#8924,#8925,#8926,#8927,#8928,
#8929,#8930,#8931,#8932,#8933,#8934,#8935,#8936,#8937,#8938,#8939,#8940,
#8941,#8942,#8943,#8944),.UNSPECIFIED.,.F.,.F.,(4,3,3,3,3,3,3,4),(-217.488636379435,
-216.490982084117,-215.493327788798,-214.49567349348,-213.498019198161,
-212.500364902843,-211.502710607524,-211.437656885764),.UNSPECIFIED.);
#244=B_SPLINE_CURVE_WITH_KNOTS('',3,(#8945,#8946,#8947,#8948,#8949,#8950,
#8951,#8952,#8953,#8954,#8955,#8956,#8957,#8958,#8959,#8960,#8961,#8962,
#8963,#8964,#8965,#8966,#8967,#8968,#8969),.UNSPECIFIED.,.F.,.F.,(4,3,3,
3,3,3,3,3,4),(208.459306174956,208.509747721569,209.507402016887,210.505056312206,
211.502710607524,212.500364902843,213.498019198161,214.49567349348,214.742491482136),
 .UNSPECIFIED.);
#245=B_SPLINE_CURVE_WITH_KNOTS('',3,(#8975,#8976,#8977,#8978,#8979,#8980,
#8981,#8982),.UNSPECIFIED.,.F.,.F.,(4,1,1,1,1,4),(223.053078404875,223.118132126635,
224.115786421954,225.113440717272,226.111095012591,227.038917765268),
 .UNSPECIFIED.);
#246=B_SPLINE_CURVE_WITH_KNOTS('',3,(#8985,#8986,#8987,#8988,#8989,#8990),
 .UNSPECIFIED.,.F.,.F.,(4,1,1,4),(223.053078404875,223.803914711538,224.801569006857,
225.799223302175),.UNSPECIFIED.);
#247=B_SPLINE_CURVE_WITH_KNOTS('',3,(#8995,#8996,#8997,#8998,#8999,#9000,
#9001,#9002,#9003,#9004),.UNSPECIFIED.,.F.,.F.,(4,1,1,1,1,1,1,4),(216.769893097696,
217.132206354724,218.129860650043,219.127514945361,220.12516924068,221.122823535998,
222.120477831317,223.053078404875),.UNSPECIFIED.);
#248=B_SPLINE_CURVE_WITH_KNOTS('',3,(#9005,#9006,#9007,#9008,#9009,#9010,
#9011,#9012,#9013,#9014,#9015),.UNSPECIFIED.,.F.,.F.,(4,1,1,1,1,1,1,1,4),
(216.769893097696,216.820334644309,217.817988939627,218.815643234946,219.813297530264,
220.810951825583,221.808606120901,222.80626041622,223.053078404875),
 .UNSPECIFIED.);
#249=B_SPLINE_CURVE_WITH_KNOTS('',3,(#9020,#9021,#9022,#9023,#9024,#9025,
#9026,#9027,#9028,#9029),.UNSPECIFIED.,.F.,.F.,(4,1,1,1,1,1,1,4),(210.486707790516,
211.146280582813,212.143934878132,213.14158917345,214.139243468769,215.136897764087,
216.134552059406,216.769893097696),.UNSPECIFIED.);
#250=B_SPLINE_CURVE_WITH_KNOTS('',3,(#9030,#9031,#9032,#9033,#9034,#9035,
#9036,#9037,#9038,#9039),.UNSPECIFIED.,.F.,.F.,(4,1,1,1,1,1,1,4),(210.486707790516,
210.834408872398,211.832063167716,212.829717463035,213.827371758353,214.825026053672,
215.82268034899,216.769893097696),.UNSPECIFIED.);
#251=B_SPLINE_CURVE_WITH_KNOTS('',3,(#9044,#9045,#9046,#9047,#9048,#9049,
#9050,#9051,#9052,#9053),.UNSPECIFIED.,.F.,.F.,(4,1,1,1,1,1,1,4),(204.203522483337,
205.160354810902,206.158009106221,207.155663401539,208.153317696858,209.150971992176,
210.148626287495,210.486707790516),.UNSPECIFIED.);
#252=B_SPLINE_CURVE_WITH_KNOTS('',3,(#9054,#9055,#9056,#9057,#9058,#9059,
#9060,#9061,#9062,#9063),.UNSPECIFIED.,.F.,.F.,(4,1,1,1,1,1,1,4),(204.203522483337,
204.848483100487,205.846137395805,206.843791691124,207.841445986442,208.839100281761,
209.836754577079,210.486707790516),.UNSPECIFIED.);
#253=B_SPLINE_CURVE_WITH_KNOTS('',3,(#9068,#9069,#9070,#9071,#9072,#9073,
#9074,#9075,#9076,#9077,#9078),.UNSPECIFIED.,.F.,.F.,(4,1,1,1,1,1,1,1,4),
(197.920337176157,198.176774743672,199.174429038991,200.172083334309,201.169737629628,
202.167391924946,203.165046220265,204.162700515584,204.203522483337),
 .UNSPECIFIED.);
#254=B_SPLINE_CURVE_WITH_KNOTS('',3,(#9079,#9080,#9081,#9082,#9083,#9084,
#9085,#9086,#9087,#9088),.UNSPECIFIED.,.F.,.F.,(4,1,1,1,1,1,1,4),(197.920337176157,
198.862557328576,199.860211623894,200.857865919213,201.855520214531,202.85317450985,
203.850828805168,204.203522483337),.UNSPECIFIED.);
#255=B_SPLINE_CURVE_WITH_KNOTS('',3,(#9093,#9094,#9095,#9096,#9097,#9098,
#9099,#9100,#9101,#9102),.UNSPECIFIED.,.F.,.F.,(4,1,1,1,1,1,1,4),(191.637151868977,
192.190848971761,193.18850326708,194.186157562398,195.183811857717,196.181466153035,
197.179120448354,197.920337176157),.UNSPECIFIED.);
#256=B_SPLINE_CURVE_WITH_KNOTS('',3,(#9103,#9104,#9105,#9106,#9107,#9108,
#9109,#9110,#9111,#9112,#9113),.UNSPECIFIED.,.F.,.F.,(4,1,1,1,1,1,1,1,4),
(191.637151868977,191.878977261346,192.876631556665,193.874285851983,194.871940147302,
195.86959444262,196.867248737939,197.864903033257,197.920337176157),
 .UNSPECIFIED.);
#257=B_SPLINE_CURVE_WITH_KNOTS('',3,(#9118,#9119,#9120,#9121,#9122,#9123,
#9124,#9125,#9126,#9127),.UNSPECIFIED.,.F.,.F.,(4,1,1,1,1,1,1,4),(185.353966561798,
186.20492319985,187.202577495169,188.200231790487,189.197886085806,190.195540381124,
191.193194676443,191.637151868977),.UNSPECIFIED.);
#258=B_SPLINE_CURVE_WITH_KNOTS('',3,(#9128,#9129,#9130,#9131,#9132,#9133,
#9134,#9135,#9136,#9137),.UNSPECIFIED.,.F.,.F.,(4,1,1,1,1,1,1,4),(185.353966561798,
185.893051489435,186.890705784754,187.888360080072,188.886014375391,189.883668670709,
190.881322966028,191.637151868977),.UNSPECIFIED.);
#259=B_SPLINE_CURVE_WITH_KNOTS('',3,(#9142,#9143,#9144,#9145,#9146,#9147,
#9148,#9149,#9150,#9151,#9152),.UNSPECIFIED.,.F.,.F.,(4,1,1,1,1,1,1,1,4),
(179.070781254618,179.221343132621,180.218997427939,181.216651723258,182.214306018576,
183.211960313895,184.209614609213,185.207268904532,185.353966561798),
 .UNSPECIFIED.);
#260=B_SPLINE_CURVE_WITH_KNOTS('',3,(#9153,#9154,#9155,#9156,#9157,#9158,
#9159,#9160,#9161,#9162),.UNSPECIFIED.,.F.,.F.,(4,1,1,1,1,1,1,4),(179.070781254618,
179.907125717524,180.904780012842,181.902434308161,182.900088603479,183.897742898798,
184.895397194116,185.353966561798),.UNSPECIFIED.);
#261=B_SPLINE_CURVE_WITH_KNOTS('',3,(#9167,#9168,#9169,#9170,#9171,#9172,
#9173,#9174,#9175,#9176),.UNSPECIFIED.,.F.,.F.,(4,1,1,1,1,1,1,4),(172.787595947439,
173.23541736071,174.233071656028,175.230725951347,176.228380246665,177.226034541984,
178.223688837302,179.070781254618),.UNSPECIFIED.);
#262=B_SPLINE_CURVE_WITH_KNOTS('',3,(#9177,#9178,#9179,#9180,#9181,#9182,
#9183,#9184,#9185,#9186,#9187),.UNSPECIFIED.,.F.,.F.,(4,1,1,1,1,1,1,1,4),
(172.787595947439,172.923545650294,173.921199945613,174.918854240931,175.91650853625,
176.914162831568,177.911817126887,178.909471422205,179.070781254618),
 .UNSPECIFIED.);
#263=B_SPLINE_CURVE_WITH_KNOTS('',3,(#9192,#9193,#9194,#9195,#9196,#9197,
#9198,#9199,#9200,#9201),.UNSPECIFIED.,.F.,.F.,(4,1,1,1,1,1,1,4),(166.504410640259,
167.249491588799,168.247145884117,169.244800179436,170.242454474754,171.240108770073,
172.237763065391,172.787595947439),.UNSPECIFIED.);
#264=B_SPLINE_CURVE_WITH_KNOTS('',3,(#9202,#9203,#9204,#9205,#9206,#9207,
#9208,#9209,#9210,#9211),.UNSPECIFIED.,.F.,.F.,(4,1,1,1,1,1,1,4),(166.504410640259,
166.937619878383,167.935274173702,168.93292846902,169.930582764339,170.928237059657,
171.925891354976,172.787595947439),.UNSPECIFIED.);
#265=B_SPLINE_CURVE_WITH_KNOTS('',3,(#9216,#9217,#9218,#9219,#9220,#9221,
#9222,#9223,#9224,#9225,#9226),.UNSPECIFIED.,.F.,.F.,(4,1,1,1,1,1,1,1,4),
(160.22122533308,160.265911521569,161.263565816888,162.261220112206,163.258874407525,
164.256528702843,165.254182998162,166.25183729348,166.504410640259),
 .UNSPECIFIED.);
#266=B_SPLINE_CURVE_WITH_KNOTS('',3,(#9227,#9228,#9229,#9230,#9231,#9232,
#9233,#9234,#9235,#9236),.UNSPECIFIED.,.F.,.F.,(4,1,1,1,1,1,1,4),(160.22122533308,
160.951694106472,161.949348401791,162.947002697109,163.944656992428,164.942311287746,
165.939965583065,166.504410640259),.UNSPECIFIED.);
#267=B_SPLINE_CURVE_WITH_KNOTS('',3,(#9241,#9242,#9243,#9244,#9245,#9246,
#9247,#9248,#9249,#9250),.UNSPECIFIED.,.F.,.F.,(4,1,1,1,1,1,1,4),(153.9380400259,
154.279985749658,155.277640044976,156.275294340295,157.272948635613,158.270602930932,
159.268257226251,160.22122533308),.UNSPECIFIED.);
#268=B_SPLINE_CURVE_WITH_KNOTS('',3,(#9251,#9252,#9253,#9254,#9255,#9256,
#9257,#9258,#9259,#9260,#9261),.UNSPECIFIED.,.F.,.F.,(4,1,1,1,1,1,1,1,4),
(153.9380400259,153.968114039243,154.965768334561,155.96342262988,156.961076925198,
157.958731220517,158.956385515835,159.954039811154,160.22122533308),
 .UNSPECIFIED.);
#269=B_SPLINE_CURVE_WITH_KNOTS('',3,(#9266,#9267,#9268,#9269,#9270,#9271,
#9272,#9273,#9274,#9275),.UNSPECIFIED.,.F.,.F.,(4,1,1,1,1,1,1,4),(147.65485471872,
148.294059977747,149.291714273065,150.289368568384,151.287022863702,152.284677159021,
153.282331454339,153.9380400259),.UNSPECIFIED.);
#270=B_SPLINE_CURVE_WITH_KNOTS('',3,(#9276,#9277,#9278,#9279,#9280,#9281,
#9282,#9283,#9284,#9285),.UNSPECIFIED.,.F.,.F.,(4,1,1,1,1,1,1,4),(147.654854718721,
147.982188267332,148.97984256265,149.977496857969,150.975151153287,151.972805448606,
152.970459743924,153.9380400259),.UNSPECIFIED.);
#271=B_SPLINE_CURVE_WITH_KNOTS('',3,(#9290,#9291,#9292,#9293,#9294,#9295,
#9296,#9297,#9298,#9299),.UNSPECIFIED.,.F.,.F.,(4,1,1,1,1,1,1,4),(141.371669411541,
142.308134205836,143.305788501154,144.303442796473,145.301097091791,146.29875138711,
147.296405682428,147.65485471872),.UNSPECIFIED.);
#272=B_SPLINE_CURVE_WITH_KNOTS('',3,(#9300,#9301,#9302,#9303,#9304,#9305,
#9306,#9307,#9308,#9309),.UNSPECIFIED.,.F.,.F.,(4,1,1,1,1,1,1,4),(141.371669411541,
141.99626249542,142.993916790739,143.991571086058,144.989225381376,145.986879676695,
146.984533972013,147.654854718721),.UNSPECIFIED.);
#273=B_SPLINE_CURVE_WITH_KNOTS('',3,(#9314,#9315,#9316,#9317,#9318,#9319,
#9320,#9321,#9322,#9323,#9324),.UNSPECIFIED.,.F.,.F.,(4,1,1,1,1,1,1,1,4),
(135.088484104361,135.324554138606,136.322208433925,137.319862729243,138.317517024562,
139.31517131988,140.312825615199,141.310479910517,141.371669411541),
 .UNSPECIFIED.);
#274=B_SPLINE_CURVE_WITH_KNOTS('',3,(#9325,#9326,#9327,#9328,#9329,#9330,
#9331,#9332,#9333,#9334),.UNSPECIFIED.,.F.,.F.,(4,1,1,1,1,1,1,4),(135.088484104361,
136.010336723509,137.007991018828,138.005645314146,139.003299609465,140.000953904783,
140.998608200102,141.371669411541),.UNSPECIFIED.);
#275=B_SPLINE_CURVE_WITH_KNOTS('',3,(#9339,#9340,#9341,#9342,#9343,#9344,
#9345,#9346,#9347,#9348),.UNSPECIFIED.,.F.,.F.,(4,1,1,1,1,1,1,4),(128.805298797182,
129.338628366695,130.336282662014,131.333936957332,132.331591252651,133.329245547969,
134.326899843288,135.088484104361),.UNSPECIFIED.);
#276=B_SPLINE_CURVE_WITH_KNOTS('',3,(#9349,#9350,#9351,#9352,#9353,#9354,
#9355,#9356,#9357,#9358,#9359),.UNSPECIFIED.,.F.,.F.,(4,1,1,1,1,1,1,1,4),
(128.805298797182,129.02675665628,130.024410951598,131.022065246917,132.019719542235,
133.017373837554,134.015028132872,135.012682428191,135.088484104361),
 .UNSPECIFIED.);
#277=B_SPLINE_CURVE_WITH_KNOTS('',3,(#9364,#9365,#9366,#9367,#9368,#9369,
#9370,#9371,#9372,#9373),.UNSPECIFIED.,.F.,.F.,(4,1,1,1,1,1,1,4),(122.522113490002,
123.352702594784,124.350356890103,125.348011185421,126.34566548074,127.343319776058,
128.340974071377,128.805298797182),.UNSPECIFIED.);
#278=B_SPLINE_CURVE_WITH_KNOTS('',3,(#9374,#9375,#9376,#9377,#9378,#9379,
#9380,#9381,#9382,#9383),.UNSPECIFIED.,.F.,.F.,(4,1,1,1,1,1,1,4),(122.522113490002,
123.040830884369,124.038485179687,125.036139475006,126.033793770324,127.031448065643,
128.029102360961,128.805298797182),.UNSPECIFIED.);
#279=B_SPLINE_CURVE_WITH_KNOTS('',3,(#9388,#9389,#9390,#9391,#9392,#9393,
#9394,#9395,#9396,#9397,#9398),.UNSPECIFIED.,.F.,.F.,(4,1,1,1,1,1,1,1,4),
(116.238928182823,116.369122527555,117.366776822873,118.364431118192,119.36208541351,
120.359739708829,121.357394004147,122.355048299466,122.522113490002),
 .UNSPECIFIED.);
#280=B_SPLINE_CURVE_WITH_KNOTS('',3,(#9399,#9400,#9401,#9402,#9403,#9404,
#9405,#9406,#9407,#9408),.UNSPECIFIED.,.F.,.F.,(4,1,1,1,1,1,1,4),(116.238928182823,
117.054905112458,118.052559407776,119.050213703095,120.047867998413,121.045522293732,
122.04317658905,122.522113490002),.UNSPECIFIED.);
#281=B_SPLINE_CURVE_WITH_KNOTS('',3,(#9413,#9414,#9415,#9416,#9417,#9418,
#9419,#9420,#9421,#9422),.UNSPECIFIED.,.F.,.F.,(4,1,1,1,1,1,1,4),(109.955742875643,
110.383196755643,111.380851050962,112.37850534628,113.376159641599,114.373813936918,
115.371468232236,116.238928182823),.UNSPECIFIED.);
#282=B_SPLINE_CURVE_WITH_KNOTS('',3,(#9423,#9424,#9425,#9426,#9427,#9428,
#9429,#9430,#9431,#9432,#9433),.UNSPECIFIED.,.F.,.F.,(4,1,1,1,1,1,1,1,4),
(109.955742875643,110.071325045228,111.068979340547,112.066633635865,113.064287931184,
114.061942226502,115.059596521821,116.057250817139,116.238928182823),
 .UNSPECIFIED.);
#283=B_SPLINE_CURVE_WITH_KNOTS('',3,(#9438,#9439,#9440,#9441,#9442,#9443,
#9444,#9445,#9446,#9447),.UNSPECIFIED.,.F.,.F.,(4,1,1,1,1,1,1,4),(103.672557568463,
104.397270983732,105.394925279051,106.392579574369,107.390233869688,108.387888165006,
109.385542460325,109.955742875643),.UNSPECIFIED.);
#284=B_SPLINE_CURVE_WITH_KNOTS('',3,(#9448,#9449,#9450,#9451,#9452,#9453,
#9454,#9455,#9456,#9457),.UNSPECIFIED.,.F.,.F.,(4,1,1,1,1,1,1,4),(103.672557568463,
104.085399273317,105.083053568636,106.080707863954,107.078362159273,108.076016454591,
109.07367074991,109.955742875643),.UNSPECIFIED.);
#285=B_SPLINE_CURVE_WITH_KNOTS('',3,(#9462,#9463,#9464,#9465,#9466,#9467,
#9468,#9469,#9470,#9471,#9472),.UNSPECIFIED.,.F.,.F.,(4,1,1,1,1,1,1,1,4),
(97.3893722612838,97.4136909165028,98.4113452118213,99.4089995071398,100.406653802458,
101.404308097777,102.401962393095,103.399616688414,103.672557568463),
 .UNSPECIFIED.);
#286=B_SPLINE_CURVE_WITH_KNOTS('',3,(#9473,#9474,#9475,#9476,#9477,#9478,
#9479,#9480,#9481,#9482),.UNSPECIFIED.,.F.,.F.,(4,1,1,1,1,1,1,4),(97.3893722612839,
98.099473501406,99.0971277967245,100.094782092043,101.092436387362,102.09009068268,
103.087744977999,103.672557568463),.UNSPECIFIED.);
#287=B_SPLINE_CURVE_WITH_KNOTS('',3,(#9487,#9488,#9489,#9490,#9491,#9492,
#9493,#9494,#9495,#9496),.UNSPECIFIED.,.F.,.F.,(4,1,1,1,1,1,1,4),(91.1061869541042,
91.4277651445918,92.4254194399103,93.4230737352288,94.4207280305473,95.4183823258658,
96.4160366211843,97.3893722612838),.UNSPECIFIED.);
#288=B_SPLINE_CURVE_WITH_KNOTS('',3,(#9497,#9498,#9499,#9500,#9501,#9502,
#9503,#9504,#9505,#9506,#9507),.UNSPECIFIED.,.F.,.F.,(4,1,1,1,1,1,1,1,4),
(91.1061869541043,91.1158934341764,92.1135477294949,93.1112020248134,94.1088563201319,
95.1065106154505,96.104164910769,97.1018192060875,97.3893722612839),
 .UNSPECIFIED.);
#289=B_SPLINE_CURVE_WITH_KNOTS('',3,(#9512,#9513,#9514,#9515,#9516,#9517,
#9518,#9519,#9520,#9521),.UNSPECIFIED.,.F.,.F.,(4,1,1,1,1,1,1,4),(84.8230016469246,
85.4418393726807,86.4394936679992,87.4371479633177,88.4348022586362,89.4324565539547,
90.4301108492732,91.1061869541042),.UNSPECIFIED.);
#290=B_SPLINE_CURVE_WITH_KNOTS('',3,(#9522,#9523,#9524,#9525,#9526,#9527,
#9528,#9529,#9530,#9531),.UNSPECIFIED.,.F.,.F.,(4,1,1,1,1,1,1,4),(84.8230016469247,
85.1299676622653,86.1276219575839,87.1252762529024,88.1229305482209,89.1205848435394,
90.1182391388579,91.1061869541043),.UNSPECIFIED.);
#291=B_SPLINE_CURVE_WITH_KNOTS('',3,(#9536,#9537,#9538,#9539,#9540,#9541,
#9542,#9543,#9544,#9545),.UNSPECIFIED.,.F.,.F.,(4,1,1,1,1,1,1,4),(78.539816339745,
79.4559136007696,80.4535678960881,81.4512221914066,82.4488764867252,83.4465307820437,
84.4441850773622,84.8230016469246),.UNSPECIFIED.);
#292=B_SPLINE_CURVE_WITH_KNOTS('',3,(#9546,#9547,#9548,#9549,#9550,#9551,
#9552,#9553,#9554,#9555),.UNSPECIFIED.,.F.,.F.,(4,1,1,1,1,1,1,4),(78.5398163397451,
79.1440418903543,80.1416961856728,81.1393504809913,82.1370047763098,83.1346590716283,
84.1323133669468,84.8230016469247),.UNSPECIFIED.);
#293=B_SPLINE_CURVE_WITH_KNOTS('',3,(#9560,#9561,#9562,#9563,#9564,#9565,
#9566,#9567,#9568,#9569,#9570),.UNSPECIFIED.,.F.,.F.,(4,1,1,1,1,1,1,1,4),
(72.2566310325654,72.4723335335401,73.4699878288586,74.4676421241771,75.4652964194956,
76.4629507148141,77.4606050101326,78.4582593054511,78.539816339745),
 .UNSPECIFIED.);
#294=B_SPLINE_CURVE_WITH_KNOTS('',3,(#9571,#9572,#9573,#9574,#9575,#9576,
#9577,#9578,#9579,#9580),.UNSPECIFIED.,.F.,.F.,(4,1,1,1,1,1,1,4),(72.2566310325655,
73.1581161184432,74.1557704137617,75.1534247090802,76.1510790043987,77.1487332997173,
78.1463875950358,78.5398163397451),.UNSPECIFIED.);
#295=B_SPLINE_CURVE_WITH_KNOTS('',3,(#9585,#9586,#9587,#9588,#9589,#9590,
#9591,#9592,#9593,#9594),.UNSPECIFIED.,.F.,.F.,(4,1,1,1,1,1,1,4),(65.9734457253858,
66.486407761629,67.4840620569475,68.481716352266,69.4793706475845,70.477024942903,
71.4746792382215,72.2566310325654),.UNSPECIFIED.);
#296=B_SPLINE_CURVE_WITH_KNOTS('',3,(#9595,#9596,#9597,#9598,#9599,#9600,
#9601,#9602,#9603,#9604,#9605),.UNSPECIFIED.,.F.,.F.,(4,1,1,1,1,1,1,1,4),
(65.9734457253859,66.1745360512136,67.1721903465321,68.1698446418506,69.1674989371692,
70.1651532324877,71.1628075278062,72.1604618231247,72.2566310325655),
 .UNSPECIFIED.);
#297=B_SPLINE_CURVE_WITH_KNOTS('',3,(#9610,#9611,#9612,#9613,#9614,#9615,
#9616,#9617,#9618,#9619),.UNSPECIFIED.,.F.,.F.,(4,1,1,1,1,1,1,4),(59.6902604182063,
60.5004819897179,61.4981362850364,62.4957905803549,63.4934448756734,64.491099170992,
65.4887534663105,65.9734457253858),.UNSPECIFIED.);
#298=B_SPLINE_CURVE_WITH_KNOTS('',3,(#9620,#9621,#9622,#9623,#9624,#9625,
#9626,#9627,#9628,#9629),.UNSPECIFIED.,.F.,.F.,(4,1,1,1,1,1,1,4),(59.6902604182063,
60.1886102793026,61.1862645746211,62.1839188699396,63.1815731652581,64.1792274605766,
65.1768817558951,65.9734457253859),.UNSPECIFIED.);
#299=B_SPLINE_CURVE_WITH_KNOTS('',3,(#9634,#9635,#9636,#9637,#9638,#9639,
#9640,#9641,#9642,#9643,#9644),.UNSPECIFIED.,.F.,.F.,(4,1,1,1,1,1,1,1,4),
(53.4070751110267,53.5169019224883,54.5145562178069,55.5122105131254,56.5098648084439,
57.5075191037624,58.5051733990809,59.5028276943994,59.6902604182063),
 .UNSPECIFIED.);
#300=B_SPLINE_CURVE_WITH_KNOTS('',3,(#9645,#9646,#9647,#9648,#9649,#9650,
#9651,#9652,#9653,#9654),.UNSPECIFIED.,.F.,.F.,(4,1,1,1,1,1,1,4),(53.4070751110267,
54.2026845073915,55.20033880271,56.1979930980285,57.195647393347,58.1933016886655,
59.190955983984,59.6902604182063),.UNSPECIFIED.);
#301=B_SPLINE_CURVE_WITH_KNOTS('',3,(#9659,#9660,#9661,#9662,#9663,#9664,
#9665,#9666,#9667,#9668),.UNSPECIFIED.,.F.,.F.,(4,1,1,1,1,1,1,4),(47.1238898038471,
47.5309761505773,48.5286304458958,49.5262847412143,50.5239390365328,51.5215933318513,
52.5192476271698,53.4070751110267),.UNSPECIFIED.);
#302=B_SPLINE_CURVE_WITH_KNOTS('',3,(#9669,#9670,#9671,#9672,#9673,#9674,
#9675,#9676,#9677,#9678,#9679),.UNSPECIFIED.,.F.,.F.,(4,1,1,1,1,1,1,1,4),
(47.1238898038471,47.2191044401619,48.2167587354804,49.2144130307989,50.2120673261174,
51.209721621436,52.2073759167545,53.205030212073,53.4070751110267),
 .UNSPECIFIED.);
#303=B_SPLINE_CURVE_WITH_KNOTS('',3,(#9684,#9685,#9686,#9687,#9688,#9689,
#9690,#9691,#9692,#9693),.UNSPECIFIED.,.F.,.F.,(4,1,1,1,1,1,1,4),(40.8407044966675,
41.5450503786662,42.5427046739847,43.5403589693032,44.5380132646217,45.5356675599403,
46.5333218552588,47.1238898038471),.UNSPECIFIED.);
#304=B_SPLINE_CURVE_WITH_KNOTS('',3,(#9694,#9695,#9696,#9697,#9698,#9699,
#9700,#9701,#9702,#9703),.UNSPECIFIED.,.F.,.F.,(4,1,1,1,1,1,1,4),(40.8407044966675,
41.2331786682508,42.2308329635693,43.2284872588879,44.2261415542064,45.2237958495249,
46.2214501448434,47.1238898038471),.UNSPECIFIED.);
#305=B_SPLINE_CURVE_WITH_KNOTS('',3,(#9708,#9709,#9710,#9711,#9712,#9713,
#9714,#9715,#9716,#9717,#9718),.UNSPECIFIED.,.F.,.F.,(4,1,1,1,1,1,1,1,4),
(34.5575191894879,34.5614703114366,35.5591246067551,36.5567789020737,37.5544331973922,
38.5520874927107,39.5497417880292,40.5473960833477,40.8407044966675),
 .UNSPECIFIED.);
#306=B_SPLINE_CURVE_WITH_KNOTS('',3,(#9719,#9720,#9721,#9722,#9723,#9724,
#9725,#9726,#9727,#9728),.UNSPECIFIED.,.F.,.F.,(4,1,1,1,1,1,1,4),(34.5575191894879,
35.2472528963398,36.2449071916583,37.2425614869768,38.2402157822953,39.2378700776138,
40.2355243729323,40.8407044966675),.UNSPECIFIED.);
#307=B_SPLINE_CURVE_WITH_KNOTS('',3,(#9733,#9734,#9735,#9736,#9737,#9738,
#9739,#9740,#9741,#9742),.UNSPECIFIED.,.F.,.F.,(4,1,1,1,1,1,1,4),(28.2743338823083,
28.5755445395256,29.5731988348441,30.5708531301626,31.5685074254811,32.5661617207996,
33.5638160161181,34.5575191894879),.UNSPECIFIED.);
#308=B_SPLINE_CURVE_WITH_KNOTS('',3,(#9743,#9744,#9745,#9746,#9747,#9748,
#9749,#9750,#9751,#9752),.UNSPECIFIED.,.F.,.F.,(4,1,1,1,1,1,1,4),(28.2743338823084,
29.2613271244287,30.2589814197472,31.2566357150657,32.2542900103842,33.2519443057027,
34.2495986010213,34.5575191894879),.UNSPECIFIED.);
#309=B_SPLINE_CURVE_WITH_KNOTS('',3,(#9757,#9758,#9759,#9760,#9761,#9762,
#9763,#9764,#9765,#9766),.UNSPECIFIED.,.F.,.F.,(4,1,1,1,1,1,1,4),(21.9911485751287,
22.5896187676145,23.587273062933,24.5849273582515,25.58258165357,26.5802359488886,
27.5778902442071,28.2743338823083),.UNSPECIFIED.);
#310=B_SPLINE_CURVE_WITH_KNOTS('',3,(#9767,#9768,#9769,#9770,#9771,#9772,
#9773,#9774,#9775,#9776,#9777),.UNSPECIFIED.,.F.,.F.,(4,1,1,1,1,1,1,1,4),
(21.9911485751288,22.2777470571991,23.2754013525176,24.2730556478361,25.2707099431546,
26.2683642384732,27.2660185337917,28.2636728291102,28.2743338823084),
 .UNSPECIFIED.);
#311=B_SPLINE_CURVE_WITH_KNOTS('',3,(#9782,#9783,#9784,#9785,#9786,#9787,
#9788,#9789,#9790,#9791),.UNSPECIFIED.,.F.,.F.,(4,1,1,1,1,1,1,4),(15.7079632679491,
16.6036929957034,17.601347291022,18.5990015863405,19.596655881659,20.5943101769775,
21.591964472296,21.9911485751287),.UNSPECIFIED.);
#312=B_SPLINE_CURVE_WITH_KNOTS('',3,(#9792,#9793,#9794,#9795,#9796,#9797,
#9798,#9799,#9800,#9801),.UNSPECIFIED.,.F.,.F.,(4,1,1,1,1,1,1,4),(15.7079632679492,
16.291821285288,17.2894755806066,18.2871298759251,19.2847841712436,20.2824384665621,
21.2800927618806,21.9911485751288),.UNSPECIFIED.);
#313=B_SPLINE_CURVE_WITH_KNOTS('',3,(#10687,#10688,#10689,#10690,#10691,
#10692,#10693,#10694,#10695,#10696,#10697,#10698,#10699,#10700,#10701,#10702,
#10703,#10704,#10705,#10706,#10707,#10708,#10709,#10710,#10711,#10712,#10713,
#10714,#10715,#10716,#10717,#10718,#10719,#10720,#10721,#10722,#10723,#10724,
#10725,#10726,#10727,#10728,#10729,#10730,#10731,#10732,#10733,#10734,#10735,
#10736,#10737,#10738,#10739,#10740,#10741),.UNSPECIFIED.,.F.,.F.,(4,3,3,
3,3,3,3,3,3,3,3,3,3,3,3,3,3,3,4),(0.,0.0136872263540572,0.0521656178595838,
0.0709950800646878,0.0819953190919729,0.119249023879074,0.145058748625905,
0.157048448925498,0.192145397802465,0.199552864933563,0.212199804588965,
0.222691438606214,0.258617973706117,0.274171447851467,0.289117136857619,
0.312609296851327,0.324805558922168,0.357088803957493,0.366397579005826),
 .UNSPECIFIED.);
#314=B_SPLINE_CURVE_WITH_KNOTS('',3,(#10742,#10743,#10744,#10745),
 .UNSPECIFIED.,.F.,.F.,(4,4),(214.742491482136,215.423496246157),
 .UNSPECIFIED.);
#315=B_SPLINE_CURVE_WITH_KNOTS('',3,(#10747,#10748,#10749,#10750,#10751,
#10752,#10753,#10754,#10755,#10756,#10757,#10758,#10759,#10760,#10761,#10762,
#10763,#10764,#10765,#10766,#10767,#10768,#10769,#10770,#10771,#10772,#10773,
#10774,#10775,#10776,#10777,#10778,#10779,#10780,#10781,#10782,#10783,#10784,
#10785,#10786,#10787,#10788,#10789,#10790,#10791,#10792,#10793,#10794,#10795,
#10796,#10797,#10798),.UNSPECIFIED.,.F.,.F.,(4,3,3,3,3,3,3,3,3,3,3,3,3,
3,3,3,3,4),(-0.366397579005832,-0.355349081053819,-0.328627709487849,-0.316006317805062,
-0.292294699921123,-0.280145524705702,-0.245167839456388,-0.218343989495843,
-0.207795842608001,-0.187146499846321,-0.163753187365531,-0.149466290679141,
-0.138688713158187,-0.10401653486864,-0.0826655685122029,-0.0667932349897769,
-0.0282993460444213,0.),.UNSPECIFIED.);
#316=B_SPLINE_CURVE_WITH_KNOTS('',3,(#10799,#10800,#10801,#10802,#10803,
#10804,#10805,#10806,#10807),.UNSPECIFIED.,.F.,.F.,(4,1,1,1,1,1,4),(10.3757270560181,
11.3035498086955,12.301204104014,13.2988583993325,14.296512694651,15.2941669899695,
15.7079632679492),.UNSPECIFIED.);
#317=B_SPLINE_CURVE_WITH_KNOTS('',3,(#10811,#10812,#10813,#10814,#10815,
#10816,#10817,#10818),.UNSPECIFIED.,.F.,.F.,(4,1,1,1,1,4),(11.6154215191109,
12.6130758144294,13.6107301097479,14.6083844050664,15.6060387003849,15.7079632679491),
 .UNSPECIFIED.);
#318=B_SPLINE_CURVE_WITH_KNOTS('',3,(#11703,#11704,#11705,#11706,#11707,
#11708,#11709,#11710,#11711,#11712,#11713,#11714,#11715,#11716,#11717,#11718,
#11719,#11720,#11721,#11722,#11723,#11724,#11725,#11726,#11727,#11728,#11729,
#11730,#11731,#11732,#11733,#11734,#11735,#11736,#11737,#11738,#11739,#11740,
#11741,#11742,#11743,#11744,#11745,#11746,#11747,#11748,#11749,#11750,#11751,
#11752,#11753,#11754,#11755,#11756,#11757),.UNSPECIFIED.,.F.,.F.,(4,3,3,
3,3,3,3,3,3,3,3,3,3,3,3,3,3,3,4),(0.,0.0110072508574968,0.0432941145547806,
0.0597161191659724,0.0689602245586863,0.103423950716991,0.120946125282339,
0.133710039597458,0.169449851669546,0.178576016460901,0.192751466168984,
0.204131677343237,0.24002978635429,0.257655102053338,0.272192488363931,
0.297601230030268,0.313197869948207,0.326770085092486,0.364629307890676),
 .UNSPECIFIED.);
#319=B_SPLINE_CURVE_WITH_KNOTS('',3,(#11758,#11759,#11760,#11761,#11762,
#11763,#11764,#11765,#11766,#11767,#11768,#11769,#11770,#11771,#11772,#11773,
#11774,#11775,#11776,#11777,#11778,#11779,#11780,#11781,#11782,#11783,#11784,
#11785,#11786,#11787,#11788,#11789,#11790,#11791,#11792,#11793,#11794,#11795,
#11796,#11797,#11798,#11799,#11800,#11801,#11802,#11803,#11804,#11805,#11806,
#11807,#11808,#11809,#11810,#11811,#11812),.UNSPECIFIED.,.F.,.F.,(4,3,3,
3,3,3,3,3,3,3,3,3,3,3,3,3,3,3,4),(-0.364629307890679,-0.351009649103909,
-0.324517397172783,-0.304129683158625,-0.282910327436154,-0.263912543184838,
-0.252746321376793,-0.216330856983722,-0.197981750539286,-0.186600442527354,
-0.166229720628164,-0.130494010253894,-0.119373904450406,-0.0895304283378048,
-0.0729804099452609,-0.062655130809591,-0.0518856098027967,-0.0196333504494857,
0.),.UNSPECIFIED.);
#360=SHAPE_REPRESENTATION_RELATIONSHIP('SRR','None',#13044,#372);
#372=ADVANCED_BREP_SHAPE_REPRESENTATION('',(#396),#12960);
#384=STYLED_ITEM('',(#13113),#396);
#396=MANIFOLD_SOLID_BREP('Body1',#4818);
#437=FACE_BOUND('',#1092,.T.);
#438=FACE_BOUND('',#1095,.T.);
#552=PLANE('',#5254);
#553=PLANE('',#5255);
#554=PLANE('',#5256);
#555=PLANE('',#5257);
#556=PLANE('',#5258);
#557=PLANE('',#5259);
#558=PLANE('',#5260);
#559=PLANE('',#5261);
#560=PLANE('',#5265);
#561=PLANE('',#5266);
#717=FACE_OUTER_BOUND('',#1011,.T.);
#718=FACE_OUTER_BOUND('',#1012,.T.);
#719=FACE_OUTER_BOUND('',#1013,.T.);
#720=FACE_OUTER_BOUND('',#1014,.T.);
#721=FACE_OUTER_BOUND('',#1015,.T.);
#722=FACE_OUTER_BOUND('',#1016,.T.);
#723=FACE_OUTER_BOUND('',#1017,.T.);
#724=FACE_OUTER_BOUND('',#1018,.T.);
#725=FACE_OUTER_BOUND('',#1019,.T.);
#726=FACE_OUTER_BOUND('',#1020,.T.);
#727=FACE_OUTER_BOUND('',#1021,.T.);
#728=FACE_OUTER_BOUND('',#1022,.T.);
#729=FACE_OUTER_BOUND('',#1023,.T.);
#730=FACE_OUTER_BOUND('',#1024,.T.);
#731=FACE_OUTER_BOUND('',#1025,.T.);
#732=FACE_OUTER_BOUND('',#1026,.T.);
#733=FACE_OUTER_BOUND('',#1027,.T.);
#734=FACE_OUTER_BOUND('',#1028,.T.);
#735=FACE_OUTER_BOUND('',#1029,.T.);
#736=FACE_OUTER_BOUND('',#1030,.T.);
#737=FACE_OUTER_BOUND('',#1031,.T.);
#738=FACE_OUTER_BOUND('',#1032,.T.);
#739=FACE_OUTER_BOUND('',#1033,.T.);
#740=FACE_OUTER_BOUND('',#1034,.T.);
#741=FACE_OUTER_BOUND('',#1035,.T.);
#742=FACE_OUTER_BOUND('',#1036,.T.);
#743=FACE_OUTER_BOUND('',#1037,.T.);
#744=FACE_OUTER_BOUND('',#1038,.T.);
#745=FACE_OUTER_BOUND('',#1039,.T.);
#746=FACE_OUTER_BOUND('',#1040,.T.);
#747=FACE_OUTER_BOUND('',#1041,.T.);
#748=FACE_OUTER_BOUND('',#1042,.T.);
#749=FACE_OUTER_BOUND('',#1043,.T.);
#750=FACE_OUTER_BOUND('',#1044,.T.);
#751=FACE_OUTER_BOUND('',#1045,.T.);
#752=FACE_OUTER_BOUND('',#1046,.T.);
#753=FACE_OUTER_BOUND('',#1047,.T.);
#754=FACE_OUTER_BOUND('',#1048,.T.);
#755=FACE_OUTER_BOUND('',#1049,.T.);
#756=FACE_OUTER_BOUND('',#1050,.T.);
#757=FACE_OUTER_BOUND('',#1051,.T.);
#758=FACE_OUTER_BOUND('',#1052,.T.);
#759=FACE_OUTER_BOUND('',#1053,.T.);
#760=FACE_OUTER_BOUND('',#1054,.T.);
#761=FACE_OUTER_BOUND('',#1055,.T.);
#762=FACE_OUTER_BOUND('',#1056,.T.);
#763=FACE_OUTER_BOUND('',#1057,.T.);
#764=FACE_OUTER_BOUND('',#1058,.T.);
#765=FACE_OUTER_BOUND('',#1059,.T.);
#766=FACE_OUTER_BOUND('',#1060,.T.);
#767=FACE_OUTER_BOUND('',#1061,.T.);
#768=FACE_OUTER_BOUND('',#1062,.T.);
#769=FACE_OUTER_BOUND('',#1063,.T.);
#770=FACE_OUTER_BOUND('',#1064,.T.);
#771=FACE_OUTER_BOUND('',#1065,.T.);
#772=FACE_OUTER_BOUND('',#1066,.T.);
#773=FACE_OUTER_BOUND('',#1067,.T.);
#774=FACE_OUTER_BOUND('',#1068,.T.);
#775=FACE_OUTER_BOUND('',#1069,.T.);
#776=FACE_OUTER_BOUND('',#1070,.T.);
#777=FACE_OUTER_BOUND('',#1071,.T.);
#778=FACE_OUTER_BOUND('',#1072,.T.);
#779=FACE_OUTER_BOUND('',#1073,.T.);
#780=FACE_OUTER_BOUND('',#1074,.T.);
#781=FACE_OUTER_BOUND('',#1075,.T.);
#782=FACE_OUTER_BOUND('',#1076,.T.);
#783=FACE_OUTER_BOUND('',#1077,.T.);
#784=FACE_OUTER_BOUND('',#1078,.T.);
#785=FACE_OUTER_BOUND('',#1079,.T.);
#786=FACE_OUTER_BOUND('',#1080,.T.);
#787=FACE_OUTER_BOUND('',#1081,.T.);
#788=FACE_OUTER_BOUND('',#1082,.T.);
#789=FACE_OUTER_BOUND('',#1083,.T.);
#790=FACE_OUTER_BOUND('',#1084,.T.);
#791=FACE_OUTER_BOUND('',#1085,.T.);
#792=FACE_OUTER_BOUND('',#1086,.T.);
#793=FACE_OUTER_BOUND('',#1087,.T.);
#794=FACE_OUTER_BOUND('',#1088,.T.);
#795=FACE_OUTER_BOUND('',#1089,.T.);
#796=FACE_OUTER_BOUND('',#1090,.T.);
#797=FACE_OUTER_BOUND('',#1091,.T.);
#798=FACE_OUTER_BOUND('',#1093,.T.);
#799=FACE_OUTER_BOUND('',#1094,.T.);
#800=FACE_OUTER_BOUND('',#1096,.T.);
#1011=EDGE_LOOP('',(#3814,#3815,#3816,#3817));
#1012=EDGE_LOOP('',(#3818,#3819,#3820,#3821));
#1013=EDGE_LOOP('',(#3822,#3823,#3824,#3825));
#1014=EDGE_LOOP('',(#3826,#3827,#3828,#3829));
#1015=EDGE_LOOP('',(#3830,#3831,#3832,#3833));
#1016=EDGE_LOOP('',(#3834,#3835,#3836,#3837));
#1017=EDGE_LOOP('',(#3838,#3839,#3840,#3841));
#1018=EDGE_LOOP('',(#3842,#3843,#3844,#3845));
#1019=EDGE_LOOP('',(#3846,#3847,#3848,#3849));
#1020=EDGE_LOOP('',(#3850,#3851,#3852,#3853));
#1021=EDGE_LOOP('',(#3854,#3855,#3856,#3857));
#1022=EDGE_LOOP('',(#3858,#3859,#3860,#3861));
#1023=EDGE_LOOP('',(#3862,#3863,#3864,#3865));
#1024=EDGE_LOOP('',(#3866,#3867,#3868,#3869));
#1025=EDGE_LOOP('',(#3870,#3871,#3872,#3873));
#1026=EDGE_LOOP('',(#3874,#3875,#3876,#3877));
#1027=EDGE_LOOP('',(#3878,#3879,#3880,#3881));
#1028=EDGE_LOOP('',(#3882,#3883,#3884,#3885));
#1029=EDGE_LOOP('',(#3886,#3887,#3888,#3889));
#1030=EDGE_LOOP('',(#3890,#3891,#3892,#3893));
#1031=EDGE_LOOP('',(#3894,#3895,#3896,#3897));
#1032=EDGE_LOOP('',(#3898,#3899,#3900,#3901));
#1033=EDGE_LOOP('',(#3902,#3903,#3904,#3905));
#1034=EDGE_LOOP('',(#3906,#3907,#3908,#3909));
#1035=EDGE_LOOP('',(#3910,#3911,#3912,#3913));
#1036=EDGE_LOOP('',(#3914,#3915,#3916,#3917));
#1037=EDGE_LOOP('',(#3918,#3919,#3920,#3921));
#1038=EDGE_LOOP('',(#3922,#3923,#3924,#3925));
#1039=EDGE_LOOP('',(#3926,#3927,#3928,#3929));
#1040=EDGE_LOOP('',(#3930,#3931,#3932,#3933));
#1041=EDGE_LOOP('',(#3934,#3935,#3936,#3937));
#1042=EDGE_LOOP('',(#3938,#3939,#3940,#3941));
#1043=EDGE_LOOP('',(#3942,#3943,#3944,#3945));
#1044=EDGE_LOOP('',(#3946,#3947,#3948,#3949));
#1045=EDGE_LOOP('',(#3950,#3951,#3952,#3953,#3954));
#1046=EDGE_LOOP('',(#3955,#3956,#3957,#3958));
#1047=EDGE_LOOP('',(#3959,#3960,#3961,#3962));
#1048=EDGE_LOOP('',(#3963,#3964,#3965,#3966));
#1049=EDGE_LOOP('',(#3967,#3968,#3969,#3970));
#1050=EDGE_LOOP('',(#3971,#3972,#3973,#3974));
#1051=EDGE_LOOP('',(#3975,#3976,#3977,#3978));
#1052=EDGE_LOOP('',(#3979,#3980,#3981,#3982));
#1053=EDGE_LOOP('',(#3983,#3984,#3985,#3986));
#1054=EDGE_LOOP('',(#3987,#3988,#3989,#3990));
#1055=EDGE_LOOP('',(#3991,#3992,#3993,#3994));
#1056=EDGE_LOOP('',(#3995,#3996,#3997,#3998));
#1057=EDGE_LOOP('',(#3999,#4000,#4001,#4002));
#1058=EDGE_LOOP('',(#4003,#4004,#4005,#4006));
#1059=EDGE_LOOP('',(#4007,#4008,#4009,#4010));
#1060=EDGE_LOOP('',(#4011,#4012,#4013,#4014));
#1061=EDGE_LOOP('',(#4015,#4016,#4017,#4018));
#1062=EDGE_LOOP('',(#4019,#4020,#4021,#4022));
#1063=EDGE_LOOP('',(#4023,#4024,#4025,#4026));
#1064=EDGE_LOOP('',(#4027,#4028,#4029,#4030));
#1065=EDGE_LOOP('',(#4031,#4032,#4033,#4034));
#1066=EDGE_LOOP('',(#4035,#4036,#4037,#4038));
#1067=EDGE_LOOP('',(#4039,#4040,#4041,#4042));
#1068=EDGE_LOOP('',(#4043,#4044,#4045,#4046));
#1069=EDGE_LOOP('',(#4047,#4048,#4049,#4050));
#1070=EDGE_LOOP('',(#4051,#4052,#4053,#4054));
#1071=EDGE_LOOP('',(#4055,#4056,#4057,#4058));
#1072=EDGE_LOOP('',(#4059,#4060,#4061,#4062));
#1073=EDGE_LOOP('',(#4063,#4064,#4065,#4066));
#1074=EDGE_LOOP('',(#4067,#4068,#4069,#4070));
#1075=EDGE_LOOP('',(#4071,#4072,#4073,#4074));
#1076=EDGE_LOOP('',(#4075,#4076,#4077,#4078));
#1077=EDGE_LOOP('',(#4079,#4080,#4081,#4082));
#1078=EDGE_LOOP('',(#4083,#4084,#4085,#4086));
#1079=EDGE_LOOP('',(#4087,#4088,#4089,#4090));
#1080=EDGE_LOOP('',(#4091,#4092,#4093,#4094,#4095,#4096,#4097,#4098,#4099,
#4100,#4101,#4102,#4103,#4104,#4105,#4106,#4107,#4108,#4109,#4110,#4111,
#4112,#4113,#4114,#4115,#4116,#4117,#4118,#4119,#4120,#4121,#4122,#4123,
#4124,#4125,#4126,#4127,#4128,#4129,#4130,#4131,#4132,#4133,#4134,#4135,
#4136,#4137,#4138,#4139,#4140,#4141,#4142,#4143,#4144,#4145,#4146,#4147,
#4148,#4149,#4150,#4151,#4152,#4153,#4154,#4155,#4156,#4157,#4158,#4159,
#4160,#4161,#4162,#4163));
#1081=EDGE_LOOP('',(#4164,#4165,#4166,#4167));
#1082=EDGE_LOOP('',(#4168,#4169,#4170,#4171,#4172,#4173,#4174,#4175,#4176,
#4177,#4178,#4179,#4180,#4181,#4182,#4183,#4184,#4185,#4186,#4187,#4188,
#4189,#4190,#4191,#4192,#4193,#4194,#4195,#4196,#4197,#4198,#4199,#4200,
#4201,#4202,#4203,#4204,#4205,#4206,#4207,#4208,#4209,#4210,#4211,#4212,
#4213,#4214,#4215,#4216,#4217,#4218,#4219,#4220,#4221,#4222,#4223,#4224,
#4225,#4226,#4227,#4228,#4229,#4230,#4231,#4232,#4233,#4234,#4235,#4236,
#4237,#4238,#4239));
#1083=EDGE_LOOP('',(#4240,#4241,#4242));
#1084=EDGE_LOOP('',(#4243,#4244,#4245,#4246));
#1085=EDGE_LOOP('',(#4247,#4248,#4249,#4250));
#1086=EDGE_LOOP('',(#4251,#4252,#4253,#4254));
#1087=EDGE_LOOP('',(#4255,#4256,#4257,#4258));
#1088=EDGE_LOOP('',(#4259,#4260,#4261,#4262));
#1089=EDGE_LOOP('',(#4263,#4264,#4265,#4266));
#1090=EDGE_LOOP('',(#4267,#4268,#4269,#4270,#4271,#4272));
#1091=EDGE_LOOP('',(#4273));
#1092=EDGE_LOOP('',(#4274,#4275,#4276,#4277));
#1093=EDGE_LOOP('',(#4278,#4279,#4280,#4281));
#1094=EDGE_LOOP('',(#4282));
#1095=EDGE_LOOP('',(#4283,#4284,#4285,#4286,#4287,#4288));
#1096=EDGE_LOOP('',(#4289,#4290,#4291,#4292,#4293));
#1409=LINE('',#7261,#1811);
#1410=LINE('',#7285,#1812);
#1411=LINE('',#7333,#1813);
#1412=LINE('',#7381,#1814);
#1413=LINE('',#7432,#1815);
#1414=LINE('',#7480,#1816);
#1415=LINE('',#7528,#1817);
#1416=LINE('',#7576,#1818);
#1417=LINE('',#7630,#1819);
#1418=LINE('',#7678,#1820);
#1419=LINE('',#7726,#1821);
#1420=LINE('',#7780,#1822);
#1421=LINE('',#7828,#1823);
#1422=LINE('',#7876,#1824);
#1423=LINE('',#7924,#1825);
#1424=LINE('',#7978,#1826);
#1425=LINE('',#8026,#1827);
#1426=LINE('',#8074,#1828);
#1427=LINE('',#8128,#1829);
#1428=LINE('',#8176,#1830);
#1429=LINE('',#8224,#1831);
#1430=LINE('',#8278,#1832);
#1431=LINE('',#8326,#1833);
#1432=LINE('',#8374,#1834);
#1433=LINE('',#8422,#1835);
#1434=LINE('',#8476,#1836);
#1435=LINE('',#8524,#1837);
#1436=LINE('',#8572,#1838);
#1437=LINE('',#8626,#1839);
#1438=LINE('',#8674,#1840);
#1439=LINE('',#8722,#1841);
#1440=LINE('',#8776,#1842);
#1441=LINE('',#8824,#1843);
#1442=LINE('',#8872,#1844);
#1443=LINE('',#8920,#1845);
#1444=LINE('',#8973,#1846);
#1445=LINE('',#8994,#1847);
#1446=LINE('',#9019,#1848);
#1447=LINE('',#9043,#1849);
#1448=LINE('',#9067,#1850);
#1449=LINE('',#9092,#1851);
#1450=LINE('',#9117,#1852);
#1451=LINE('',#9141,#1853);
#1452=LINE('',#9166,#1854);
#1453=LINE('',#9191,#1855);
#1454=LINE('',#9215,#1856);
#1455=LINE('',#9240,#1857);
#1456=LINE('',#9265,#1858);
#1457=LINE('',#9289,#1859);
#1458=LINE('',#9313,#1860);
#1459=LINE('',#9338,#1861);
#1460=LINE('',#9363,#1862);
#1461=LINE('',#9387,#1863);
#1462=LINE('',#9412,#1864);
#1463=LINE('',#9437,#1865);
#1464=LINE('',#9461,#1866);
#1465=LINE('',#9486,#1867);
#1466=LINE('',#9511,#1868);
#1467=LINE('',#9535,#1869);
#1468=LINE('',#9559,#1870);
#1469=LINE('',#9584,#1871);
#1470=LINE('',#9609,#1872);
#1471=LINE('',#9633,#1873);
#1472=LINE('',#9658,#1874);
#1473=LINE('',#9683,#1875);
#1474=LINE('',#9707,#1876);
#1475=LINE('',#9732,#1877);
#1476=LINE('',#9756,#1878);
#1477=LINE('',#9781,#1879);
#1478=LINE('',#11818,#1880);
#1479=LINE('',#11820,#1881);
#1480=LINE('',#11822,#1882);
#1481=LINE('',#11823,#1883);
#1482=LINE('',#11826,#1884);
#1483=LINE('',#11828,#1885);
#1484=LINE('',#11829,#1886);
#1485=LINE('',#11832,#1887);
#1486=LINE('',#11834,#1888);
#1487=LINE('',#11835,#1889);
#1488=LINE('',#11838,#1890);
#1489=LINE('',#11840,#1891);
#1490=LINE('',#11841,#1892);
#1491=LINE('',#11844,#1893);
#1492=LINE('',#11846,#1894);
#1493=LINE('',#11847,#1895);
#1494=LINE('',#11849,#1896);
#1495=LINE('',#11850,#1897);
#1496=LINE('',#11857,#1898);
#1811=VECTOR('',#6074,0.2);
#1812=VECTOR('',#6079,0.2);
#1813=VECTOR('',#6082,0.2);
#1814=VECTOR('',#6085,0.2);
#1815=VECTOR('',#6088,0.2);
#1816=VECTOR('',#6091,0.2);
#1817=VECTOR('',#6094,0.2);
#1818=VECTOR('',#6097,0.2);
#1819=VECTOR('',#6100,0.2);
#1820=VECTOR('',#6103,0.2);
#1821=VECTOR('',#6106,0.2);
#1822=VECTOR('',#6109,0.2);
#1823=VECTOR('',#6112,0.2);
#1824=VECTOR('',#6115,0.2);
#1825=VECTOR('',#6118,0.2);
#1826=VECTOR('',#6121,0.2);
#1827=VECTOR('',#6124,0.2);
#1828=VECTOR('',#6127,0.2);
#1829=VECTOR('',#6130,0.2);
#1830=VECTOR('',#6133,0.2);
#1831=VECTOR('',#6136,0.2);
#1832=VECTOR('',#6139,0.2);
#1833=VECTOR('',#6142,0.2);
#1834=VECTOR('',#6145,0.2);
#1835=VECTOR('',#6148,0.2);
#1836=VECTOR('',#6151,0.2);
#1837=VECTOR('',#6154,0.2);
#1838=VECTOR('',#6157,0.2);
#1839=VECTOR('',#6160,0.2);
#1840=VECTOR('',#6163,0.2);
#1841=VECTOR('',#6166,0.2);
#1842=VECTOR('',#6169,0.2);
#1843=VECTOR('',#6172,0.2);
#1844=VECTOR('',#6175,0.2);
#1845=VECTOR('',#6178,0.2);
#1846=VECTOR('',#6183,0.15555);
#1847=VECTOR('',#6188,0.15555);
#1848=VECTOR('',#6191,0.15555);
#1849=VECTOR('',#6194,0.15555);
#1850=VECTOR('',#6197,0.15555);
#1851=VECTOR('',#6200,0.15555);
#1852=VECTOR('',#6203,0.15555);
#1853=VECTOR('',#6206,0.15555);
#1854=VECTOR('',#6209,0.15555);
#1855=VECTOR('',#6212,0.15555);
#1856=VECTOR('',#6215,0.15555);
#1857=VECTOR('',#6218,0.15555);
#1858=VECTOR('',#6221,0.15555);
#1859=VECTOR('',#6224,0.15555);
#1860=VECTOR('',#6227,0.15555);
#1861=VECTOR('',#6230,0.15555);
#1862=VECTOR('',#6233,0.15555);
#1863=VECTOR('',#6236,0.15555);
#1864=VECTOR('',#6239,0.15555);
#1865=VECTOR('',#6242,0.15555);
#1866=VECTOR('',#6245,0.15555);
#1867=VECTOR('',#6248,0.15555);
#1868=VECTOR('',#6251,0.15555);
#1869=VECTOR('',#6254,0.15555);
#1870=VECTOR('',#6257,0.15555);
#1871=VECTOR('',#6260,0.15555);
#1872=VECTOR('',#6263,0.15555);
#1873=VECTOR('',#6266,0.15555);
#1874=VECTOR('',#6269,0.15555);
#1875=VECTOR('',#6272,0.15555);
#1876=VECTOR('',#6275,0.15555);
#1877=VECTOR('',#6278,0.15555);
#1878=VECTOR('',#6281,0.15555);
#1879=VECTOR('',#6284,0.15555);
#1880=VECTOR('',#6295,1.);
#1881=VECTOR('',#6296,1.);
#1882=VECTOR('',#6297,1.);
#1883=VECTOR('',#6298,1.);
#1884=VECTOR('',#6301,1.);
#1885=VECTOR('',#6302,1.);
#1886=VECTOR('',#6303,1.);
#1887=VECTOR('',#6306,1.);
#1888=VECTOR('',#6307,1.);
#1889=VECTOR('',#6308,1.);
#1890=VECTOR('',#6311,1.);
#1891=VECTOR('',#6312,1.);
#1892=VECTOR('',#6313,1.);
#1893=VECTOR('',#6316,1.);
#1894=VECTOR('',#6317,1.);
#1895=VECTOR('',#6318,1.);
#1896=VECTOR('',#6321,1.);
#1897=VECTOR('',#6322,1.);
#1898=VECTOR('',#6331,0.4);
#1998=CIRCLE('',#5179,0.1954);
#1999=CIRCLE('',#5214,0.1954);
#2000=CIRCLE('',#5216,0.15555);
#2001=CIRCLE('',#5251,0.15555);
#2002=CIRCLE('',#5253,0.1954);
#2003=CIRCLE('',#5262,0.4);
#2004=CIRCLE('',#5264,0.4);
#2246=VERTEX_POINT('',#7259);
#2247=VERTEX_POINT('',#7260);
#2248=VERTEX_POINT('',#7262);
#2249=VERTEX_POINT('',#7273);
#2250=VERTEX_POINT('',#7283);
#2251=VERTEX_POINT('',#7284);
#2252=VERTEX_POINT('',#7331);
#2253=VERTEX_POINT('',#7332);
#2254=VERTEX_POINT('',#7379);
#2255=VERTEX_POINT('',#7380);
#2256=VERTEX_POINT('',#7430);
#2257=VERTEX_POINT('',#7431);
#2258=VERTEX_POINT('',#7478);
#2259=VERTEX_POINT('',#7479);
#2260=VERTEX_POINT('',#7526);
#2261=VERTEX_POINT('',#7527);
#2262=VERTEX_POINT('',#7574);
#2263=VERTEX_POINT('',#7575);
#2264=VERTEX_POINT('',#7628);
#2265=VERTEX_POINT('',#7629);
#2266=VERTEX_POINT('',#7676);
#2267=VERTEX_POINT('',#7677);
#2268=VERTEX_POINT('',#7724);
#2269=VERTEX_POINT('',#7725);
#2270=VERTEX_POINT('',#7778);
#2271=VERTEX_POINT('',#7779);
#2272=VERTEX_POINT('',#7826);
#2273=VERTEX_POINT('',#7827);
#2274=VERTEX_POINT('',#7874);
#2275=VERTEX_POINT('',#7875);
#2276=VERTEX_POINT('',#7922);
#2277=VERTEX_POINT('',#7923);
#2278=VERTEX_POINT('',#7976);
#2279=VERTEX_POINT('',#7977);
#2280=VERTEX_POINT('',#8024);
#2281=VERTEX_POINT('',#8025);
#2282=VERTEX_POINT('',#8072);
#2283=VERTEX_POINT('',#8073);
#2284=VERTEX_POINT('',#8126);
#2285=VERTEX_POINT('',#8127);
#2286=VERTEX_POINT('',#8174);
#2287=VERTEX_POINT('',#8175);
#2288=VERTEX_POINT('',#8222);
#2289=VERTEX_POINT('',#8223);
#2290=VERTEX_POINT('',#8276);
#2291=VERTEX_POINT('',#8277);
#2292=VERTEX_POINT('',#8324);
#2293=VERTEX_POINT('',#8325);
#2294=VERTEX_POINT('',#8372);
#2295=VERTEX_POINT('',#8373);
#2296=VERTEX_POINT('',#8420);
#2297=VERTEX_POINT('',#8421);
#2298=VERTEX_POINT('',#8474);
#2299=VERTEX_POINT('',#8475);
#2300=VERTEX_POINT('',#8522);
#2301=VERTEX_POINT('',#8523);
#2302=VERTEX_POINT('',#8570);
#2303=VERTEX_POINT('',#8571);
#2304=VERTEX_POINT('',#8624);
#2305=VERTEX_POINT('',#8625);
#2306=VERTEX_POINT('',#8672);
#2307=VERTEX_POINT('',#8673);
#2308=VERTEX_POINT('',#8720);
#2309=VERTEX_POINT('',#8721);
#2310=VERTEX_POINT('',#8774);
#2311=VERTEX_POINT('',#8775);
#2312=VERTEX_POINT('',#8822);
#2313=VERTEX_POINT('',#8823);
#2314=VERTEX_POINT('',#8870);
#2315=VERTEX_POINT('',#8871);
#2316=VERTEX_POINT('',#8918);
#2317=VERTEX_POINT('',#8919);
#2318=VERTEX_POINT('',#8921);
#2319=VERTEX_POINT('',#8971);
#2320=VERTEX_POINT('',#8972);
#2321=VERTEX_POINT('',#8974);
#2322=VERTEX_POINT('',#8983);
#2323=VERTEX_POINT('',#8992);
#2324=VERTEX_POINT('',#8993);
#2325=VERTEX_POINT('',#9017);
#2326=VERTEX_POINT('',#9018);
#2327=VERTEX_POINT('',#9041);
#2328=VERTEX_POINT('',#9042);
#2329=VERTEX_POINT('',#9065);
#2330=VERTEX_POINT('',#9066);
#2331=VERTEX_POINT('',#9090);
#2332=VERTEX_POINT('',#9091);
#2333=VERTEX_POINT('',#9115);
#2334=VERTEX_POINT('',#9116);
#2335=VERTEX_POINT('',#9139);
#2336=VERTEX_POINT('',#9140);
#2337=VERTEX_POINT('',#9164);
#2338=VERTEX_POINT('',#9165);
#2339=VERTEX_POINT('',#9189);
#2340=VERTEX_POINT('',#9190);
#2341=VERTEX_POINT('',#9213);
#2342=VERTEX_POINT('',#9214);
#2343=VERTEX_POINT('',#9238);
#2344=VERTEX_POINT('',#9239);
#2345=VERTEX_POINT('',#9263);
#2346=VERTEX_POINT('',#9264);
#2347=VERTEX_POINT('',#9287);
#2348=VERTEX_POINT('',#9288);
#2349=VERTEX_POINT('',#9311);
#2350=VERTEX_POINT('',#9312);
#2351=VERTEX_POINT('',#9336);
#2352=VERTEX_POINT('',#9337);
#2353=VERTEX_POINT('',#9361);
#2354=VERTEX_POINT('',#9362);
#2355=VERTEX_POINT('',#9385);
#2356=VERTEX_POINT('',#9386);
#2357=VERTEX_POINT('',#9410);
#2358=VERTEX_POINT('',#9411);
#2359=VERTEX_POINT('',#9435);
#2360=VERTEX_POINT('',#9436);
#2361=VERTEX_POINT('',#9459);
#2362=VERTEX_POINT('',#9460);
#2363=VERTEX_POINT('',#9484);
#2364=VERTEX_POINT('',#9485);
#2365=VERTEX_POINT('',#9509);
#2366=VERTEX_POINT('',#9510);
#2367=VERTEX_POINT('',#9533);
#2368=VERTEX_POINT('',#9534);
#2369=VERTEX_POINT('',#9557);
#2370=VERTEX_POINT('',#9558);
#2371=VERTEX_POINT('',#9582);
#2372=VERTEX_POINT('',#9583);
#2373=VERTEX_POINT('',#9607);
#2374=VERTEX_POINT('',#9608);
#2375=VERTEX_POINT('',#9631);
#2376=VERTEX_POINT('',#9632);
#2377=VERTEX_POINT('',#9656);
#2378=VERTEX_POINT('',#9657);
#2379=VERTEX_POINT('',#9681);
#2380=VERTEX_POINT('',#9682);
#2381=VERTEX_POINT('',#9705);
#2382=VERTEX_POINT('',#9706);
#2383=VERTEX_POINT('',#9730);
#2384=VERTEX_POINT('',#9731);
#2385=VERTEX_POINT('',#9754);
#2386=VERTEX_POINT('',#9755);
#2387=VERTEX_POINT('',#9779);
#2388=VERTEX_POINT('',#9780);
#2389=VERTEX_POINT('',#10686);
#2390=VERTEX_POINT('',#10746);
#2391=VERTEX_POINT('',#10809);
#2392=VERTEX_POINT('',#11816);
#2393=VERTEX_POINT('',#11817);
#2394=VERTEX_POINT('',#11819);
#2395=VERTEX_POINT('',#11821);
#2396=VERTEX_POINT('',#11825);
#2397=VERTEX_POINT('',#11827);
#2398=VERTEX_POINT('',#11831);
#2399=VERTEX_POINT('',#11833);
#2400=VERTEX_POINT('',#11837);
#2401=VERTEX_POINT('',#11839);
#2402=VERTEX_POINT('',#11843);
#2403=VERTEX_POINT('',#11845);
#2404=VERTEX_POINT('',#11853);
#2405=VERTEX_POINT('',#11856);
#2803=EDGE_CURVE('',#2246,#2247,#1409,.T.);
#2804=EDGE_CURVE('',#2246,#2248,#175,.T.);
#2805=EDGE_CURVE('',#2248,#2249,#1998,.F.);
#2806=EDGE_CURVE('',#2249,#2247,#176,.T.);
#2807=EDGE_CURVE('',#2250,#2251,#1410,.T.);
#2808=EDGE_CURVE('',#2250,#2246,#177,.T.);
#2809=EDGE_CURVE('',#2247,#2251,#178,.T.);
#2810=EDGE_CURVE('',#2252,#2253,#1411,.T.);
#2811=EDGE_CURVE('',#2252,#2250,#179,.T.);
#2812=EDGE_CURVE('',#2251,#2253,#180,.T.);
#2813=EDGE_CURVE('',#2254,#2255,#1412,.T.);
#2814=EDGE_CURVE('',#2254,#2252,#181,.T.);
#2815=EDGE_CURVE('',#2253,#2255,#182,.T.);
#2816=EDGE_CURVE('',#2256,#2257,#1413,.T.);
#2817=EDGE_CURVE('',#2256,#2254,#183,.T.);
#2818=EDGE_CURVE('',#2255,#2257,#184,.T.);
#2819=EDGE_CURVE('',#2258,#2259,#1414,.T.);
#2820=EDGE_CURVE('',#2258,#2256,#185,.T.);
#2821=EDGE_CURVE('',#2257,#2259,#186,.T.);
#2822=EDGE_CURVE('',#2260,#2261,#1415,.T.);
#2823=EDGE_CURVE('',#2260,#2258,#187,.T.);
#2824=EDGE_CURVE('',#2259,#2261,#188,.T.);
#2825=EDGE_CURVE('',#2262,#2263,#1416,.T.);
#2826=EDGE_CURVE('',#2262,#2260,#189,.T.);
#2827=EDGE_CURVE('',#2261,#2263,#190,.T.);
#2828=EDGE_CURVE('',#2264,#2265,#1417,.T.);
#2829=EDGE_CURVE('',#2264,#2262,#191,.T.);
#2830=EDGE_CURVE('',#2263,#2265,#192,.T.);
#2831=EDGE_CURVE('',#2266,#2267,#1418,.T.);
#2832=EDGE_CURVE('',#2266,#2264,#193,.T.);
#2833=EDGE_CURVE('',#2265,#2267,#194,.T.);
#2834=EDGE_CURVE('',#2268,#2269,#1419,.T.);
#2835=EDGE_CURVE('',#2268,#2266,#195,.T.);
#2836=EDGE_CURVE('',#2267,#2269,#196,.T.);
#2837=EDGE_CURVE('',#2270,#2271,#1420,.T.);
#2838=EDGE_CURVE('',#2270,#2268,#197,.T.);
#2839=EDGE_CURVE('',#2269,#2271,#198,.T.);
#2840=EDGE_CURVE('',#2272,#2273,#1421,.T.);
#2841=EDGE_CURVE('',#2272,#2270,#199,.T.);
#2842=EDGE_CURVE('',#2271,#2273,#200,.T.);
#2843=EDGE_CURVE('',#2274,#2275,#1422,.T.);
#2844=EDGE_CURVE('',#2274,#2272,#201,.T.);
#2845=EDGE_CURVE('',#2273,#2275,#202,.T.);
#2846=EDGE_CURVE('',#2276,#2277,#1423,.T.);
#2847=EDGE_CURVE('',#2276,#2274,#203,.T.);
#2848=EDGE_CURVE('',#2275,#2277,#204,.T.);
#2849=EDGE_CURVE('',#2278,#2279,#1424,.T.);
#2850=EDGE_CURVE('',#2278,#2276,#205,.T.);
#2851=EDGE_CURVE('',#2277,#2279,#206,.T.);
#2852=EDGE_CURVE('',#2280,#2281,#1425,.T.);
#2853=EDGE_CURVE('',#2280,#2278,#207,.T.);
#2854=EDGE_CURVE('',#2279,#2281,#208,.T.);
#2855=EDGE_CURVE('',#2282,#2283,#1426,.T.);
#2856=EDGE_CURVE('',#2282,#2280,#209,.T.);
#2857=EDGE_CURVE('',#2281,#2283,#210,.T.);
#2858=EDGE_CURVE('',#2284,#2285,#1427,.T.);
#2859=EDGE_CURVE('',#2284,#2282,#211,.T.);
#2860=EDGE_CURVE('',#2283,#2285,#212,.T.);
#2861=EDGE_CURVE('',#2286,#2287,#1428,.T.);
#2862=EDGE_CURVE('',#2286,#2284,#213,.T.);
#2863=EDGE_CURVE('',#2285,#2287,#214,.T.);
#2864=EDGE_CURVE('',#2288,#2289,#1429,.T.);
#2865=EDGE_CURVE('',#2288,#2286,#215,.T.);
#2866=EDGE_CURVE('',#2287,#2289,#216,.T.);
#2867=EDGE_CURVE('',#2290,#2291,#1430,.T.);
#2868=EDGE_CURVE('',#2290,#2288,#217,.T.);
#2869=EDGE_CURVE('',#2289,#2291,#218,.T.);
#2870=EDGE_CURVE('',#2292,#2293,#1431,.T.);
#2871=EDGE_CURVE('',#2292,#2290,#219,.T.);
#2872=EDGE_CURVE('',#2291,#2293,#220,.T.);
#2873=EDGE_CURVE('',#2294,#2295,#1432,.T.);
#2874=EDGE_CURVE('',#2294,#2292,#221,.T.);
#2875=EDGE_CURVE('',#2293,#2295,#222,.T.);
#2876=EDGE_CURVE('',#2296,#2297,#1433,.T.);
#2877=EDGE_CURVE('',#2296,#2294,#223,.T.);
#2878=EDGE_CURVE('',#2295,#2297,#224,.T.);
#2879=EDGE_CURVE('',#2298,#2299,#1434,.T.);
#2880=EDGE_CURVE('',#2298,#2296,#225,.T.);
#2881=EDGE_CURVE('',#2297,#2299,#226,.T.);
#2882=EDGE_CURVE('',#2300,#2301,#1435,.T.);
#2883=EDGE_CURVE('',#2300,#2298,#227,.T.);
#2884=EDGE_CURVE('',#2299,#2301,#228,.T.);
#2885=EDGE_CURVE('',#2302,#2303,#1436,.T.);
#2886=EDGE_CURVE('',#2302,#2300,#229,.T.);
#2887=EDGE_CURVE('',#2301,#2303,#230,.T.);
#2888=EDGE_CURVE('',#2304,#2305,#1437,.T.);
#2889=EDGE_CURVE('',#2304,#2302,#231,.T.);
#2890=EDGE_CURVE('',#2303,#2305,#232,.T.);
#2891=EDGE_CURVE('',#2306,#2307,#1438,.T.);
#2892=EDGE_CURVE('',#2306,#2304,#233,.T.);
#2893=EDGE_CURVE('',#2305,#2307,#234,.T.);
#2894=EDGE_CURVE('',#2308,#2309,#1439,.T.);
#2895=EDGE_CURVE('',#2308,#2306,#235,.T.);
#2896=EDGE_CURVE('',#2307,#2309,#236,.T.);
#2897=EDGE_CURVE('',#2310,#2311,#1440,.T.);
#2898=EDGE_CURVE('',#2310,#2308,#237,.T.);
#2899=EDGE_CURVE('',#2309,#2311,#238,.T.);
#2900=EDGE_CURVE('',#2312,#2313,#1441,.T.);
#2901=EDGE_CURVE('',#2312,#2310,#239,.T.);
#2902=EDGE_CURVE('',#2311,#2313,#240,.T.);
#2903=EDGE_CURVE('',#2314,#2315,#1442,.T.);
#2904=EDGE_CURVE('',#2314,#2312,#241,.T.);
#2905=EDGE_CURVE('',#2313,#2315,#242,.T.);
#2906=EDGE_CURVE('',#2316,#2317,#1443,.T.);
#2907=EDGE_CURVE('',#2318,#2316,#1999,.F.);
#2908=EDGE_CURVE('',#2318,#2314,#243,.T.);
#2909=EDGE_CURVE('',#2315,#2317,#244,.T.);
#2910=EDGE_CURVE('',#2319,#2320,#1444,.T.);
#2911=EDGE_CURVE('',#2319,#2321,#245,.T.);
#2912=EDGE_CURVE('',#2322,#2321,#2000,.T.);
#2913=EDGE_CURVE('',#2320,#2322,#246,.T.);
#2914=EDGE_CURVE('',#2323,#2324,#1445,.T.);
#2915=EDGE_CURVE('',#2323,#2319,#247,.T.);
#2916=EDGE_CURVE('',#2324,#2320,#248,.T.);
#2917=EDGE_CURVE('',#2325,#2326,#1446,.T.);
#2918=EDGE_CURVE('',#2325,#2323,#249,.T.);
#2919=EDGE_CURVE('',#2326,#2324,#250,.T.);
#2920=EDGE_CURVE('',#2327,#2328,#1447,.T.);
#2921=EDGE_CURVE('',#2327,#2325,#251,.T.);
#2922=EDGE_CURVE('',#2328,#2326,#252,.T.);
#2923=EDGE_CURVE('',#2329,#2330,#1448,.T.);
#2924=EDGE_CURVE('',#2329,#2327,#253,.T.);
#2925=EDGE_CURVE('',#2330,#2328,#254,.T.);
#2926=EDGE_CURVE('',#2331,#2332,#1449,.T.);
#2927=EDGE_CURVE('',#2331,#2329,#255,.T.);
#2928=EDGE_CURVE('',#2332,#2330,#256,.T.);
#2929=EDGE_CURVE('',#2333,#2334,#1450,.T.);
#2930=EDGE_CURVE('',#2333,#2331,#257,.T.);
#2931=EDGE_CURVE('',#2334,#2332,#258,.T.);
#2932=EDGE_CURVE('',#2335,#2336,#1451,.T.);
#2933=EDGE_CURVE('',#2335,#2333,#259,.T.);
#2934=EDGE_CURVE('',#2336,#2334,#260,.T.);
#2935=EDGE_CURVE('',#2337,#2338,#1452,.T.);
#2936=EDGE_CURVE('',#2337,#2335,#261,.T.);
#2937=EDGE_CURVE('',#2338,#2336,#262,.T.);
#2938=EDGE_CURVE('',#2339,#2340,#1453,.T.);
#2939=EDGE_CURVE('',#2339,#2337,#263,.T.);
#2940=EDGE_CURVE('',#2340,#2338,#264,.T.);
#2941=EDGE_CURVE('',#2341,#2342,#1454,.T.);
#2942=EDGE_CURVE('',#2341,#2339,#265,.T.);
#2943=EDGE_CURVE('',#2342,#2340,#266,.T.);
#2944=EDGE_CURVE('',#2343,#2344,#1455,.T.);
#2945=EDGE_CURVE('',#2343,#2341,#267,.T.);
#2946=EDGE_CURVE('',#2344,#2342,#268,.T.);
#2947=EDGE_CURVE('',#2345,#2346,#1456,.T.);
#2948=EDGE_CURVE('',#2345,#2343,#269,.T.);
#2949=EDGE_CURVE('',#2346,#2344,#270,.T.);
#2950=EDGE_CURVE('',#2347,#2348,#1457,.T.);
#2951=EDGE_CURVE('',#2347,#2345,#271,.T.);
#2952=EDGE_CURVE('',#2348,#2346,#272,.T.);
#2953=EDGE_CURVE('',#2349,#2350,#1458,.T.);
#2954=EDGE_CURVE('',#2349,#2347,#273,.T.);
#2955=EDGE_CURVE('',#2350,#2348,#274,.T.);
#2956=EDGE_CURVE('',#2351,#2352,#1459,.T.);
#2957=EDGE_CURVE('',#2351,#2349,#275,.T.);
#2958=EDGE_CURVE('',#2352,#2350,#276,.T.);
#2959=EDGE_CURVE('',#2353,#2354,#1460,.T.);
#2960=EDGE_CURVE('',#2353,#2351,#277,.T.);
#2961=EDGE_CURVE('',#2354,#2352,#278,.T.);
#2962=EDGE_CURVE('',#2355,#2356,#1461,.T.);
#2963=EDGE_CURVE('',#2355,#2353,#279,.T.);
#2964=EDGE_CURVE('',#2356,#2354,#280,.T.);
#2965=EDGE_CURVE('',#2357,#2358,#1462,.T.);
#2966=EDGE_CURVE('',#2357,#2355,#281,.T.);
#2967=EDGE_CURVE('',#2358,#2356,#282,.T.);
#2968=EDGE_CURVE('',#2359,#2360,#1463,.T.);
#2969=EDGE_CURVE('',#2359,#2357,#283,.T.);
#2970=EDGE_CURVE('',#2360,#2358,#284,.T.);
#2971=EDGE_CURVE('',#2361,#2362,#1464,.T.);
#2972=EDGE_CURVE('',#2361,#2359,#285,.T.);
#2973=EDGE_CURVE('',#2362,#2360,#286,.T.);
#2974=EDGE_CURVE('',#2363,#2364,#1465,.T.);
#2975=EDGE_CURVE('',#2363,#2361,#287,.T.);
#2976=EDGE_CURVE('',#2364,#2362,#288,.T.);
#2977=EDGE_CURVE('',#2365,#2366,#1466,.T.);
#2978=EDGE_CURVE('',#2365,#2363,#289,.T.);
#2979=EDGE_CURVE('',#2366,#2364,#290,.T.);
#2980=EDGE_CURVE('',#2367,#2368,#1467,.T.);
#2981=EDGE_CURVE('',#2367,#2365,#291,.T.);
#2982=EDGE_CURVE('',#2368,#2366,#292,.T.);
#2983=EDGE_CURVE('',#2369,#2370,#1468,.T.);
#2984=EDGE_CURVE('',#2369,#2367,#293,.T.);
#2985=EDGE_CURVE('',#2370,#2368,#294,.T.);
#2986=EDGE_CURVE('',#2371,#2372,#1469,.T.);
#2987=EDGE_CURVE('',#2371,#2369,#295,.T.);
#2988=EDGE_CURVE('',#2372,#2370,#296,.T.);
#2989=EDGE_CURVE('',#2373,#2374,#1470,.T.);
#2990=EDGE_CURVE('',#2373,#2371,#297,.T.);
#2991=EDGE_CURVE('',#2374,#2372,#298,.T.);
#2992=EDGE_CURVE('',#2375,#2376,#1471,.T.);
#2993=EDGE_CURVE('',#2375,#2373,#299,.T.);
#2994=EDGE_CURVE('',#2376,#2374,#300,.T.);
#2995=EDGE_CURVE('',#2377,#2378,#1472,.T.);
#2996=EDGE_CURVE('',#2377,#2375,#301,.T.);
#2997=EDGE_CURVE('',#2378,#2376,#302,.T.);
#2998=EDGE_CURVE('',#2379,#2380,#1473,.T.);
#2999=EDGE_CURVE('',#2379,#2377,#303,.T.);
#3000=EDGE_CURVE('',#2380,#2378,#304,.T.);
#3001=EDGE_CURVE('',#2381,#2382,#1474,.T.);
#3002=EDGE_CURVE('',#2381,#2379,#305,.T.);
#3003=EDGE_CURVE('',#2382,#2380,#306,.T.);
#3004=EDGE_CURVE('',#2383,#2384,#1475,.T.);
#3005=EDGE_CURVE('',#2383,#2381,#307,.T.);
#3006=EDGE_CURVE('',#2384,#2382,#308,.T.);
#3007=EDGE_CURVE('',#2385,#2386,#1476,.T.);
#3008=EDGE_CURVE('',#2385,#2383,#309,.T.);
#3009=EDGE_CURVE('',#2386,#2384,#310,.T.);
#3010=EDGE_CURVE('',#2387,#2388,#1477,.T.);
#3011=EDGE_CURVE('',#2387,#2385,#311,.T.);
#3012=EDGE_CURVE('',#2388,#2386,#312,.T.);
#3013=EDGE_CURVE('',#2389,#2322,#313,.T.);
#3014=EDGE_CURVE('',#2317,#2389,#314,.T.);
#3015=EDGE_CURVE('',#2390,#2249,#315,.T.);
#3016=EDGE_CURVE('',#2390,#2388,#316,.T.);
#3017=EDGE_CURVE('',#2391,#2390,#2001,.T.);
#3018=EDGE_CURVE('',#2391,#2387,#317,.T.);
#3019=EDGE_CURVE('',#2321,#2318,#318,.T.);
#3020=EDGE_CURVE('',#2248,#2391,#319,.T.);
#3021=EDGE_CURVE('',#2316,#2389,#2002,.F.);
#3022=EDGE_CURVE('',#2392,#2393,#1478,.T.);
#3023=EDGE_CURVE('',#2392,#2394,#1479,.T.);
#3024=EDGE_CURVE('',#2394,#2395,#1480,.T.);
#3025=EDGE_CURVE('',#2393,#2395,#1481,.T.);
#3026=EDGE_CURVE('',#2396,#2392,#1482,.T.);
#3027=EDGE_CURVE('',#2396,#2397,#1483,.T.);
#3028=EDGE_CURVE('',#2397,#2394,#1484,.T.);
#3029=EDGE_CURVE('',#2398,#2396,#1485,.T.);
#3030=EDGE_CURVE('',#2398,#2399,#1486,.T.);
#3031=EDGE_CURVE('',#2399,#2397,#1487,.T.);
#3032=EDGE_CURVE('',#2400,#2398,#1488,.T.);
#3033=EDGE_CURVE('',#2400,#2401,#1489,.T.);
#3034=EDGE_CURVE('',#2401,#2399,#1490,.T.);
#3035=EDGE_CURVE('',#2402,#2400,#1491,.T.);
#3036=EDGE_CURVE('',#2402,#2403,#1492,.T.);
#3037=EDGE_CURVE('',#2403,#2401,#1493,.T.);
#3038=EDGE_CURVE('',#2393,#2402,#1494,.T.);
#3039=EDGE_CURVE('',#2395,#2403,#1495,.T.);
#3040=EDGE_CURVE('',#2404,#2404,#2003,.T.);
#3041=EDGE_CURVE('',#2404,#2405,#1496,.T.);
#3042=EDGE_CURVE('',#2405,#2405,#2004,.T.);
#3814=ORIENTED_EDGE('',*,*,#2803,.F.);
#3815=ORIENTED_EDGE('',*,*,#2804,.T.);
#3816=ORIENTED_EDGE('',*,*,#2805,.T.);
#3817=ORIENTED_EDGE('',*,*,#2806,.T.);
#3818=ORIENTED_EDGE('',*,*,#2807,.F.);
#3819=ORIENTED_EDGE('',*,*,#2808,.T.);
#3820=ORIENTED_EDGE('',*,*,#2803,.T.);
#3821=ORIENTED_EDGE('',*,*,#2809,.T.);
#3822=ORIENTED_EDGE('',*,*,#2810,.F.);
#3823=ORIENTED_EDGE('',*,*,#2811,.T.);
#3824=ORIENTED_EDGE('',*,*,#2807,.T.);
#3825=ORIENTED_EDGE('',*,*,#2812,.T.);
#3826=ORIENTED_EDGE('',*,*,#2813,.F.);
#3827=ORIENTED_EDGE('',*,*,#2814,.T.);
#3828=ORIENTED_EDGE('',*,*,#2810,.T.);
#3829=ORIENTED_EDGE('',*,*,#2815,.T.);
#3830=ORIENTED_EDGE('',*,*,#2816,.F.);
#3831=ORIENTED_EDGE('',*,*,#2817,.T.);
#3832=ORIENTED_EDGE('',*,*,#2813,.T.);
#3833=ORIENTED_EDGE('',*,*,#2818,.T.);
#3834=ORIENTED_EDGE('',*,*,#2819,.F.);
#3835=ORIENTED_EDGE('',*,*,#2820,.T.);
#3836=ORIENTED_EDGE('',*,*,#2816,.T.);
#3837=ORIENTED_EDGE('',*,*,#2821,.T.);
#3838=ORIENTED_EDGE('',*,*,#2822,.F.);
#3839=ORIENTED_EDGE('',*,*,#2823,.T.);
#3840=ORIENTED_EDGE('',*,*,#2819,.T.);
#3841=ORIENTED_EDGE('',*,*,#2824,.T.);
#3842=ORIENTED_EDGE('',*,*,#2825,.F.);
#3843=ORIENTED_EDGE('',*,*,#2826,.T.);
#3844=ORIENTED_EDGE('',*,*,#2822,.T.);
#3845=ORIENTED_EDGE('',*,*,#2827,.T.);
#3846=ORIENTED_EDGE('',*,*,#2828,.F.);
#3847=ORIENTED_EDGE('',*,*,#2829,.T.);
#3848=ORIENTED_EDGE('',*,*,#2825,.T.);
#3849=ORIENTED_EDGE('',*,*,#2830,.T.);
#3850=ORIENTED_EDGE('',*,*,#2831,.F.);
#3851=ORIENTED_EDGE('',*,*,#2832,.T.);
#3852=ORIENTED_EDGE('',*,*,#2828,.T.);
#3853=ORIENTED_EDGE('',*,*,#2833,.T.);
#3854=ORIENTED_EDGE('',*,*,#2834,.F.);
#3855=ORIENTED_EDGE('',*,*,#2835,.T.);
#3856=ORIENTED_EDGE('',*,*,#2831,.T.);
#3857=ORIENTED_EDGE('',*,*,#2836,.T.);
#3858=ORIENTED_EDGE('',*,*,#2837,.F.);
#3859=ORIENTED_EDGE('',*,*,#2838,.T.);
#3860=ORIENTED_EDGE('',*,*,#2834,.T.);
#3861=ORIENTED_EDGE('',*,*,#2839,.T.);
#3862=ORIENTED_EDGE('',*,*,#2840,.F.);
#3863=ORIENTED_EDGE('',*,*,#2841,.T.);
#3864=ORIENTED_EDGE('',*,*,#2837,.T.);
#3865=ORIENTED_EDGE('',*,*,#2842,.T.);
#3866=ORIENTED_EDGE('',*,*,#2843,.F.);
#3867=ORIENTED_EDGE('',*,*,#2844,.T.);
#3868=ORIENTED_EDGE('',*,*,#2840,.T.);
#3869=ORIENTED_EDGE('',*,*,#2845,.T.);
#3870=ORIENTED_EDGE('',*,*,#2846,.F.);
#3871=ORIENTED_EDGE('',*,*,#2847,.T.);
#3872=ORIENTED_EDGE('',*,*,#2843,.T.);
#3873=ORIENTED_EDGE('',*,*,#2848,.T.);
#3874=ORIENTED_EDGE('',*,*,#2849,.F.);
#3875=ORIENTED_EDGE('',*,*,#2850,.T.);
#3876=ORIENTED_EDGE('',*,*,#2846,.T.);
#3877=ORIENTED_EDGE('',*,*,#2851,.T.);
#3878=ORIENTED_EDGE('',*,*,#2852,.F.);
#3879=ORIENTED_EDGE('',*,*,#2853,.T.);
#3880=ORIENTED_EDGE('',*,*,#2849,.T.);
#3881=ORIENTED_EDGE('',*,*,#2854,.T.);
#3882=ORIENTED_EDGE('',*,*,#2855,.F.);
#3883=ORIENTED_EDGE('',*,*,#2856,.T.);
#3884=ORIENTED_EDGE('',*,*,#2852,.T.);
#3885=ORIENTED_EDGE('',*,*,#2857,.T.);
#3886=ORIENTED_EDGE('',*,*,#2858,.F.);
#3887=ORIENTED_EDGE('',*,*,#2859,.T.);
#3888=ORIENTED_EDGE('',*,*,#2855,.T.);
#3889=ORIENTED_EDGE('',*,*,#2860,.T.);
#3890=ORIENTED_EDGE('',*,*,#2861,.F.);
#3891=ORIENTED_EDGE('',*,*,#2862,.T.);
#3892=ORIENTED_EDGE('',*,*,#2858,.T.);
#3893=ORIENTED_EDGE('',*,*,#2863,.T.);
#3894=ORIENTED_EDGE('',*,*,#2864,.F.);
#3895=ORIENTED_EDGE('',*,*,#2865,.T.);
#3896=ORIENTED_EDGE('',*,*,#2861,.T.);
#3897=ORIENTED_EDGE('',*,*,#2866,.T.);
#3898=ORIENTED_EDGE('',*,*,#2867,.F.);
#3899=ORIENTED_EDGE('',*,*,#2868,.T.);
#3900=ORIENTED_EDGE('',*,*,#2864,.T.);
#3901=ORIENTED_EDGE('',*,*,#2869,.T.);
#3902=ORIENTED_EDGE('',*,*,#2870,.F.);
#3903=ORIENTED_EDGE('',*,*,#2871,.T.);
#3904=ORIENTED_EDGE('',*,*,#2867,.T.);
#3905=ORIENTED_EDGE('',*,*,#2872,.T.);
#3906=ORIENTED_EDGE('',*,*,#2873,.F.);
#3907=ORIENTED_EDGE('',*,*,#2874,.T.);
#3908=ORIENTED_EDGE('',*,*,#2870,.T.);
#3909=ORIENTED_EDGE('',*,*,#2875,.T.);
#3910=ORIENTED_EDGE('',*,*,#2876,.F.);
#3911=ORIENTED_EDGE('',*,*,#2877,.T.);
#3912=ORIENTED_EDGE('',*,*,#2873,.T.);
#3913=ORIENTED_EDGE('',*,*,#2878,.T.);
#3914=ORIENTED_EDGE('',*,*,#2879,.F.);
#3915=ORIENTED_EDGE('',*,*,#2880,.T.);
#3916=ORIENTED_EDGE('',*,*,#2876,.T.);
#3917=ORIENTED_EDGE('',*,*,#2881,.T.);
#3918=ORIENTED_EDGE('',*,*,#2882,.F.);
#3919=ORIENTED_EDGE('',*,*,#2883,.T.);
#3920=ORIENTED_EDGE('',*,*,#2879,.T.);
#3921=ORIENTED_EDGE('',*,*,#2884,.T.);
#3922=ORIENTED_EDGE('',*,*,#2885,.F.);
#3923=ORIENTED_EDGE('',*,*,#2886,.T.);
#3924=ORIENTED_EDGE('',*,*,#2882,.T.);
#3925=ORIENTED_EDGE('',*,*,#2887,.T.);
#3926=ORIENTED_EDGE('',*,*,#2888,.F.);
#3927=ORIENTED_EDGE('',*,*,#2889,.T.);
#3928=ORIENTED_EDGE('',*,*,#2885,.T.);
#3929=ORIENTED_EDGE('',*,*,#2890,.T.);
#3930=ORIENTED_EDGE('',*,*,#2891,.F.);
#3931=ORIENTED_EDGE('',*,*,#2892,.T.);
#3932=ORIENTED_EDGE('',*,*,#2888,.T.);
#3933=ORIENTED_EDGE('',*,*,#2893,.T.);
#3934=ORIENTED_EDGE('',*,*,#2894,.F.);
#3935=ORIENTED_EDGE('',*,*,#2895,.T.);
#3936=ORIENTED_EDGE('',*,*,#2891,.T.);
#3937=ORIENTED_EDGE('',*,*,#2896,.T.);
#3938=ORIENTED_EDGE('',*,*,#2897,.F.);
#3939=ORIENTED_EDGE('',*,*,#2898,.T.);
#3940=ORIENTED_EDGE('',*,*,#2894,.T.);
#3941=ORIENTED_EDGE('',*,*,#2899,.T.);
#3942=ORIENTED_EDGE('',*,*,#2900,.F.);
#3943=ORIENTED_EDGE('',*,*,#2901,.T.);
#3944=ORIENTED_EDGE('',*,*,#2897,.T.);
#3945=ORIENTED_EDGE('',*,*,#2902,.T.);
#3946=ORIENTED_EDGE('',*,*,#2903,.F.);
#3947=ORIENTED_EDGE('',*,*,#2904,.T.);
#3948=ORIENTED_EDGE('',*,*,#2900,.T.);
#3949=ORIENTED_EDGE('',*,*,#2905,.T.);
#3950=ORIENTED_EDGE('',*,*,#2906,.F.);
#3951=ORIENTED_EDGE('',*,*,#2907,.F.);
#3952=ORIENTED_EDGE('',*,*,#2908,.T.);
#3953=ORIENTED_EDGE('',*,*,#2903,.T.);
#3954=ORIENTED_EDGE('',*,*,#2909,.T.);
#3955=ORIENTED_EDGE('',*,*,#2910,.F.);
#3956=ORIENTED_EDGE('',*,*,#2911,.T.);
#3957=ORIENTED_EDGE('',*,*,#2912,.F.);
#3958=ORIENTED_EDGE('',*,*,#2913,.F.);
#3959=ORIENTED_EDGE('',*,*,#2914,.F.);
#3960=ORIENTED_EDGE('',*,*,#2915,.T.);
#3961=ORIENTED_EDGE('',*,*,#2910,.T.);
#3962=ORIENTED_EDGE('',*,*,#2916,.F.);
#3963=ORIENTED_EDGE('',*,*,#2917,.F.);
#3964=ORIENTED_EDGE('',*,*,#2918,.T.);
#3965=ORIENTED_EDGE('',*,*,#2914,.T.);
#3966=ORIENTED_EDGE('',*,*,#2919,.F.);
#3967=ORIENTED_EDGE('',*,*,#2920,.F.);
#3968=ORIENTED_EDGE('',*,*,#2921,.T.);
#3969=ORIENTED_EDGE('',*,*,#2917,.T.);
#3970=ORIENTED_EDGE('',*,*,#2922,.F.);
#3971=ORIENTED_EDGE('',*,*,#2923,.F.);
#3972=ORIENTED_EDGE('',*,*,#2924,.T.);
#3973=ORIENTED_EDGE('',*,*,#2920,.T.);
#3974=ORIENTED_EDGE('',*,*,#2925,.F.);
#3975=ORIENTED_EDGE('',*,*,#2926,.F.);
#3976=ORIENTED_EDGE('',*,*,#2927,.T.);
#3977=ORIENTED_EDGE('',*,*,#2923,.T.);
#3978=ORIENTED_EDGE('',*,*,#2928,.F.);
#3979=ORIENTED_EDGE('',*,*,#2929,.F.);
#3980=ORIENTED_EDGE('',*,*,#2930,.T.);
#3981=ORIENTED_EDGE('',*,*,#2926,.T.);
#3982=ORIENTED_EDGE('',*,*,#2931,.F.);
#3983=ORIENTED_EDGE('',*,*,#2932,.F.);
#3984=ORIENTED_EDGE('',*,*,#2933,.T.);
#3985=ORIENTED_EDGE('',*,*,#2929,.T.);
#3986=ORIENTED_EDGE('',*,*,#2934,.F.);
#3987=ORIENTED_EDGE('',*,*,#2935,.F.);
#3988=ORIENTED_EDGE('',*,*,#2936,.T.);
#3989=ORIENTED_EDGE('',*,*,#2932,.T.);
#3990=ORIENTED_EDGE('',*,*,#2937,.F.);
#3991=ORIENTED_EDGE('',*,*,#2938,.F.);
#3992=ORIENTED_EDGE('',*,*,#2939,.T.);
#3993=ORIENTED_EDGE('',*,*,#2935,.T.);
#3994=ORIENTED_EDGE('',*,*,#2940,.F.);
#3995=ORIENTED_EDGE('',*,*,#2941,.F.);
#3996=ORIENTED_EDGE('',*,*,#2942,.T.);
#3997=ORIENTED_EDGE('',*,*,#2938,.T.);
#3998=ORIENTED_EDGE('',*,*,#2943,.F.);
#3999=ORIENTED_EDGE('',*,*,#2944,.F.);
#4000=ORIENTED_EDGE('',*,*,#2945,.T.);
#4001=ORIENTED_EDGE('',*,*,#2941,.T.);
#4002=ORIENTED_EDGE('',*,*,#2946,.F.);
#4003=ORIENTED_EDGE('',*,*,#2947,.F.);
#4004=ORIENTED_EDGE('',*,*,#2948,.T.);
#4005=ORIENTED_EDGE('',*,*,#2944,.T.);
#4006=ORIENTED_EDGE('',*,*,#2949,.F.);
#4007=ORIENTED_EDGE('',*,*,#2950,.F.);
#4008=ORIENTED_EDGE('',*,*,#2951,.T.);
#4009=ORIENTED_EDGE('',*,*,#2947,.T.);
#4010=ORIENTED_EDGE('',*,*,#2952,.F.);
#4011=ORIENTED_EDGE('',*,*,#2953,.F.);
#4012=ORIENTED_EDGE('',*,*,#2954,.T.);
#4013=ORIENTED_EDGE('',*,*,#2950,.T.);
#4014=ORIENTED_EDGE('',*,*,#2955,.F.);
#4015=ORIENTED_EDGE('',*,*,#2956,.F.);
#4016=ORIENTED_EDGE('',*,*,#2957,.T.);
#4017=ORIENTED_EDGE('',*,*,#2953,.T.);
#4018=ORIENTED_EDGE('',*,*,#2958,.F.);
#4019=ORIENTED_EDGE('',*,*,#2959,.F.);
#4020=ORIENTED_EDGE('',*,*,#2960,.T.);
#4021=ORIENTED_EDGE('',*,*,#2956,.T.);
#4022=ORIENTED_EDGE('',*,*,#2961,.F.);
#4023=ORIENTED_EDGE('',*,*,#2962,.F.);
#4024=ORIENTED_EDGE('',*,*,#2963,.T.);
#4025=ORIENTED_EDGE('',*,*,#2959,.T.);
#4026=ORIENTED_EDGE('',*,*,#2964,.F.);
#4027=ORIENTED_EDGE('',*,*,#2965,.F.);
#4028=ORIENTED_EDGE('',*,*,#2966,.T.);
#4029=ORIENTED_EDGE('',*,*,#2962,.T.);
#4030=ORIENTED_EDGE('',*,*,#2967,.F.);
#4031=ORIENTED_EDGE('',*,*,#2968,.F.);
#4032=ORIENTED_EDGE('',*,*,#2969,.T.);
#4033=ORIENTED_EDGE('',*,*,#2965,.T.);
#4034=ORIENTED_EDGE('',*,*,#2970,.F.);
#4035=ORIENTED_EDGE('',*,*,#2971,.F.);
#4036=ORIENTED_EDGE('',*,*,#2972,.T.);
#4037=ORIENTED_EDGE('',*,*,#2968,.T.);
#4038=ORIENTED_EDGE('',*,*,#2973,.F.);
#4039=ORIENTED_EDGE('',*,*,#2974,.F.);
#4040=ORIENTED_EDGE('',*,*,#2975,.T.);
#4041=ORIENTED_EDGE('',*,*,#2971,.T.);
#4042=ORIENTED_EDGE('',*,*,#2976,.F.);
#4043=ORIENTED_EDGE('',*,*,#2977,.F.);
#4044=ORIENTED_EDGE('',*,*,#2978,.T.);
#4045=ORIENTED_EDGE('',*,*,#2974,.T.);
#4046=ORIENTED_EDGE('',*,*,#2979,.F.);
#4047=ORIENTED_EDGE('',*,*,#2980,.F.);
#4048=ORIENTED_EDGE('',*,*,#2981,.T.);
#4049=ORIENTED_EDGE('',*,*,#2977,.T.);
#4050=ORIENTED_EDGE('',*,*,#2982,.F.);
#4051=ORIENTED_EDGE('',*,*,#2983,.F.);
#4052=ORIENTED_EDGE('',*,*,#2984,.T.);
#4053=ORIENTED_EDGE('',*,*,#2980,.T.);
#4054=ORIENTED_EDGE('',*,*,#2985,.F.);
#4055=ORIENTED_EDGE('',*,*,#2986,.F.);
#4056=ORIENTED_EDGE('',*,*,#2987,.T.);
#4057=ORIENTED_EDGE('',*,*,#2983,.T.);
#4058=ORIENTED_EDGE('',*,*,#2988,.F.);
#4059=ORIENTED_EDGE('',*,*,#2989,.F.);
#4060=ORIENTED_EDGE('',*,*,#2990,.T.);
#4061=ORIENTED_EDGE('',*,*,#2986,.T.);
#4062=ORIENTED_EDGE('',*,*,#2991,.F.);
#4063=ORIENTED_EDGE('',*,*,#2992,.F.);
#4064=ORIENTED_EDGE('',*,*,#2993,.T.);
#4065=ORIENTED_EDGE('',*,*,#2989,.T.);
#4066=ORIENTED_EDGE('',*,*,#2994,.F.);
#4067=ORIENTED_EDGE('',*,*,#2995,.F.);
#4068=ORIENTED_EDGE('',*,*,#2996,.T.);
#4069=ORIENTED_EDGE('',*,*,#2992,.T.);
#4070=ORIENTED_EDGE('',*,*,#2997,.F.);
#4071=ORIENTED_EDGE('',*,*,#2998,.F.);
#4072=ORIENTED_EDGE('',*,*,#2999,.T.);
#4073=ORIENTED_EDGE('',*,*,#2995,.T.);
#4074=ORIENTED_EDGE('',*,*,#3000,.F.);
#4075=ORIENTED_EDGE('',*,*,#3001,.F.);
#4076=ORIENTED_EDGE('',*,*,#3002,.T.);
#4077=ORIENTED_EDGE('',*,*,#2998,.T.);
#4078=ORIENTED_EDGE('',*,*,#3003,.F.);
#4079=ORIENTED_EDGE('',*,*,#3004,.F.);
#4080=ORIENTED_EDGE('',*,*,#3005,.T.);
#4081=ORIENTED_EDGE('',*,*,#3001,.T.);
#4082=ORIENTED_EDGE('',*,*,#3006,.F.);
#4083=ORIENTED_EDGE('',*,*,#3007,.F.);
#4084=ORIENTED_EDGE('',*,*,#3008,.T.);
#4085=ORIENTED_EDGE('',*,*,#3004,.T.);
#4086=ORIENTED_EDGE('',*,*,#3009,.F.);
#4087=ORIENTED_EDGE('',*,*,#3010,.F.);
#4088=ORIENTED_EDGE('',*,*,#3011,.T.);
#4089=ORIENTED_EDGE('',*,*,#3007,.T.);
#4090=ORIENTED_EDGE('',*,*,#3012,.F.);
#4091=ORIENTED_EDGE('',*,*,#3013,.F.);
#4092=ORIENTED_EDGE('',*,*,#3014,.F.);
#4093=ORIENTED_EDGE('',*,*,#2909,.F.);
#4094=ORIENTED_EDGE('',*,*,#2905,.F.);
#4095=ORIENTED_EDGE('',*,*,#2902,.F.);
#4096=ORIENTED_EDGE('',*,*,#2899,.F.);
#4097=ORIENTED_EDGE('',*,*,#2896,.F.);
#4098=ORIENTED_EDGE('',*,*,#2893,.F.);
#4099=ORIENTED_EDGE('',*,*,#2890,.F.);
#4100=ORIENTED_EDGE('',*,*,#2887,.F.);
#4101=ORIENTED_EDGE('',*,*,#2884,.F.);
#4102=ORIENTED_EDGE('',*,*,#2881,.F.);
#4103=ORIENTED_EDGE('',*,*,#2878,.F.);
#4104=ORIENTED_EDGE('',*,*,#2875,.F.);
#4105=ORIENTED_EDGE('',*,*,#2872,.F.);
#4106=ORIENTED_EDGE('',*,*,#2869,.F.);
#4107=ORIENTED_EDGE('',*,*,#2866,.F.);
#4108=ORIENTED_EDGE('',*,*,#2863,.F.);
#4109=ORIENTED_EDGE('',*,*,#2860,.F.);
#4110=ORIENTED_EDGE('',*,*,#2857,.F.);
#4111=ORIENTED_EDGE('',*,*,#2854,.F.);
#4112=ORIENTED_EDGE('',*,*,#2851,.F.);
#4113=ORIENTED_EDGE('',*,*,#2848,.F.);
#4114=ORIENTED_EDGE('',*,*,#2845,.F.);
#4115=ORIENTED_EDGE('',*,*,#2842,.F.);
#4116=ORIENTED_EDGE('',*,*,#2839,.F.);
#4117=ORIENTED_EDGE('',*,*,#2836,.F.);
#4118=ORIENTED_EDGE('',*,*,#2833,.F.);
#4119=ORIENTED_EDGE('',*,*,#2830,.F.);
#4120=ORIENTED_EDGE('',*,*,#2827,.F.);
#4121=ORIENTED_EDGE('',*,*,#2824,.F.);
#4122=ORIENTED_EDGE('',*,*,#2821,.F.);
#4123=ORIENTED_EDGE('',*,*,#2818,.F.);
#4124=ORIENTED_EDGE('',*,*,#2815,.F.);
#4125=ORIENTED_EDGE('',*,*,#2812,.F.);
#4126=ORIENTED_EDGE('',*,*,#2809,.F.);
#4127=ORIENTED_EDGE('',*,*,#2806,.F.);
#4128=ORIENTED_EDGE('',*,*,#3015,.F.);
#4129=ORIENTED_EDGE('',*,*,#3016,.T.);
#4130=ORIENTED_EDGE('',*,*,#3012,.T.);
#4131=ORIENTED_EDGE('',*,*,#3009,.T.);
#4132=ORIENTED_EDGE('',*,*,#3006,.T.);
#4133=ORIENTED_EDGE('',*,*,#3003,.T.);
#4134=ORIENTED_EDGE('',*,*,#3000,.T.);
#4135=ORIENTED_EDGE('',*,*,#2997,.T.);
#4136=ORIENTED_EDGE('',*,*,#2994,.T.);
#4137=ORIENTED_EDGE('',*,*,#2991,.T.);
#4138=ORIENTED_EDGE('',*,*,#2988,.T.);
#4139=ORIENTED_EDGE('',*,*,#2985,.T.);
#4140=ORIENTED_EDGE('',*,*,#2982,.T.);
#4141=ORIENTED_EDGE('',*,*,#2979,.T.);
#4142=ORIENTED_EDGE('',*,*,#2976,.T.);
#4143=ORIENTED_EDGE('',*,*,#2973,.T.);
#4144=ORIENTED_EDGE('',*,*,#2970,.T.);
#4145=ORIENTED_EDGE('',*,*,#2967,.T.);
#4146=ORIENTED_EDGE('',*,*,#2964,.T.);
#4147=ORIENTED_EDGE('',*,*,#2961,.T.);
#4148=ORIENTED_EDGE('',*,*,#2958,.T.);
#4149=ORIENTED_EDGE('',*,*,#2955,.T.);
#4150=ORIENTED_EDGE('',*,*,#2952,.T.);
#4151=ORIENTED_EDGE('',*,*,#2949,.T.);
#4152=ORIENTED_EDGE('',*,*,#2946,.T.);
#4153=ORIENTED_EDGE('',*,*,#2943,.T.);
#4154=ORIENTED_EDGE('',*,*,#2940,.T.);
#4155=ORIENTED_EDGE('',*,*,#2937,.T.);
#4156=ORIENTED_EDGE('',*,*,#2934,.T.);
#4157=ORIENTED_EDGE('',*,*,#2931,.T.);
#4158=ORIENTED_EDGE('',*,*,#2928,.T.);
#4159=ORIENTED_EDGE('',*,*,#2925,.T.);
#4160=ORIENTED_EDGE('',*,*,#2922,.T.);
#4161=ORIENTED_EDGE('',*,*,#2919,.T.);
#4162=ORIENTED_EDGE('',*,*,#2916,.T.);
#4163=ORIENTED_EDGE('',*,*,#2913,.T.);
#4164=ORIENTED_EDGE('',*,*,#3010,.T.);
#4165=ORIENTED_EDGE('',*,*,#3016,.F.);
#4166=ORIENTED_EDGE('',*,*,#3017,.F.);
#4167=ORIENTED_EDGE('',*,*,#3018,.T.);
#4168=ORIENTED_EDGE('',*,*,#3019,.F.);
#4169=ORIENTED_EDGE('',*,*,#2911,.F.);
#4170=ORIENTED_EDGE('',*,*,#2915,.F.);
#4171=ORIENTED_EDGE('',*,*,#2918,.F.);
#4172=ORIENTED_EDGE('',*,*,#2921,.F.);
#4173=ORIENTED_EDGE('',*,*,#2924,.F.);
#4174=ORIENTED_EDGE('',*,*,#2927,.F.);
#4175=ORIENTED_EDGE('',*,*,#2930,.F.);
#4176=ORIENTED_EDGE('',*,*,#2933,.F.);
#4177=ORIENTED_EDGE('',*,*,#2936,.F.);
#4178=ORIENTED_EDGE('',*,*,#2939,.F.);
#4179=ORIENTED_EDGE('',*,*,#2942,.F.);
#4180=ORIENTED_EDGE('',*,*,#2945,.F.);
#4181=ORIENTED_EDGE('',*,*,#2948,.F.);
#4182=ORIENTED_EDGE('',*,*,#2951,.F.);
#4183=ORIENTED_EDGE('',*,*,#2954,.F.);
#4184=ORIENTED_EDGE('',*,*,#2957,.F.);
#4185=ORIENTED_EDGE('',*,*,#2960,.F.);
#4186=ORIENTED_EDGE('',*,*,#2963,.F.);
#4187=ORIENTED_EDGE('',*,*,#2966,.F.);
#4188=ORIENTED_EDGE('',*,*,#2969,.F.);
#4189=ORIENTED_EDGE('',*,*,#2972,.F.);
#4190=ORIENTED_EDGE('',*,*,#2975,.F.);
#4191=ORIENTED_EDGE('',*,*,#2978,.F.);
#4192=ORIENTED_EDGE('',*,*,#2981,.F.);
#4193=ORIENTED_EDGE('',*,*,#2984,.F.);
#4194=ORIENTED_EDGE('',*,*,#2987,.F.);
#4195=ORIENTED_EDGE('',*,*,#2990,.F.);
#4196=ORIENTED_EDGE('',*,*,#2993,.F.);
#4197=ORIENTED_EDGE('',*,*,#2996,.F.);
#4198=ORIENTED_EDGE('',*,*,#2999,.F.);
#4199=ORIENTED_EDGE('',*,*,#3002,.F.);
#4200=ORIENTED_EDGE('',*,*,#3005,.F.);
#4201=ORIENTED_EDGE('',*,*,#3008,.F.);
#4202=ORIENTED_EDGE('',*,*,#3011,.F.);
#4203=ORIENTED_EDGE('',*,*,#3018,.F.);
#4204=ORIENTED_EDGE('',*,*,#3020,.F.);
#4205=ORIENTED_EDGE('',*,*,#2804,.F.);
#4206=ORIENTED_EDGE('',*,*,#2808,.F.);
#4207=ORIENTED_EDGE('',*,*,#2811,.F.);
#4208=ORIENTED_EDGE('',*,*,#2814,.F.);
#4209=ORIENTED_EDGE('',*,*,#2817,.F.);
#4210=ORIENTED_EDGE('',*,*,#2820,.F.);
#4211=ORIENTED_EDGE('',*,*,#2823,.F.);
#4212=ORIENTED_EDGE('',*,*,#2826,.F.);
#4213=ORIENTED_EDGE('',*,*,#2829,.F.);
#4214=ORIENTED_EDGE('',*,*,#2832,.F.);
#4215=ORIENTED_EDGE('',*,*,#2835,.F.);
#4216=ORIENTED_EDGE('',*,*,#2838,.F.);
#4217=ORIENTED_EDGE('',*,*,#2841,.F.);
#4218=ORIENTED_EDGE('',*,*,#2844,.F.);
#4219=ORIENTED_EDGE('',*,*,#2847,.F.);
#4220=ORIENTED_EDGE('',*,*,#2850,.F.);
#4221=ORIENTED_EDGE('',*,*,#2853,.F.);
#4222=ORIENTED_EDGE('',*,*,#2856,.F.);
#4223=ORIENTED_EDGE('',*,*,#2859,.F.);
#4224=ORIENTED_EDGE('',*,*,#2862,.F.);
#4225=ORIENTED_EDGE('',*,*,#2865,.F.);
#4226=ORIENTED_EDGE('',*,*,#2868,.F.);
#4227=ORIENTED_EDGE('',*,*,#2871,.F.);
#4228=ORIENTED_EDGE('',*,*,#2874,.F.);
#4229=ORIENTED_EDGE('',*,*,#2877,.F.);
#4230=ORIENTED_EDGE('',*,*,#2880,.F.);
#4231=ORIENTED_EDGE('',*,*,#2883,.F.);
#4232=ORIENTED_EDGE('',*,*,#2886,.F.);
#4233=ORIENTED_EDGE('',*,*,#2889,.F.);
#4234=ORIENTED_EDGE('',*,*,#2892,.F.);
#4235=ORIENTED_EDGE('',*,*,#2895,.F.);
#4236=ORIENTED_EDGE('',*,*,#2898,.F.);
#4237=ORIENTED_EDGE('',*,*,#2901,.F.);
#4238=ORIENTED_EDGE('',*,*,#2904,.F.);
#4239=ORIENTED_EDGE('',*,*,#2908,.F.);
#4240=ORIENTED_EDGE('',*,*,#2906,.T.);
#4241=ORIENTED_EDGE('',*,*,#3014,.T.);
#4242=ORIENTED_EDGE('',*,*,#3021,.F.);
#4243=ORIENTED_EDGE('',*,*,#3022,.F.);
#4244=ORIENTED_EDGE('',*,*,#3023,.T.);
#4245=ORIENTED_EDGE('',*,*,#3024,.T.);
#4246=ORIENTED_EDGE('',*,*,#3025,.F.);
#4247=ORIENTED_EDGE('',*,*,#3026,.F.);
#4248=ORIENTED_EDGE('',*,*,#3027,.T.);
#4249=ORIENTED_EDGE('',*,*,#3028,.T.);
#4250=ORIENTED_EDGE('',*,*,#3023,.F.);
#4251=ORIENTED_EDGE('',*,*,#3029,.F.);
#4252=ORIENTED_EDGE('',*,*,#3030,.T.);
#4253=ORIENTED_EDGE('',*,*,#3031,.T.);
#4254=ORIENTED_EDGE('',*,*,#3027,.F.);
#4255=ORIENTED_EDGE('',*,*,#3032,.F.);
#4256=ORIENTED_EDGE('',*,*,#3033,.T.);
#4257=ORIENTED_EDGE('',*,*,#3034,.T.);
#4258=ORIENTED_EDGE('',*,*,#3030,.F.);
#4259=ORIENTED_EDGE('',*,*,#3035,.F.);
#4260=ORIENTED_EDGE('',*,*,#3036,.T.);
#4261=ORIENTED_EDGE('',*,*,#3037,.T.);
#4262=ORIENTED_EDGE('',*,*,#3033,.F.);
#4263=ORIENTED_EDGE('',*,*,#3038,.F.);
#4264=ORIENTED_EDGE('',*,*,#3025,.T.);
#4265=ORIENTED_EDGE('',*,*,#3039,.T.);
#4266=ORIENTED_EDGE('',*,*,#3036,.F.);
#4267=ORIENTED_EDGE('',*,*,#3039,.F.);
#4268=ORIENTED_EDGE('',*,*,#3024,.F.);
#4269=ORIENTED_EDGE('',*,*,#3028,.F.);
#4270=ORIENTED_EDGE('',*,*,#3031,.F.);
#4271=ORIENTED_EDGE('',*,*,#3034,.F.);
#4272=ORIENTED_EDGE('',*,*,#3037,.F.);
#4273=ORIENTED_EDGE('',*,*,#3040,.T.);
#4274=ORIENTED_EDGE('',*,*,#3020,.T.);
#4275=ORIENTED_EDGE('',*,*,#3017,.T.);
#4276=ORIENTED_EDGE('',*,*,#3015,.T.);
#4277=ORIENTED_EDGE('',*,*,#2805,.F.);
#4278=ORIENTED_EDGE('',*,*,#3040,.F.);
#4279=ORIENTED_EDGE('',*,*,#3041,.T.);
#4280=ORIENTED_EDGE('',*,*,#3042,.T.);
#4281=ORIENTED_EDGE('',*,*,#3041,.F.);
#4282=ORIENTED_EDGE('',*,*,#3042,.F.);
#4283=ORIENTED_EDGE('',*,*,#3022,.T.);
#4284=ORIENTED_EDGE('',*,*,#3038,.T.);
#4285=ORIENTED_EDGE('',*,*,#3035,.T.);
#4286=ORIENTED_EDGE('',*,*,#3032,.T.);
#4287=ORIENTED_EDGE('',*,*,#3029,.T.);
#4288=ORIENTED_EDGE('',*,*,#3026,.T.);
#4289=ORIENTED_EDGE('',*,*,#3019,.T.);
#4290=ORIENTED_EDGE('',*,*,#2907,.T.);
#4291=ORIENTED_EDGE('',*,*,#3021,.T.);
#4292=ORIENTED_EDGE('',*,*,#3013,.T.);
#4293=ORIENTED_EDGE('',*,*,#2912,.T.);
#4466=CYLINDRICAL_SURFACE('',#5178,0.1954);
#4467=CYLINDRICAL_SURFACE('',#5180,0.1954);
#4468=CYLINDRICAL_SURFACE('',#5181,0.1954);
#4469=CYLINDRICAL_SURFACE('',#5182,0.1954);
#4470=CYLINDRICAL_SURFACE('',#5183,0.1954);
#4471=CYLINDRICAL_SURFACE('',#5184,0.1954);
#4472=CYLINDRICAL_SURFACE('',#5185,0.1954);
#4473=CYLINDRICAL_SURFACE('',#5186,0.1954);
#4474=CYLINDRICAL_SURFACE('',#5187,0.1954);
#4475=CYLINDRICAL_SURFACE('',#5188,0.1954);
#4476=CYLINDRICAL_SURFACE('',#5189,0.1954);
#4477=CYLINDRICAL_SURFACE('',#5190,0.1954);
#4478=CYLINDRICAL_SURFACE('',#5191,0.1954);
#4479=CYLINDRICAL_SURFACE('',#5192,0.1954);
#4480=CYLINDRICAL_SURFACE('',#5193,0.1954);
#4481=CYLINDRICAL_SURFACE('',#5194,0.1954);
#4482=CYLINDRICAL_SURFACE('',#5195,0.1954);
#4483=CYLINDRICAL_SURFACE('',#5196,0.1954);
#4484=CYLINDRICAL_SURFACE('',#5197,0.1954);
#4485=CYLINDRICAL_SURFACE('',#5198,0.1954);
#4486=CYLINDRICAL_SURFACE('',#5199,0.1954);
#4487=CYLINDRICAL_SURFACE('',#5200,0.1954);
#4488=CYLINDRICAL_SURFACE('',#5201,0.1954);
#4489=CYLINDRICAL_SURFACE('',#5202,0.1954);
#4490=CYLINDRICAL_SURFACE('',#5203,0.1954);
#4491=CYLINDRICAL_SURFACE('',#5204,0.1954);
#4492=CYLINDRICAL_SURFACE('',#5205,0.1954);
#4493=CYLINDRICAL_SURFACE('',#5206,0.1954);
#4494=CYLINDRICAL_SURFACE('',#5207,0.1954);
#4495=CYLINDRICAL_SURFACE('',#5208,0.1954);
#4496=CYLINDRICAL_SURFACE('',#5209,0.1954);
#4497=CYLINDRICAL_SURFACE('',#5210,0.1954);
#4498=CYLINDRICAL_SURFACE('',#5211,0.1954);
#4499=CYLINDRICAL_SURFACE('',#5212,0.1954);
#4500=CYLINDRICAL_SURFACE('',#5213,0.1954);
#4501=CYLINDRICAL_SURFACE('',#5215,0.15555);
#4502=CYLINDRICAL_SURFACE('',#5217,0.15555);
#4503=CYLINDRICAL_SURFACE('',#5218,0.15555);
#4504=CYLINDRICAL_SURFACE('',#5219,0.15555);
#4505=CYLINDRICAL_SURFACE('',#5220,0.15555);
#4506=CYLINDRICAL_SURFACE('',#5221,0.15555);
#4507=CYLINDRICAL_SURFACE('',#5222,0.15555);
#4508=CYLINDRICAL_SURFACE('',#5223,0.15555);
#4509=CYLINDRICAL_SURFACE('',#5224,0.15555);
#4510=CYLINDRICAL_SURFACE('',#5225,0.15555);
#4511=CYLINDRICAL_SURFACE('',#5226,0.15555);
#4512=CYLINDRICAL_SURFACE('',#5227,0.15555);
#4513=CYLINDRICAL_SURFACE('',#5228,0.15555);
#4514=CYLINDRICAL_SURFACE('',#5229,0.15555);
#4515=CYLINDRICAL_SURFACE('',#5230,0.15555);
#4516=CYLINDRICAL_SURFACE('',#5231,0.15555);
#4517=CYLINDRICAL_SURFACE('',#5232,0.15555);
#4518=CYLINDRICAL_SURFACE('',#5233,0.15555);
#4519=CYLINDRICAL_SURFACE('',#5234,0.15555);
#4520=CYLINDRICAL_SURFACE('',#5235,0.15555);
#4521=CYLINDRICAL_SURFACE('',#5236,0.15555);
#4522=CYLINDRICAL_SURFACE('',#5237,0.15555);
#4523=CYLINDRICAL_SURFACE('',#5238,0.15555);
#4524=CYLINDRICAL_SURFACE('',#5239,0.15555);
#4525=CYLINDRICAL_SURFACE('',#5240,0.15555);
#4526=CYLINDRICAL_SURFACE('',#5241,0.15555);
#4527=CYLINDRICAL_SURFACE('',#5242,0.15555);
#4528=CYLINDRICAL_SURFACE('',#5243,0.15555);
#4529=CYLINDRICAL_SURFACE('',#5244,0.15555);
#4530=CYLINDRICAL_SURFACE('',#5245,0.15555);
#4531=CYLINDRICAL_SURFACE('',#5246,0.15555);
#4532=CYLINDRICAL_SURFACE('',#5247,0.15555);
#4533=CYLINDRICAL_SURFACE('',#5248,0.15555);
#4534=CYLINDRICAL_SURFACE('',#5249,0.15555);
#4535=CYLINDRICAL_SURFACE('',#5250,0.15555);
#4536=CYLINDRICAL_SURFACE('',#5252,0.1954);
#4537=CYLINDRICAL_SURFACE('',#5263,0.4);
#4698=ADVANCED_FACE('',(#717),#4466,.T.);
#4699=ADVANCED_FACE('',(#718),#4467,.T.);
#4700=ADVANCED_FACE('',(#719),#4468,.T.);
#4701=ADVANCED_FACE('',(#720),#4469,.T.);
#4702=ADVANCED_FACE('',(#721),#4470,.T.);
#4703=ADVANCED_FACE('',(#722),#4471,.T.);
#4704=ADVANCED_FACE('',(#723),#4472,.T.);
#4705=ADVANCED_FACE('',(#724),#4473,.T.);
#4706=ADVANCED_FACE('',(#725),#4474,.T.);
#4707=ADVANCED_FACE('',(#726),#4475,.T.);
#4708=ADVANCED_FACE('',(#727),#4476,.T.);
#4709=ADVANCED_FACE('',(#728),#4477,.T.);
#4710=ADVANCED_FACE('',(#729),#4478,.T.);
#4711=ADVANCED_FACE('',(#730),#4479,.T.);
#4712=ADVANCED_FACE('',(#731),#4480,.T.);
#4713=ADVANCED_FACE('',(#732),#4481,.T.);
#4714=ADVANCED_FACE('',(#733),#4482,.T.);
#4715=ADVANCED_FACE('',(#734),#4483,.T.);
#4716=ADVANCED_FACE('',(#735),#4484,.T.);
#4717=ADVANCED_FACE('',(#736),#4485,.T.);
#4718=ADVANCED_FACE('',(#737),#4486,.T.);
#4719=ADVANCED_FACE('',(#738),#4487,.T.);
#4720=ADVANCED_FACE('',(#739),#4488,.T.);
#4721=ADVANCED_FACE('',(#740),#4489,.T.);
#4722=ADVANCED_FACE('',(#741),#4490,.T.);
#4723=ADVANCED_FACE('',(#742),#4491,.T.);
#4724=ADVANCED_FACE('',(#743),#4492,.T.);
#4725=ADVANCED_FACE('',(#744),#4493,.T.);
#4726=ADVANCED_FACE('',(#745),#4494,.T.);
#4727=ADVANCED_FACE('',(#746),#4495,.T.);
#4728=ADVANCED_FACE('',(#747),#4496,.T.);
#4729=ADVANCED_FACE('',(#748),#4497,.T.);
#4730=ADVANCED_FACE('',(#749),#4498,.T.);
#4731=ADVANCED_FACE('',(#750),#4499,.T.);
#4732=ADVANCED_FACE('',(#751),#4500,.T.);
#4733=ADVANCED_FACE('',(#752),#4501,.T.);
#4734=ADVANCED_FACE('',(#753),#4502,.T.);
#4735=ADVANCED_FACE('',(#754),#4503,.T.);
#4736=ADVANCED_FACE('',(#755),#4504,.T.);
#4737=ADVANCED_FACE('',(#756),#4505,.T.);
#4738=ADVANCED_FACE('',(#757),#4506,.T.);
#4739=ADVANCED_FACE('',(#758),#4507,.T.);
#4740=ADVANCED_FACE('',(#759),#4508,.T.);
#4741=ADVANCED_FACE('',(#760),#4509,.T.);
#4742=ADVANCED_FACE('',(#761),#4510,.T.);
#4743=ADVANCED_FACE('',(#762),#4511,.T.);
#4744=ADVANCED_FACE('',(#763),#4512,.T.);
#4745=ADVANCED_FACE('',(#764),#4513,.T.);
#4746=ADVANCED_FACE('',(#765),#4514,.T.);
#4747=ADVANCED_FACE('',(#766),#4515,.T.);
#4748=ADVANCED_FACE('',(#767),#4516,.T.);
#4749=ADVANCED_FACE('',(#768),#4517,.T.);
#4750=ADVANCED_FACE('',(#769),#4518,.T.);
#4751=ADVANCED_FACE('',(#770),#4519,.T.);
#4752=ADVANCED_FACE('',(#771),#4520,.T.);
#4753=ADVANCED_FACE('',(#772),#4521,.T.);
#4754=ADVANCED_FACE('',(#773),#4522,.T.);
#4755=ADVANCED_FACE('',(#774),#4523,.T.);
#4756=ADVANCED_FACE('',(#775),#4524,.T.);
#4757=ADVANCED_FACE('',(#776),#4525,.T.);
#4758=ADVANCED_FACE('',(#777),#4526,.T.);
#4759=ADVANCED_FACE('',(#778),#4527,.T.);
#4760=ADVANCED_FACE('',(#779),#4528,.T.);
#4761=ADVANCED_FACE('',(#780),#4529,.T.);
#4762=ADVANCED_FACE('',(#781),#4530,.T.);
#4763=ADVANCED_FACE('',(#782),#4531,.T.);
#4764=ADVANCED_FACE('',(#783),#4532,.T.);
#4765=ADVANCED_FACE('',(#784),#4533,.T.);
#4766=ADVANCED_FACE('',(#785),#4534,.T.);
#4767=ADVANCED_FACE('',(#786),#171,.F.);
#4768=ADVANCED_FACE('',(#787),#4535,.T.);
#4769=ADVANCED_FACE('',(#788),#172,.F.);
#4770=ADVANCED_FACE('',(#789),#4536,.T.);
#4771=ADVANCED_FACE('',(#790),#552,.F.);
#4772=ADVANCED_FACE('',(#791),#553,.F.);
#4773=ADVANCED_FACE('',(#792),#554,.F.);
#4774=ADVANCED_FACE('',(#793),#555,.F.);
#4775=ADVANCED_FACE('',(#794),#556,.F.);
#4776=ADVANCED_FACE('',(#795),#557,.F.);
#4777=ADVANCED_FACE('',(#796),#558,.F.);
#4778=ADVANCED_FACE('',(#797,#437),#559,.T.);
#4779=ADVANCED_FACE('',(#798),#4537,.T.);
#4780=ADVANCED_FACE('',(#799,#438),#560,.F.);
#4781=ADVANCED_FACE('',(#800),#561,.T.);
#4818=CLOSED_SHELL('',(#4698,#4699,#4700,#4701,#4702,#4703,#4704,#4705,
#4706,#4707,#4708,#4709,#4710,#4711,#4712,#4713,#4714,#4715,#4716,#4717,
#4718,#4719,#4720,#4721,#4722,#4723,#4724,#4725,#4726,#4727,#4728,#4729,
#4730,#4731,#4732,#4733,#4734,#4735,#4736,#4737,#4738,#4739,#4740,#4741,
#4742,#4743,#4744,#4745,#4746,#4747,#4748,#4749,#4750,#4751,#4752,#4753,
#4754,#4755,#4756,#4757,#4758,#4759,#4760,#4761,#4762,#4763,#4764,#4765,
#4766,#4767,#4768,#4769,#4770,#4771,#4772,#4773,#4774,#4775,#4776,#4777,
#4778,#4779,#4780,#4781));
#5177=AXIS2_PLACEMENT_3D('',#7257,#6070,#6071);
#5178=AXIS2_PLACEMENT_3D('',#7258,#6072,#6073);
#5179=AXIS2_PLACEMENT_3D('',#7274,#6075,#6076);
#5180=AXIS2_PLACEMENT_3D('',#7282,#6077,#6078);
#5181=AXIS2_PLACEMENT_3D('',#7330,#6080,#6081);
#5182=AXIS2_PLACEMENT_3D('',#7378,#6083,#6084);
#5183=AXIS2_PLACEMENT_3D('',#7429,#6086,#6087);
#5184=AXIS2_PLACEMENT_3D('',#7477,#6089,#6090);
#5185=AXIS2_PLACEMENT_3D('',#7525,#6092,#6093);
#5186=AXIS2_PLACEMENT_3D('',#7573,#6095,#6096);
#5187=AXIS2_PLACEMENT_3D('',#7627,#6098,#6099);
#5188=AXIS2_PLACEMENT_3D('',#7675,#6101,#6102);
#5189=AXIS2_PLACEMENT_3D('',#7723,#6104,#6105);
#5190=AXIS2_PLACEMENT_3D('',#7777,#6107,#6108);
#5191=AXIS2_PLACEMENT_3D('',#7825,#6110,#6111);
#5192=AXIS2_PLACEMENT_3D('',#7873,#6113,#6114);
#5193=AXIS2_PLACEMENT_3D('',#7921,#6116,#6117);
#5194=AXIS2_PLACEMENT_3D('',#7975,#6119,#6120);
#5195=AXIS2_PLACEMENT_3D('',#8023,#6122,#6123);
#5196=AXIS2_PLACEMENT_3D('',#8071,#6125,#6126);
#5197=AXIS2_PLACEMENT_3D('',#8125,#6128,#6129);
#5198=AXIS2_PLACEMENT_3D('',#8173,#6131,#6132);
#5199=AXIS2_PLACEMENT_3D('',#8221,#6134,#6135);
#5200=AXIS2_PLACEMENT_3D('',#8275,#6137,#6138);
#5201=AXIS2_PLACEMENT_3D('',#8323,#6140,#6141);
#5202=AXIS2_PLACEMENT_3D('',#8371,#6143,#6144);
#5203=AXIS2_PLACEMENT_3D('',#8419,#6146,#6147);
#5204=AXIS2_PLACEMENT_3D('',#8473,#6149,#6150);
#5205=AXIS2_PLACEMENT_3D('',#8521,#6152,#6153);
#5206=AXIS2_PLACEMENT_3D('',#8569,#6155,#6156);
#5207=AXIS2_PLACEMENT_3D('',#8623,#6158,#6159);
#5208=AXIS2_PLACEMENT_3D('',#8671,#6161,#6162);
#5209=AXIS2_PLACEMENT_3D('',#8719,#6164,#6165);
#5210=AXIS2_PLACEMENT_3D('',#8773,#6167,#6168);
#5211=AXIS2_PLACEMENT_3D('',#8821,#6170,#6171);
#5212=AXIS2_PLACEMENT_3D('',#8869,#6173,#6174);
#5213=AXIS2_PLACEMENT_3D('',#8917,#6176,#6177);
#5214=AXIS2_PLACEMENT_3D('',#8922,#6179,#6180);
#5215=AXIS2_PLACEMENT_3D('',#8970,#6181,#6182);
#5216=AXIS2_PLACEMENT_3D('',#8984,#6184,#6185);
#5217=AXIS2_PLACEMENT_3D('',#8991,#6186,#6187);
#5218=AXIS2_PLACEMENT_3D('',#9016,#6189,#6190);
#5219=AXIS2_PLACEMENT_3D('',#9040,#6192,#6193);
#5220=AXIS2_PLACEMENT_3D('',#9064,#6195,#6196);
#5221=AXIS2_PLACEMENT_3D('',#9089,#6198,#6199);
#5222=AXIS2_PLACEMENT_3D('',#9114,#6201,#6202);
#5223=AXIS2_PLACEMENT_3D('',#9138,#6204,#6205);
#5224=AXIS2_PLACEMENT_3D('',#9163,#6207,#6208);
#5225=AXIS2_PLACEMENT_3D('',#9188,#6210,#6211);
#5226=AXIS2_PLACEMENT_3D('',#9212,#6213,#6214);
#5227=AXIS2_PLACEMENT_3D('',#9237,#6216,#6217);
#5228=AXIS2_PLACEMENT_3D('',#9262,#6219,#6220);
#5229=AXIS2_PLACEMENT_3D('',#9286,#6222,#6223);
#5230=AXIS2_PLACEMENT_3D('',#9310,#6225,#6226);
#5231=AXIS2_PLACEMENT_3D('',#9335,#6228,#6229);
#5232=AXIS2_PLACEMENT_3D('',#9360,#6231,#6232);
#5233=AXIS2_PLACEMENT_3D('',#9384,#6234,#6235);
#5234=AXIS2_PLACEMENT_3D('',#9409,#6237,#6238);
#5235=AXIS2_PLACEMENT_3D('',#9434,#6240,#6241);
#5236=AXIS2_PLACEMENT_3D('',#9458,#6243,#6244);
#5237=AXIS2_PLACEMENT_3D('',#9483,#6246,#6247);
#5238=AXIS2_PLACEMENT_3D('',#9508,#6249,#6250);
#5239=AXIS2_PLACEMENT_3D('',#9532,#6252,#6253);
#5240=AXIS2_PLACEMENT_3D('',#9556,#6255,#6256);
#5241=AXIS2_PLACEMENT_3D('',#9581,#6258,#6259);
#5242=AXIS2_PLACEMENT_3D('',#9606,#6261,#6262);
#5243=AXIS2_PLACEMENT_3D('',#9630,#6264,#6265);
#5244=AXIS2_PLACEMENT_3D('',#9655,#6267,#6268);
#5245=AXIS2_PLACEMENT_3D('',#9680,#6270,#6271);
#5246=AXIS2_PLACEMENT_3D('',#9704,#6273,#6274);
#5247=AXIS2_PLACEMENT_3D('',#9729,#6276,#6277);
#5248=AXIS2_PLACEMENT_3D('',#9753,#6279,#6280);
#5249=AXIS2_PLACEMENT_3D('',#9778,#6282,#6283);
#5250=AXIS2_PLACEMENT_3D('',#10808,#6285,#6286);
#5251=AXIS2_PLACEMENT_3D('',#10810,#6287,#6288);
#5252=AXIS2_PLACEMENT_3D('',#11813,#6289,#6290);
#5253=AXIS2_PLACEMENT_3D('',#11814,#6291,#6292);
#5254=AXIS2_PLACEMENT_3D('',#11815,#6293,#6294);
#5255=AXIS2_PLACEMENT_3D('',#11824,#6299,#6300);
#5256=AXIS2_PLACEMENT_3D('',#11830,#6304,#6305);
#5257=AXIS2_PLACEMENT_3D('',#11836,#6309,#6310);
#5258=AXIS2_PLACEMENT_3D('',#11842,#6314,#6315);
#5259=AXIS2_PLACEMENT_3D('',#11848,#6319,#6320);
#5260=AXIS2_PLACEMENT_3D('',#11851,#6323,#6324);
#5261=AXIS2_PLACEMENT_3D('',#11852,#6325,#6326);
#5262=AXIS2_PLACEMENT_3D('',#11854,#6327,#6328);
#5263=AXIS2_PLACEMENT_3D('',#11855,#6329,#6330);
#5264=AXIS2_PLACEMENT_3D('',#11858,#6332,#6333);
#5265=AXIS2_PLACEMENT_3D('',#11859,#6334,#6335);
#5266=AXIS2_PLACEMENT_3D('',#11860,#6336,#6337);
#6070=DIRECTION('axis',(0.,0.,1.));
#6071=DIRECTION('refdir',(1.,0.,0.));
#6072=DIRECTION('center_axis',(0.,0.,1.));
#6073=DIRECTION('ref_axis',(1.,0.,0.));
#6074=DIRECTION('',(0.,0.,-1.));
#6075=DIRECTION('center_axis',(0.,0.,-1.));
#6076=DIRECTION('ref_axis',(1.,0.,0.));
#6077=DIRECTION('center_axis',(0.,0.,1.));
#6078=DIRECTION('ref_axis',(1.,0.,0.));
#6079=DIRECTION('',(0.,0.,-1.));
#6080=DIRECTION('center_axis',(0.,0.,1.));
#6081=DIRECTION('ref_axis',(1.,0.,0.));
#6082=DIRECTION('',(0.,0.,-1.));
#6083=DIRECTION('center_axis',(0.,0.,1.));
#6084=DIRECTION('ref_axis',(1.,0.,0.));
#6085=DIRECTION('',(0.,0.,-1.));
#6086=DIRECTION('center_axis',(0.,0.,1.));
#6087=DIRECTION('ref_axis',(1.,0.,0.));
#6088=DIRECTION('',(0.,0.,-1.));
#6089=DIRECTION('center_axis',(0.,0.,1.));
#6090=DIRECTION('ref_axis',(1.,0.,0.));
#6091=DIRECTION('',(0.,0.,-1.));
#6092=DIRECTION('center_axis',(0.,0.,1.));
#6093=DIRECTION('ref_axis',(1.,0.,0.));
#6094=DIRECTION('',(0.,0.,-1.));
#6095=DIRECTION('center_axis',(0.,0.,1.));
#6096=DIRECTION('ref_axis',(1.,0.,0.));
#6097=DIRECTION('',(0.,0.,-1.));
#6098=DIRECTION('center_axis',(0.,0.,1.));
#6099=DIRECTION('ref_axis',(1.,0.,0.));
#6100=DIRECTION('',(0.,0.,-1.));
#6101=DIRECTION('center_axis',(0.,0.,1.));
#6102=DIRECTION('ref_axis',(1.,0.,0.));
#6103=DIRECTION('',(0.,0.,-1.));
#6104=DIRECTION('center_axis',(0.,0.,1.));
#6105=DIRECTION('ref_axis',(1.,0.,0.));
#6106=DIRECTION('',(0.,0.,-1.));
#6107=DIRECTION('center_axis',(0.,0.,1.));
#6108=DIRECTION('ref_axis',(1.,0.,0.));
#6109=DIRECTION('',(0.,0.,-1.));
#6110=DIRECTION('center_axis',(0.,0.,1.));
#6111=DIRECTION('ref_axis',(1.,0.,0.));
#6112=DIRECTION('',(0.,0.,-1.));
#6113=DIRECTION('center_axis',(0.,0.,1.));
#6114=DIRECTION('ref_axis',(1.,0.,0.));
#6115=DIRECTION('',(0.,0.,-1.));
#6116=DIRECTION('center_axis',(0.,0.,1.));
#6117=DIRECTION('ref_axis',(1.,0.,0.));
#6118=DIRECTION('',(0.,0.,-1.));
#6119=DIRECTION('center_axis',(0.,0.,1.));
#6120=DIRECTION('ref_axis',(1.,0.,0.));
#6121=DIRECTION('',(0.,0.,-1.));
#6122=DIRECTION('center_axis',(0.,0.,1.));
#6123=DIRECTION('ref_axis',(1.,0.,0.));
#6124=DIRECTION('',(0.,0.,-1.));
#6125=DIRECTION('center_axis',(0.,0.,1.));
#6126=DIRECTION('ref_axis',(1.,0.,0.));
#6127=DIRECTION('',(0.,0.,-1.));
#6128=DIRECTION('center_axis',(0.,0.,1.));
#6129=DIRECTION('ref_axis',(1.,0.,0.));
#6130=DIRECTION('',(0.,0.,-1.));
#6131=DIRECTION('center_axis',(0.,0.,1.));
#6132=DIRECTION('ref_axis',(1.,0.,0.));
#6133=DIRECTION('',(0.,0.,-1.));
#6134=DIRECTION('center_axis',(0.,0.,1.));
#6135=DIRECTION('ref_axis',(1.,0.,0.));
#6136=DIRECTION('',(0.,0.,-1.));
#6137=DIRECTION('center_axis',(0.,0.,1.));
#6138=DIRECTION('ref_axis',(1.,0.,0.));
#6139=DIRECTION('',(0.,0.,-1.));
#6140=DIRECTION('center_axis',(0.,0.,1.));
#6141=DIRECTION('ref_axis',(1.,0.,0.));
#6142=DIRECTION('',(0.,0.,-1.));
#6143=DIRECTION('center_axis',(0.,0.,1.));
#6144=DIRECTION('ref_axis',(1.,0.,0.));
#6145=DIRECTION('',(0.,0.,-1.));
#6146=DIRECTION('center_axis',(0.,0.,1.));
#6147=DIRECTION('ref_axis',(1.,0.,0.));
#6148=DIRECTION('',(0.,0.,-1.));
#6149=DIRECTION('center_axis',(0.,0.,1.));
#6150=DIRECTION('ref_axis',(1.,0.,0.));
#6151=DIRECTION('',(0.,0.,-1.));
#6152=DIRECTION('center_axis',(0.,0.,1.));
#6153=DIRECTION('ref_axis',(1.,0.,0.));
#6154=DIRECTION('',(0.,0.,-1.));
#6155=DIRECTION('center_axis',(0.,0.,1.));
#6156=DIRECTION('ref_axis',(1.,0.,0.));
#6157=DIRECTION('',(0.,0.,-1.));
#6158=DIRECTION('center_axis',(0.,0.,1.));
#6159=DIRECTION('ref_axis',(1.,0.,0.));
#6160=DIRECTION('',(0.,0.,-1.));
#6161=DIRECTION('center_axis',(0.,0.,1.));
#6162=DIRECTION('ref_axis',(1.,0.,0.));
#6163=DIRECTION('',(0.,0.,-1.));
#6164=DIRECTION('center_axis',(0.,0.,1.));
#6165=DIRECTION('ref_axis',(1.,0.,0.));
#6166=DIRECTION('',(0.,0.,-1.));
#6167=DIRECTION('center_axis',(0.,0.,1.));
#6168=DIRECTION('ref_axis',(1.,0.,0.));
#6169=DIRECTION('',(0.,0.,-1.));
#6170=DIRECTION('center_axis',(0.,0.,1.));
#6171=DIRECTION('ref_axis',(1.,0.,0.));
#6172=DIRECTION('',(0.,0.,-1.));
#6173=DIRECTION('center_axis',(0.,0.,1.));
#6174=DIRECTION('ref_axis',(1.,0.,0.));
#6175=DIRECTION('',(0.,0.,-1.));
#6176=DIRECTION('center_axis',(0.,0.,1.));
#6177=DIRECTION('ref_axis',(1.,0.,0.));
#6178=DIRECTION('',(0.,0.,-1.));
#6179=DIRECTION('center_axis',(0.,0.,-1.));
#6180=DIRECTION('ref_axis',(1.,0.,0.));
#6181=DIRECTION('center_axis',(0.,0.,1.));
#6182=DIRECTION('ref_axis',(0.409441503265782,-0.912336371851663,0.));
#6183=DIRECTION('',(0.,0.,1.));
#6184=DIRECTION('center_axis',(0.,0.,1.));
#6185=DIRECTION('ref_axis',(1.,-2.80853466614331E-13,0.));
#6186=DIRECTION('center_axis',(0.,0.,1.));
#6187=DIRECTION('ref_axis',(1.,-2.80853466614331E-13,0.));
#6188=DIRECTION('',(0.,0.,1.));
#6189=DIRECTION('center_axis',(0.,0.,1.));
#6190=DIRECTION('ref_axis',(1.,-2.80853466614331E-13,0.));
#6191=DIRECTION('',(0.,0.,1.));
#6192=DIRECTION('center_axis',(0.,0.,1.));
#6193=DIRECTION('ref_axis',(1.,-2.80853466614331E-13,0.));
#6194=DIRECTION('',(0.,0.,1.));
#6195=DIRECTION('center_axis',(0.,0.,1.));
#6196=DIRECTION('ref_axis',(1.,-2.80853466614331E-13,0.));
#6197=DIRECTION('',(0.,0.,1.));
#6198=DIRECTION('center_axis',(0.,0.,1.));
#6199=DIRECTION('ref_axis',(1.,-2.80853466614331E-13,0.));
#6200=DIRECTION('',(0.,0.,1.));
#6201=DIRECTION('center_axis',(0.,0.,1.));
#6202=DIRECTION('ref_axis',(1.,-2.80853466614331E-13,0.));
#6203=DIRECTION('',(0.,0.,1.));
#6204=DIRECTION('center_axis',(0.,0.,1.));
#6205=DIRECTION('ref_axis',(1.,-2.80853466614331E-13,0.));
#6206=DIRECTION('',(0.,0.,1.));
#6207=DIRECTION('center_axis',(0.,0.,1.));
#6208=DIRECTION('ref_axis',(1.,-2.80853466614331E-13,0.));
#6209=DIRECTION('',(0.,0.,1.));
#6210=DIRECTION('center_axis',(0.,0.,1.));
#6211=DIRECTION('ref_axis',(1.,-2.80853466614331E-13,0.));
#6212=DIRECTION('',(0.,0.,1.));
#6213=DIRECTION('center_axis',(0.,0.,1.));
#6214=DIRECTION('ref_axis',(1.,-2.80853466614331E-13,0.));
#6215=DIRECTION('',(0.,0.,1.));
#6216=DIRECTION('center_axis',(0.,0.,1.));
#6217=DIRECTION('ref_axis',(1.,-2.80853466614331E-13,0.));
#6218=DIRECTION('',(0.,0.,1.));
#6219=DIRECTION('center_axis',(0.,0.,1.));
#6220=DIRECTION('ref_axis',(1.,-2.80853466614331E-13,0.));
#6221=DIRECTION('',(0.,0.,1.));
#6222=DIRECTION('center_axis',(0.,0.,1.));
#6223=DIRECTION('ref_axis',(1.,-2.80853466614331E-13,0.));
#6224=DIRECTION('',(0.,0.,1.));
#6225=DIRECTION('center_axis',(0.,0.,1.));
#6226=DIRECTION('ref_axis',(1.,-2.80853466614331E-13,0.));
#6227=DIRECTION('',(0.,0.,1.));
#6228=DIRECTION('center_axis',(0.,0.,1.));
#6229=DIRECTION('ref_axis',(1.,-2.80853466614331E-13,0.));
#6230=DIRECTION('',(0.,0.,1.));
#6231=DIRECTION('center_axis',(0.,0.,1.));
#6232=DIRECTION('ref_axis',(1.,-2.80853466614331E-13,0.));
#6233=DIRECTION('',(0.,0.,1.));
#6234=DIRECTION('center_axis',(0.,0.,1.));
#6235=DIRECTION('ref_axis',(1.,-2.80853466614331E-13,0.));
#6236=DIRECTION('',(0.,0.,1.));
#6237=DIRECTION('center_axis',(0.,0.,1.));
#6238=DIRECTION('ref_axis',(1.,-2.80853466614331E-13,0.));
#6239=DIRECTION('',(0.,0.,1.));
#6240=DIRECTION('center_axis',(0.,0.,1.));
#6241=DIRECTION('ref_axis',(1.,-2.80853466614331E-13,0.));
#6242=DIRECTION('',(0.,0.,1.));
#6243=DIRECTION('center_axis',(0.,0.,1.));
#6244=DIRECTION('ref_axis',(1.,-2.80853466614331E-13,0.));
#6245=DIRECTION('',(0.,0.,1.));
#6246=DIRECTION('center_axis',(0.,0.,1.));
#6247=DIRECTION('ref_axis',(1.,-2.80853466614331E-13,0.));
#6248=DIRECTION('',(0.,0.,1.));
#6249=DIRECTION('center_axis',(0.,0.,1.));
#6250=DIRECTION('ref_axis',(1.,-2.80853466614331E-13,0.));
#6251=DIRECTION('',(0.,0.,1.));
#6252=DIRECTION('center_axis',(0.,0.,1.));
#6253=DIRECTION('ref_axis',(1.,-2.80853466614331E-13,0.));
#6254=DIRECTION('',(0.,0.,1.));
#6255=DIRECTION('center_axis',(0.,0.,1.));
#6256=DIRECTION('ref_axis',(1.,-2.80853466614331E-13,0.));
#6257=DIRECTION('',(0.,0.,1.));
#6258=DIRECTION('center_axis',(0.,0.,1.));
#6259=DIRECTION('ref_axis',(1.,-2.80853466614331E-13,0.));
#6260=DIRECTION('',(0.,0.,1.));
#6261=DIRECTION('center_axis',(0.,0.,1.));
#6262=DIRECTION('ref_axis',(1.,-2.80853466614331E-13,0.));
#6263=DIRECTION('',(0.,0.,1.));
#6264=DIRECTION('center_axis',(0.,0.,1.));
#6265=DIRECTION('ref_axis',(1.,-2.80853466614331E-13,0.));
#6266=DIRECTION('',(0.,0.,1.));
#6267=DIRECTION('center_axis',(0.,0.,1.));
#6268=DIRECTION('ref_axis',(1.,-2.80853466614331E-13,0.));
#6269=DIRECTION('',(0.,0.,1.));
#6270=DIRECTION('center_axis',(0.,0.,1.));
#6271=DIRECTION('ref_axis',(1.,-2.80853466614331E-13,0.));
#6272=DIRECTION('',(0.,0.,1.));
#6273=DIRECTION('center_axis',(0.,0.,1.));
#6274=DIRECTION('ref_axis',(1.,-2.80853466614331E-13,0.));
#6275=DIRECTION('',(0.,0.,1.));
#6276=DIRECTION('center_axis',(0.,0.,1.));
#6277=DIRECTION('ref_axis',(1.,-2.80853466614331E-13,0.));
#6278=DIRECTION('',(0.,0.,1.));
#6279=DIRECTION('center_axis',(0.,0.,1.));
#6280=DIRECTION('ref_axis',(1.,-2.80853466614331E-13,0.));
#6281=DIRECTION('',(0.,0.,1.));
#6282=DIRECTION('center_axis',(0.,0.,1.));
#6283=DIRECTION('ref_axis',(1.,-2.80853466614331E-13,0.));
#6284=DIRECTION('',(0.,0.,1.));
#6285=DIRECTION('center_axis',(0.,0.,1.));
#6286=DIRECTION('ref_axis',(1.,-2.80853466614331E-13,0.));
#6287=DIRECTION('center_axis',(0.,0.,-1.));
#6288=DIRECTION('ref_axis',(1.,-2.80853466614331E-13,0.));
#6289=DIRECTION('center_axis',(0.,0.,1.));
#6290=DIRECTION('ref_axis',(-0.942680984145002,-0.333695313319517,0.));
#6291=DIRECTION('center_axis',(0.,0.,-1.));
#6292=DIRECTION('ref_axis',(1.,0.,0.));
#6293=DIRECTION('center_axis',(-1.60246890531964E-16,-1.,0.));
#6294=DIRECTION('ref_axis',(1.,-1.60246890531964E-16,0.));
#6295=DIRECTION('',(1.,-1.60246890531964E-16,0.));
#6296=DIRECTION('',(0.,0.,1.));
#6297=DIRECTION('',(1.,-1.60246890531964E-16,0.));
#6298=DIRECTION('',(0.,0.,1.));
#6299=DIRECTION('center_axis',(-0.866025403784439,-0.5,0.));
#6300=DIRECTION('ref_axis',(0.5,-0.866025403784439,0.));
#6301=DIRECTION('',(0.5,-0.866025403784439,0.));
#6302=DIRECTION('',(0.,0.,1.));
#6303=DIRECTION('',(0.5,-0.866025403784439,0.));
#6304=DIRECTION('center_axis',(-0.866025403784439,0.5,0.));
#6305=DIRECTION('ref_axis',(-0.5,-0.866025403784439,0.));
#6306=DIRECTION('',(-0.5,-0.866025403784439,0.));
#6307=DIRECTION('',(0.,0.,1.));
#6308=DIRECTION('',(-0.5,-0.866025403784439,0.));
#6309=DIRECTION('center_axis',(1.60246890531964E-16,1.,0.));
#6310=DIRECTION('ref_axis',(-1.,1.60246890531964E-16,0.));
#6311=DIRECTION('',(-1.,1.60246890531964E-16,0.));
#6312=DIRECTION('',(0.,0.,1.));
#6313=DIRECTION('',(-1.,1.60246890531964E-16,0.));
#6314=DIRECTION('center_axis',(0.866025403784439,0.5,0.));
#6315=DIRECTION('ref_axis',(-0.5,0.866025403784439,0.));
#6316=DIRECTION('',(-0.5,0.866025403784439,0.));
#6317=DIRECTION('',(0.,0.,1.));
#6318=DIRECTION('',(-0.5,0.866025403784439,0.));
#6319=DIRECTION('center_axis',(0.866025403784439,-0.5,0.));
#6320=DIRECTION('ref_axis',(0.5,0.866025403784439,0.));
#6321=DIRECTION('',(0.5,0.866025403784439,0.));
#6322=DIRECTION('',(0.5,0.866025403784439,0.));
#6323=DIRECTION('center_axis',(0.,0.,1.));
#6324=DIRECTION('ref_axis',(1.,0.,0.));
#6325=DIRECTION('center_axis',(0.,0.,1.));
#6326=DIRECTION('ref_axis',(1.,0.,0.));
#6327=DIRECTION('center_axis',(0.,0.,1.));
#6328=DIRECTION('ref_axis',(1.,0.,0.));
#6329=DIRECTION('center_axis',(0.,0.,1.));
#6330=DIRECTION('ref_axis',(1.,0.,0.));
#6331=DIRECTION('',(0.,0.,-1.));
#6332=DIRECTION('center_axis',(0.,0.,1.));
#6333=DIRECTION('ref_axis',(1.,0.,0.));
#6334=DIRECTION('center_axis',(0.,0.,1.));
#6335=DIRECTION('ref_axis',(1.,0.,0.));
#6336=DIRECTION('center_axis',(0.,0.,1.));
#6337=DIRECTION('ref_axis',(1.,0.,0.));
#7257=CARTESIAN_POINT('',(0.,0.,0.));
#7258=CARTESIAN_POINT('Origin',(0.,0.,0.));
#7259=CARTESIAN_POINT('',(-0.195635777923873,0.00012637639400136,0.022586969212423));
#7260=CARTESIAN_POINT('',(-0.195586996729399,0.000207538314137144,0.0124130307875798));
#7261=CARTESIAN_POINT('',(-0.1954,-2.39295984553393E-17,0.));
#7262=CARTESIAN_POINT('',(0.0861525859670519,0.175382131162755,0.));
#7263=CARTESIAN_POINT('Ctrl Pts',(-0.195635777923873,0.00012637639400136,
0.022586969212423));
#7264=CARTESIAN_POINT('Ctrl Pts',(-0.195681347828373,0.00674175378970602,
0.0222084605749147));
#7265=CARTESIAN_POINT('Ctrl Pts',(-0.195374969862562,0.0133525801096144,
0.0218299519374064));
#7266=CARTESIAN_POINT('Ctrl Pts',(-0.194702755071016,0.0199256447333511,
0.0214514432998981));
#7267=CARTESIAN_POINT('Ctrl Pts',(-0.188123007026072,0.0842638736018979,
0.0177465390059727));
#7268=CARTESIAN_POINT('Ctrl Pts',(-0.146493114019884,0.144984224685349,
0.0140416347120473));
#7269=CARTESIAN_POINT('Ctrl Pts',(-0.0888552784097874,0.174368623359793,
0.0103367304181219));
#7270=CARTESIAN_POINT('Ctrl Pts',(-0.03525184529165,0.201696239540897,0.00689115361208129));
#7271=CARTESIAN_POINT('Ctrl Pts',(0.0321969844649043,0.201921141720556,
0.00344557680604065));
#7272=CARTESIAN_POINT('Ctrl Pts',(0.0863566694936594,0.175642871684081,
1.97324795392362E-17));
#7273=CARTESIAN_POINT('',(-0.0861525859670424,0.175382131162759,0.));
#7274=CARTESIAN_POINT('Origin',(0.,0.,0.));
#7275=CARTESIAN_POINT('Ctrl Pts',(-0.0861525859670425,0.175382131162759,
-6.38378239159465E-16));
#7276=CARTESIAN_POINT('Ctrl Pts',(-0.14447616479259,0.146731965348487,0.00370490429392476));
#7277=CARTESIAN_POINT('Ctrl Pts',(-0.18688174608519,0.0869523829547151,
0.00740980858785015));
#7278=CARTESIAN_POINT('Ctrl Pts',(-0.194371679194925,0.0228123128668349,
0.0111147128817756));
#7279=CARTESIAN_POINT('Ctrl Pts',(-0.195246583870653,0.0153200634169035,
0.0115474855170436));
#7280=CARTESIAN_POINT('Ctrl Pts',(-0.195645073240692,0.00776831620061643,
0.0119802581523117));
#7281=CARTESIAN_POINT('Ctrl Pts',(-0.195586996729399,0.000207538314137144,
0.0124130307875798));
#7282=CARTESIAN_POINT('Origin',(0.,0.,0.));
#7283=CARTESIAN_POINT('',(-0.195131096902049,0.000101113969644753,0.092586969212423));
#7284=CARTESIAN_POINT('',(-0.195116749400228,8.89926274127593E-5,0.0824130307875797));
#7285=CARTESIAN_POINT('',(-0.1954,-2.39295984553393E-17,0.));
#7286=CARTESIAN_POINT('Ctrl Pts',(-0.195131096902049,0.000101113969644753,
0.092586969212423));
#7287=CARTESIAN_POINT('Ctrl Pts',(-0.195253097178586,0.026184219880761,
0.0911045530051337));
#7288=CARTESIAN_POINT('Ctrl Pts',(-0.190391876856765,0.0522236645961475,
0.0896221367978444));
#7289=CARTESIAN_POINT('Ctrl Pts',(-0.180332593264173,0.0760702837060908,
0.0881397205905551));
#7290=CARTESIAN_POINT('Ctrl Pts',(-0.155192094399714,0.135668553815123,
0.0844348162966297));
#7291=CARTESIAN_POINT('Ctrl Pts',(-0.0975836177799518,0.181570066253063,
0.0807299120027044));
#7292=CARTESIAN_POINT('Ctrl Pts',(-0.0338757516333478,0.192766106246862,
0.077025007708779));
#7293=CARTESIAN_POINT('Ctrl Pts',(0.029832114513256,0.203962146240662,0.0733201034148536));
#7294=CARTESIAN_POINT('Ctrl Pts',(0.0996393701867018,0.180452713790321,
0.0696151991209281));
#7295=CARTESIAN_POINT('Ctrl Pts',(0.143592949422358,0.132995684060219,0.0659102948270027));
#7296=CARTESIAN_POINT('Ctrl Pts',(0.187546528658014,0.0855386543301167,
0.0622053905330773));
#7297=CARTESIAN_POINT('Ctrl Pts',(0.205646431455881,0.0141340273202524,
0.058500486239152));
#7298=CARTESIAN_POINT('Ctrl Pts',(0.189608855488219,-0.0485288059909611,
0.0547955819452266));
#7299=CARTESIAN_POINT('Ctrl Pts',(0.173571279520558,-0.111191639302175,
0.0510906776513013));
#7300=CARTESIAN_POINT('Ctrl Pts',(0.123396224787368,-0.165112678914738,
0.0473857733573758));
#7301=CARTESIAN_POINT('Ctrl Pts',(0.0620482175311841,-0.185621711873549,
0.0436808690634505));
#7302=CARTESIAN_POINT('Ctrl Pts',(0.000700210274999877,-0.206130744832361,
0.0399759647695251));
#7303=CARTESIAN_POINT('Ctrl Pts',(-0.0718207495041789,-0.193227771137421,
0.0362710604755997));
#7304=CARTESIAN_POINT('Ctrl Pts',(-0.122316427851919,-0.15279823096313,
0.0325661561816743));
#7305=CARTESIAN_POINT('Ctrl Pts',(-0.167653254878506,-0.116499143009035,
0.0292397605252572));
#7306=CARTESIAN_POINT('Ctrl Pts',(-0.19523530216884,-0.0580106393937795,
0.0259133648688401));
#7307=CARTESIAN_POINT('Ctrl Pts',(-0.195635777923873,0.00012637639400136,
0.022586969212423));
#7308=CARTESIAN_POINT('Ctrl Pts',(-0.195586996729399,0.000207538314137144,
0.0124130307875798));
#7309=CARTESIAN_POINT('Ctrl Pts',(-0.195147888579442,-0.056958415977544,
0.0156851624462371));
#7310=CARTESIAN_POINT('Ctrl Pts',(-0.168608485816707,-0.114640622495256,
0.0189572941048945));
#7311=CARTESIAN_POINT('Ctrl Pts',(-0.124548266143515,-0.151025787390765,
0.0222294257635518));
#7312=CARTESIAN_POINT('Ctrl Pts',(-0.0746606350555016,-0.192223259778496,
0.0259343300574772));
#7313=CARTESIAN_POINT('Ctrl Pts',(-0.00231108795260535,-0.20611764677197,
0.0296392343514025));
#7314=CARTESIAN_POINT('Ctrl Pts',(0.0593359806590351,-0.186491079647165,
0.0333441386453279));
#7315=CARTESIAN_POINT('Ctrl Pts',(0.120983049270676,-0.16686451252236,0.0370490429392533));
#7316=CARTESIAN_POINT('Ctrl Pts',(0.17192763939106,-0.113716991279275,0.0407539472331787));
#7317=CARTESIAN_POINT('Ctrl Pts',(0.188876026712615,-0.0513034241454011,
0.0444588515271041));
#7318=CARTESIAN_POINT('Ctrl Pts',(0.205824414034169,0.0111101429884734,
0.0481637558210295));
#7319=CARTESIAN_POINT('Ctrl Pts',(0.188776598556893,0.082789756013138,0.0518686601149549));
#7320=CARTESIAN_POINT('Ctrl Pts',(0.14552275371934,0.130888260289707,0.0555735644088803));
#7321=CARTESIAN_POINT('Ctrl Pts',(0.102268908881787,0.178986764566276,0.0592784687028057));
#7322=CARTESIAN_POINT('Ctrl Pts',(0.0328090346839575,0.203504160094748,
0.0629833729967312));
#7323=CARTESIAN_POINT('Ctrl Pts',(-0.0310564735112635,0.193237932504459,
0.0666882772906565));
#7324=CARTESIAN_POINT('Ctrl Pts',(-0.0949219817064845,0.18297170491417,
0.0703931815845819));
#7325=CARTESIAN_POINT('Ctrl Pts',(-0.153193123899096,0.137921854205119,
0.0740980858785072));
#7326=CARTESIAN_POINT('Ctrl Pts',(-0.179201322195063,0.0786984774853335,
0.0778029901724326));
#7327=CARTESIAN_POINT('Ctrl Pts',(-0.189988721900888,0.0541344446624959,
0.0793396703774816));
#7328=CARTESIAN_POINT('Ctrl Pts',(-0.195225814685876,0.0271320906572496,
0.0808763505825307));
#7329=CARTESIAN_POINT('Ctrl Pts',(-0.195116749400228,8.89926274127593E-5,
0.0824130307875797));
#7330=CARTESIAN_POINT('Origin',(0.,0.,0.));
#7331=CARTESIAN_POINT('',(-0.195269961073647,-0.00016635217456426,0.162586969212423));
#7332=CARTESIAN_POINT('',(-0.195296072527608,-0.000171556393799694,0.15241303078758));
#7333=CARTESIAN_POINT('',(-0.1954,-2.39295984553393E-17,0.));
#7334=CARTESIAN_POINT('Ctrl Pts',(-0.195269961073647,-0.00016635217456426,
0.162586969212423));
#7335=CARTESIAN_POINT('Ctrl Pts',(-0.194902238792413,0.0452585421341261,
0.160000645435353));
#7336=CARTESIAN_POINT('Ctrl Pts',(-0.179109205182361,0.0909139814220055,
0.157414321658282));
#7337=CARTESIAN_POINT('Ctrl Pts',(-0.150142749348677,0.125553440155619,
0.154827997881212));
#7338=CARTESIAN_POINT('Ctrl Pts',(-0.108648351953627,0.175174404297546,
0.151123093587287));
#7339=CARTESIAN_POINT('Ctrl Pts',(-0.0401214170626077,0.202190011810589,
0.147418189293361));
#7340=CARTESIAN_POINT('Ctrl Pts',(0.0240715464793194,0.194234567703968,
0.143713284999436));
#7341=CARTESIAN_POINT('Ctrl Pts',(0.0882645100212464,0.186279123597346,
0.140008380705511));
#7342=CARTESIAN_POINT('Ctrl Pts',(0.148123502214081,0.143352627871059,0.136303476411585));
#7343=CARTESIAN_POINT('Ctrl Pts',(0.176249534614617,0.0851035623277452,
0.13259857211766));
#7344=CARTESIAN_POINT('Ctrl Pts',(0.204375567015153,0.0268544967844316,
0.128893667823734));
#7345=CARTESIAN_POINT('Ctrl Pts',(0.20076863962339,-0.0467171385759083,
0.125188763529809));
#7346=CARTESIAN_POINT('Ctrl Pts',(0.167079755224462,-0.101935622009865,
0.121483859235884));
#7347=CARTESIAN_POINT('Ctrl Pts',(0.133390870825534,-0.157154105443821,
0.117778954941958));
#7348=CARTESIAN_POINT('Ctrl Pts',(0.0696200294194389,-0.194019436951393,
0.114074050648033));
#7349=CARTESIAN_POINT('Ctrl Pts',(0.00495672165634356,-0.195657648289217,
0.110369146354107));
#7350=CARTESIAN_POINT('Ctrl Pts',(-0.0597065861067518,-0.19729585962704,
0.106664242060182));
#7351=CARTESIAN_POINT('Ctrl Pts',(-0.125262360226848,-0.163706950795115,
0.102959337766257));
#7352=CARTESIAN_POINT('Ctrl Pts',(-0.161703986732318,-0.11026498248909,
0.0992544334723314));
#7353=CARTESIAN_POINT('Ctrl Pts',(-0.183564492251676,-0.0782063573631269,
0.0970319453856953));
#7354=CARTESIAN_POINT('Ctrl Pts',(-0.19494818999653,-0.0390035530360715,
0.0948094572990591));
#7355=CARTESIAN_POINT('Ctrl Pts',(-0.195131096902049,0.000101113969644753,
0.092586969212423));
#7356=CARTESIAN_POINT('Ctrl Pts',(-0.195116749400228,8.89926274127593E-5,
0.0824130307875797));
#7357=CARTESIAN_POINT('Ctrl Pts',(-0.194962860530686,-0.0380682611678014,
0.0845812548764561));
#7358=CARTESIAN_POINT('Ctrl Pts',(-0.184165504319832,-0.0763066307267761,
0.0867494789653325));
#7359=CARTESIAN_POINT('Ctrl Pts',(-0.163298148442827,-0.10789116262043,
0.0889177030542089));
#7360=CARTESIAN_POINT('Ctrl Pts',(-0.127641521995304,-0.161860523275888,
0.0926226073481343));
#7361=CARTESIAN_POINT('Ctrl Pts',(-0.0625830147009374,-0.196402341856286,
0.0963275116420596));
#7362=CARTESIAN_POINT('Ctrl Pts',(0.00209745128795896,-0.195708815241575,
0.100032415935985));
#7363=CARTESIAN_POINT('Ctrl Pts',(0.0667779172768549,-0.195015288626865,
0.10373732022991));
#7364=CARTESIAN_POINT('Ctrl Pts',(0.13108034196028,-0.159086416817049,0.107442224523836));
#7365=CARTESIAN_POINT('Ctrl Pts',(0.165572399043018,-0.104366250199005,
0.111147128817761));
#7366=CARTESIAN_POINT('Ctrl Pts',(0.200064456125757,-0.0496460835809611,
0.114852033111687));
#7367=CARTESIAN_POINT('Ctrl Pts',(0.204746145607807,0.0238653778453102,
0.118556937405612));
#7368=CARTESIAN_POINT('Ctrl Pts',(0.177474264716175,0.0825192844773609,
0.122261841699537));
#7369=CARTESIAN_POINT('Ctrl Pts',(0.150202383824543,0.141173191109411,0.125966745993463));
#7370=CARTESIAN_POINT('Ctrl Pts',(0.0909769325592305,0.184969542947241,
0.129671650287388));
#7371=CARTESIAN_POINT('Ctrl Pts',(0.0269070452168959,0.193862055706153,
0.133376554581313));
#7372=CARTESIAN_POINT('Ctrl Pts',(-0.037162842125439,0.202754568465066,
0.137081458875239));
#7373=CARTESIAN_POINT('Ctrl Pts',(-0.106077165544796,0.176743242145061,
0.140786363169164));
#7374=CARTESIAN_POINT('Ctrl Pts',(-0.148292168871142,0.127733901391228,
0.14449126746309));
#7375=CARTESIAN_POINT('Ctrl Pts',(-0.178379969487403,0.0928035885463768,
0.14713185523792));
#7376=CARTESIAN_POINT('Ctrl Pts',(-0.194905030259773,0.0461907277712621,
0.14977244301275));
#7377=CARTESIAN_POINT('Ctrl Pts',(-0.195296072527608,-0.000171556393799694,
0.15241303078758));
#7378=CARTESIAN_POINT('Origin',(0.,0.,0.));
#7379=CARTESIAN_POINT('',(-0.195720342430618,-4.78848216406425E-6,0.232586969212423));
#7380=CARTESIAN_POINT('',(-0.195719426634615,1.29078158682454E-5,0.22241303078758));
#7381=CARTESIAN_POINT('',(-0.1954,-2.39295984553393E-17,0.));
#7382=CARTESIAN_POINT('Ctrl Pts',(-0.195720342430618,-4.78848216406425E-6,
0.232586969212423));
#7383=CARTESIAN_POINT('Ctrl Pts',(-0.195697143051313,0.0644232125710103,
0.228896737865572));
#7384=CARTESIAN_POINT('Ctrl Pts',(-0.160777086274134,0.128872764270736,
0.22520650651872));
#7385=CARTESIAN_POINT('Ctrl Pts',(-0.106783173118586,0.164023975286507,
0.221516275171869));
#7386=CARTESIAN_POINT('Ctrl Pts',(-0.0525745715720951,0.199314953111009,
0.217811370877944));
#7387=CARTESIAN_POINT('Ctrl Pts',(0.0208598692839071,0.205074137319626,
0.214106466584018));
#7388=CARTESIAN_POINT('Ctrl Pts',(0.0799073451636341,0.178665404061868,
0.210401562290093));
#7389=CARTESIAN_POINT('Ctrl Pts',(0.138954821043361,0.152256670804111,0.206696657996168));
#7390=CARTESIAN_POINT('Ctrl Pts',(0.183615331946813,0.0936800200799801,
0.202991753702242));
#7391=CARTESIAN_POINT('Ctrl Pts',(0.193446630107478,0.0297474679262876,
0.199286849408317));
#7392=CARTESIAN_POINT('Ctrl Pts',(0.203277928268144,-0.0341850842274047,
0.195581945114392));
#7393=CARTESIAN_POINT('Ctrl Pts',(0.178280013686022,-0.103473537810658,
0.191877040820466));
#7394=CARTESIAN_POINT('Ctrl Pts',(0.129895065749049,-0.146402809319959,
0.188172136526541));
#7395=CARTESIAN_POINT('Ctrl Pts',(0.0815101178120762,-0.18933208082926,
0.184467232232615));
#7396=CARTESIAN_POINT('Ctrl Pts',(0.00973813652025106,-0.205902170264609,
0.18076232793869));
#7397=CARTESIAN_POINT('Ctrl Pts',(-0.0525690244207131,-0.188528532620279,
0.177057423644765));
#7398=CARTESIAN_POINT('Ctrl Pts',(-0.114876185361677,-0.171154894975948,
0.173352519350839));
#7399=CARTESIAN_POINT('Ctrl Pts',(-0.16771852595178,-0.119837530251938,
0.169647615056914));
#7400=CARTESIAN_POINT('Ctrl Pts',(-0.186908766297293,-0.0580656875045278,
0.165942710762988));
#7401=CARTESIAN_POINT('Ctrl Pts',(-0.192702661972129,-0.0394156025615012,
0.164824130246133));
#7402=CARTESIAN_POINT('Ctrl Pts',(-0.195429000318094,-0.0198125396335311,
0.163705549729278));
#7403=CARTESIAN_POINT('Ctrl Pts',(-0.195269961073647,-0.00016635217456426,
0.162586969212423));
#7404=CARTESIAN_POINT('Ctrl Pts',(-0.195296072527608,-0.000171556393799694,
0.15241303078758));
#7405=CARTESIAN_POINT('Ctrl Pts',(-0.195453686203354,-0.0188583599040719,
0.153477347306675));
#7406=CARTESIAN_POINT('Ctrl Pts',(-0.192990203806021,-0.0375044553062908,
0.15454166382577));
#7407=CARTESIAN_POINT('Ctrl Pts',(-0.187737257267333,-0.0553284581639518,
0.155605980344866));
#7408=CARTESIAN_POINT('Ctrl Pts',(-0.169451659103841,-0.117374121777638,
0.159310884638791));
#7409=CARTESIAN_POINT('Ctrl Pts',(-0.117364779543521,-0.169458093817348,
0.163015788932717));
#7410=CARTESIAN_POINT('Ctrl Pts',(-0.0553181242256267,-0.187740280857214,
0.166720693226642));
#7411=CARTESIAN_POINT('Ctrl Pts',(0.00672853109226811,-0.20602246789708,
0.170425597520567));
#7412=CARTESIAN_POINT('Ctrl Pts',(0.0787349621677377,-0.190502869937101,
0.174130501814493));
#7413=CARTESIAN_POINT('Ctrl Pts',(0.127742011886824,-0.148285168489488,
0.177835406108418));
#7414=CARTESIAN_POINT('Ctrl Pts',(0.17674906160591,-0.106067467041874,0.181540310402344));
#7415=CARTESIAN_POINT('Ctrl Pts',(0.202756729968613,-0.0371516621066246,
0.185245214696269));
#7416=CARTESIAN_POINT('Ctrl Pts',(0.193860642333605,0.0269177193885033,
0.188950118990194));
#7417=CARTESIAN_POINT('Ctrl Pts',(0.184964554698597,0.0909871008836312,
0.19265502328412));
#7418=CARTESIAN_POINT('Ctrl Pts',(0.141164711065879,0.150210058938638,0.196359927578045));
#7419=CARTESIAN_POINT('Ctrl Pts',(0.0825094128007834,0.17747875371355,0.200064831871971));
#7420=CARTESIAN_POINT('Ctrl Pts',(0.0238541145356881,0.204747448488462,
0.203769736165896));
#7421=CARTESIAN_POINT('Ctrl Pts',(-0.0496566383617833,0.200061879983279,
0.207474640459821));
#7422=CARTESIAN_POINT('Ctrl Pts',(-0.104375113131947,0.165566747025073,
0.211179544753747));
#7423=CARTESIAN_POINT('Ctrl Pts',(-0.15909358790211,0.131071614066866,0.214884449047672));
#7424=CARTESIAN_POINT('Ctrl Pts',(-0.195019784544964,0.0667669166556367,
0.218589353341598));
#7425=CARTESIAN_POINT('Ctrl Pts',(-0.195709371646085,0.00208654669905255,
0.222294257635523));
#7426=CARTESIAN_POINT('Ctrl Pts',(-0.195716740656376,0.00139536452478984,
0.222333848686209));
#7427=CARTESIAN_POINT('Ctrl Pts',(-0.195720085887096,0.000704139451294379,
0.222373439736894));
#7428=CARTESIAN_POINT('Ctrl Pts',(-0.195719426634615,1.29078158682454E-5,
0.22241303078758));
#7429=CARTESIAN_POINT('Origin',(0.,0.,0.));
#7430=CARTESIAN_POINT('',(-0.195283952697599,0.000169337138534779,0.302586969212423));
#7431=CARTESIAN_POINT('',(-0.195258340825392,0.000163515663356278,0.29241303078758));
#7432=CARTESIAN_POINT('',(-0.1954,-2.39295984553393E-17,0.));
#7433=CARTESIAN_POINT('Ctrl Pts',(-0.195283952697599,0.000169337138534779,
0.302586969212423));
#7434=CARTESIAN_POINT('Ctrl Pts',(-0.19544242560897,0.0192966383326108,
0.301497734589716));
#7435=CARTESIAN_POINT('Ctrl Pts',(-0.192859982037008,0.0383820720800439,
0.300408499967009));
#7436=CARTESIAN_POINT('Ctrl Pts',(-0.187361774489973,0.0565868885747682,
0.299319265344303));
#7437=CARTESIAN_POINT('Ctrl Pts',(-0.16866026397493,0.11850844467975,0.295614361050377));
#7438=CARTESIAN_POINT('Ctrl Pts',(-0.116225092311322,0.170241781073389,
0.291909456756452));
#7439=CARTESIAN_POINT('Ctrl Pts',(-0.0540571662767995,0.188107238759169,
0.288204552462526));
#7440=CARTESIAN_POINT('Ctrl Pts',(0.00811075975772279,0.205972696444949,
0.284499648168601));
#7441=CARTESIAN_POINT('Ctrl Pts',(0.080011440163159,0.189970275422869,0.280794743874676));
#7442=CARTESIAN_POINT('Ctrl Pts',(0.128734111559132,0.147424689310423,0.27708983958075));
#7443=CARTESIAN_POINT('Ctrl Pts',(0.177456782955104,0.104879103197978,0.273384935286825));
#7444=CARTESIAN_POINT('Ctrl Pts',(0.203001445341614,0.0357903519951666,
0.269680030992899));
#7445=CARTESIAN_POINT('Ctrl Pts',(0.193675659438429,-0.0282178921934112,
0.265975126698974));
#7446=CARTESIAN_POINT('Ctrl Pts',(0.184349873535243,-0.0922261363819893,
0.262270222405049));
#7447=CARTESIAN_POINT('Ctrl Pts',(0.140153639342363,-0.151153873556334,
0.258565318111123));
#7448=CARTESIAN_POINT('Ctrl Pts',(0.081316693190513,-0.178028385131025,
0.254860413817198));
#7449=CARTESIAN_POINT('Ctrl Pts',(0.0224797470386625,-0.204902896705717,
0.251155509523273));
#7450=CARTESIAN_POINT('Ctrl Pts',(-0.0509979110721584,-0.199724182680755,
0.247450605229347));
#7451=CARTESIAN_POINT('Ctrl Pts',(-0.105483695120245,-0.164862671795436,
0.243745700935422));
#7452=CARTESIAN_POINT('Ctrl Pts',(-0.160185265316152,-0.129863094967365,
0.240026123694422));
#7453=CARTESIAN_POINT('Ctrl Pts',(-0.19574372629877,-0.0649451415050078,
0.236306546453423));
#7454=CARTESIAN_POINT('Ctrl Pts',(-0.195720342430618,-4.78848216406425E-6,
0.232586969212423));
#7455=CARTESIAN_POINT('Ctrl Pts',(-0.195719426634615,1.29078158682454E-5,
0.22241303078758));
#7456=CARTESIAN_POINT('Ctrl Pts',(-0.195658393476725,-0.0639808590481945,
0.22607834403082));
#7457=CARTESIAN_POINT('Ctrl Pts',(-0.161275200187356,-0.128030867785169,
0.229743657274059));
#7458=CARTESIAN_POINT('Ctrl Pts',(-0.107881352358607,-0.163303782908962,
0.233408970517299));
#7459=CARTESIAN_POINT('Ctrl Pts',(-0.0539107684106243,-0.198957700058453,
0.237113874811225));
#7460=CARTESIAN_POINT('Ctrl Pts',(0.0194833770447268,-0.205209491855498,
0.24081877910515));
#7461=CARTESIAN_POINT('Ctrl Pts',(0.0787067240594876,-0.179197554104805,
0.244523683399075));
#7462=CARTESIAN_POINT('Ctrl Pts',(0.137930071074249,-0.153185616354111,
0.248228587693001));
#7463=CARTESIAN_POINT('Ctrl Pts',(0.182982619648419,-0.0949099490556798,
0.251933491986926));
#7464=CARTESIAN_POINT('Ctrl Pts',(0.193242676546893,-0.0310448021878294,
0.255638396280851));
#7465=CARTESIAN_POINT('Ctrl Pts',(0.203502733445366,0.0328203446800207,
0.259343300574777));
#7466=CARTESIAN_POINT('Ctrl Pts',(0.178970298668143,0.10227497111729,0.263048204868703));
#7467=CARTESIAN_POINT('Ctrl Pts',(0.130874489328304,0.145527934810222,0.266753109162628));
#7468=CARTESIAN_POINT('Ctrl Pts',(0.0827786799884639,0.188780898503155,
0.270458013456553));
#7469=CARTESIAN_POINT('Ctrl Pts',(0.0111194960860082,0.205832199451752,
0.274162917750478));
#7470=CARTESIAN_POINT('Ctrl Pts',(-0.0513028380988605,0.188877025035076,
0.277867822044404));
#7471=CARTESIAN_POINT('Ctrl Pts',(-0.113725172283729,0.1719218506184,0.281572726338329));
#7472=CARTESIAN_POINT('Ctrl Pts',(-0.166910656751011,0.120960200836452,
0.285277630632255));
#7473=CARTESIAN_POINT('Ctrl Pts',(-0.186514947523482,0.0593185142124166,
0.28898253492618));
#7474=CARTESIAN_POINT('Ctrl Pts',(-0.192565705566086,0.0402931418881201,
0.290126033546647));
#7475=CARTESIAN_POINT('Ctrl Pts',(-0.195417469557725,0.0202503734988586,
0.291269532167113));
#7476=CARTESIAN_POINT('Ctrl Pts',(-0.195258340825392,0.000163515663356278,
0.29241303078758));
#7477=CARTESIAN_POINT('Origin',(0.,0.,0.));
#7478=CARTESIAN_POINT('',(-0.195123386395527,-9.37244138880245E-5,0.372586969212423));
#7479=CARTESIAN_POINT('',(-0.195138177948142,-0.000106777846584659,0.36241303078758));
#7480=CARTESIAN_POINT('',(-0.1954,-2.39295984553393E-17,0.));
#7481=CARTESIAN_POINT('Ctrl Pts',(-0.195123386395527,-9.37244138880245E-5,
0.372586969212423));
#7482=CARTESIAN_POINT('Ctrl Pts',(-0.19495607068899,0.0384983387935844,
0.370393827019935));
#7483=CARTESIAN_POINT('Ctrl Pts',(-0.183891455427995,0.0771788701751315,
0.368200684827447));
#7484=CARTESIAN_POINT('Ctrl Pts',(-0.162570246636473,0.108983601551862,
0.366007542634959));
#7485=CARTESIAN_POINT('Ctrl Pts',(-0.126552044864621,0.162711757550323,
0.362302638341034));
#7486=CARTESIAN_POINT('Ctrl Pts',(-0.0612637871930766,0.196817896755676,
0.358597734047109));
#7487=CARTESIAN_POINT('Ctrl Pts',(0.00341043643912528,0.195690775004793,
0.354892829753183));
#7488=CARTESIAN_POINT('Ctrl Pts',(0.0680846600713272,0.194563653253909,
0.351187925459258));
#7489=CARTESIAN_POINT('Ctrl Pts',(0.132144849664187,0.158203270546789,0.347483021165333));
#7490=CARTESIAN_POINT('Ctrl Pts',(0.166269033157579,0.103252695419938,0.343778116871407));
#7491=CARTESIAN_POINT('Ctrl Pts',(0.200393216650971,0.0483021202930879,
0.340073212577482));
#7492=CARTESIAN_POINT('Ctrl Pts',(0.204581394044897,-0.0252386472534923,
0.336368308283556));
#7493=CARTESIAN_POINT('Ctrl Pts',(0.176916530417748,-0.0837081343932021,
0.332663403989631));
#7494=CARTESIAN_POINT('Ctrl Pts',(0.149251666790599,-0.142177621532912,
0.328958499695706));
#7495=CARTESIAN_POINT('Ctrl Pts',(0.0897337621423753,-0.185575828265751,
0.32525359540178));
#7496=CARTESIAN_POINT('Ctrl Pts',(0.025605669612909,-0.19403829565955,0.321548691107855));
#7497=CARTESIAN_POINT('Ctrl Pts',(-0.0385224229165574,-0.202500763053348,
0.317843786813929));
#7498=CARTESIAN_POINT('Ctrl Pts',(-0.107260703327267,-0.176027491108105,
0.314138882520004));
#7499=CARTESIAN_POINT('Ctrl Pts',(-0.149145918849381,-0.126735967227322,
0.310433978226078));
#7500=CARTESIAN_POINT('Ctrl Pts',(-0.178716962855371,-0.0919360550475366,
0.30781830855486));
#7501=CARTESIAN_POINT('Ctrl Pts',(-0.194903398518234,-0.0457626416864486,
0.305202638883641));
#7502=CARTESIAN_POINT('Ctrl Pts',(-0.195283952697599,0.000169337138534779,
0.302586969212423));
#7503=CARTESIAN_POINT('Ctrl Pts',(-0.195258340825392,0.000163515663356278,
0.29241303078758));
#7504=CARTESIAN_POINT('Ctrl Pts',(-0.194901896811807,-0.0448304971854093,
0.294974436461039));
#7505=CARTESIAN_POINT('Ctrl Pts',(-0.179438365931039,-0.0900457278440895,
0.297535842134498));
#7506=CARTESIAN_POINT('Ctrl Pts',(-0.150981821407715,-0.124543170751799,
0.300097247807956));
#7507=CARTESIAN_POINT('Ctrl Pts',(-0.109821307441813,-0.174441445625855,
0.303802152101882));
#7508=CARTESIAN_POINT('Ctrl Pts',(-0.0414771824323471,-0.201916271907844,
0.307507056395807));
#7509=CARTESIAN_POINT('Ctrl Pts',(0.0227677157704201,-0.194391725382998,
0.311211960689733));
#7510=CARTESIAN_POINT('Ctrl Pts',(0.0870126139731875,-0.186867178858152,
0.314916864983658));
#7511=CARTESIAN_POINT('Ctrl Pts',(0.147158285369256,-0.14434325952647,0.318621769277583));
#7512=CARTESIAN_POINT('Ctrl Pts',(0.175674532068328,-0.0862842428284894,
0.322326673571509));
#7513=CARTESIAN_POINT('Ctrl Pts',(0.204190778767399,-0.0282252261305095,
0.326031577865434));
#7514=CARTESIAN_POINT('Ctrl Pts',(0.201077600769473,0.0453688879337687,
0.32973648215936));
#7515=CARTESIAN_POINT('Ctrl Pts',(0.167759978533406,0.100812208488104,0.333441386453285));
#7516=CARTESIAN_POINT('Ctrl Pts',(0.134442356297339,0.156255529042441,0.33714629074721));
#7517=CARTESIAN_POINT('Ctrl Pts',(0.070920289823129,0.193548056086834,0.340851195041136));
#7518=CARTESIAN_POINT('Ctrl Pts',(0.00626943858281168,0.195620054999355,
0.344556099335061));
#7519=CARTESIAN_POINT('Ctrl Pts',(-0.0583814126575052,0.197692053911877,
0.348261003628986));
#7520=CARTESIAN_POINT('Ctrl Pts',(-0.12416104866393,0.164543524692526,0.351965907922912));
#7521=CARTESIAN_POINT('Ctrl Pts',(-0.160960463181693,0.111347389148941,
0.355670812216837));
#7522=CARTESIAN_POINT('Ctrl Pts',(-0.18328309972599,0.0790784518611643,
0.357918218407085));
#7523=CARTESIAN_POINT('Ctrl Pts',(-0.19494196408341,0.0394326521564634,
0.360165624597332));
#7524=CARTESIAN_POINT('Ctrl Pts',(-0.195138177948142,-0.000106777846584659,
0.36241303078758));
#7525=CARTESIAN_POINT('Origin',(0.,0.,0.));
#7526=CARTESIAN_POINT('',(-0.195626364086859,-0.000119838590748017,0.442586969212423));
#7527=CARTESIAN_POINT('',(-0.195647655240959,-0.000106560329145428,0.43241303078758));
#7528=CARTESIAN_POINT('',(-0.1954,-2.39295984553393E-17,0.));
#7529=CARTESIAN_POINT('Ctrl Pts',(-0.195626364086859,-0.000119838590748017,
0.442586969212423));
#7530=CARTESIAN_POINT('Ctrl Pts',(-0.195210765908107,0.0575169625739688,
0.439289919450154));
#7531=CARTESIAN_POINT('Ctrl Pts',(-0.168170950548248,0.115492749874537,
0.435992869687885));
#7532=CARTESIAN_POINT('Ctrl Pts',(-0.123518955260722,0.151820875343157,
0.432695819925617));
#7533=CARTESIAN_POINT('Ctrl Pts',(-0.0733433798216494,0.192642894343057,
0.428990915631691));
#7534=CARTESIAN_POINT('Ctrl Pts',(-0.00092876126150717,0.206130234335124,
0.425286011337766));
#7535=CARTESIAN_POINT('Ctrl Pts',(0.0605788945201889,0.186109398036142,
0.421581107043841));
#7536=CARTESIAN_POINT('Ctrl Pts',(0.122086550301885,0.16608856173716,0.417876202749915));
#7537=CARTESIAN_POINT('Ctrl Pts',(0.172687243305135,0.11255954914713,0.41417129845599));
#7538=CARTESIAN_POINT('Ctrl Pts',(0.189219754122116,0.0500239457522927,
0.410466394162064));
#7539=CARTESIAN_POINT('Ctrl Pts',(0.205752264939098,-0.0125116576425448,
0.406761489868139));
#7540=CARTESIAN_POINT('Ctrl Pts',(0.188216593569811,-0.0840538518421897,
0.403056585574214));
#7541=CARTESIAN_POINT('Ctrl Pts',(0.14463926115343,-0.131855961684149,0.399351681280288));
#7542=CARTESIAN_POINT('Ctrl Pts',(0.101061928737049,-0.179658071526109,
0.395646776986363));
#7543=CARTESIAN_POINT('Ctrl Pts',(0.0314429352735729,-0.203720097010384,
0.391941872692437));
#7544=CARTESIAN_POINT('Ctrl Pts',(-0.0323513417852891,-0.193028239341701,
0.388236968398512));
#7545=CARTESIAN_POINT('Ctrl Pts',(-0.096145618844151,-0.182336381673018,
0.384532064104586));
#7546=CARTESIAN_POINT('Ctrl Pts',(-0.154115179498399,-0.136890640851379,
0.380827159810661));
#7547=CARTESIAN_POINT('Ctrl Pts',(-0.179725886889443,-0.0774926840447737,
0.377122255516736));
#7548=CARTESIAN_POINT('Ctrl Pts',(-0.190176169475222,-0.0532557340781358,
0.375610493415298));
#7549=CARTESIAN_POINT('Ctrl Pts',(-0.19523871933882,-0.0266957471979921,
0.374098731313861));
#7550=CARTESIAN_POINT('Ctrl Pts',(-0.195123386395527,-9.37244138880245E-5,
0.372586969212423));
#7551=CARTESIAN_POINT('Ctrl Pts',(-0.195138177948142,-0.000106777846584659,
0.36241303078758));
#7552=CARTESIAN_POINT('Ctrl Pts',(-0.195265427457823,-0.0257490691689222,
0.363870528891258));
#7553=CARTESIAN_POINT('Ctrl Pts',(-0.190571668416256,-0.0513466230859282,
0.365328026994935));
#7554=CARTESIAN_POINT('Ctrl Pts',(-0.180838999481628,-0.0748583198076805,
0.366785525098613));
#7555=CARTESIAN_POINT('Ctrl Pts',(-0.156098928234699,-0.134624151352898,
0.370490429392539));
#7556=CARTESIAN_POINT('Ctrl Pts',(-0.0987995927117393,-0.180912072575515,
0.374195333686464));
#7557=CARTESIAN_POINT('Ctrl Pts',(-0.0351683507451656,-0.192534928996931,
0.37790023798039));
#7558=CARTESIAN_POINT('Ctrl Pts',(0.0284628912214086,-0.204157785418346,
0.381605142274315));
#7559=CARTESIAN_POINT('Ctrl Pts',(0.0984260396315977,-0.181115577038558,
0.38531004656824));
#7560=CARTESIAN_POINT('Ctrl Pts',(0.142697188593653,-0.133955306522111,
0.389014950862166));
#7561=CARTESIAN_POINT('Ctrl Pts',(0.186968337555709,-0.086795036005663,
0.392719855156091));
#7562=CARTESIAN_POINT('Ctrl Pts',(0.205547487069631,-0.0155167033525556,
0.396424759450017));
#7563=CARTESIAN_POINT('Ctrl Pts',(0.189930489607766,0.0472537923908843,
0.400129663743942));
#7564=CARTESIAN_POINT('Ctrl Pts',(0.1743134921459,0.110024288134324,0.403834568037867));
#7565=CARTESIAN_POINT('Ctrl Pts',(0.124500347708247,0.164286946968095,0.407539472331793));
#7566=CARTESIAN_POINT('Ctrl Pts',(0.0632917947676797,0.185204374929584,
0.411244376625718));
#7567=CARTESIAN_POINT('Ctrl Pts',(0.00208324182711199,0.206121802891074,
0.414949280919643));
#7568=CARTESIAN_POINT('Ctrl Pts',(-0.0705207196163706,0.19369399998028,
0.418654185213569));
#7569=CARTESIAN_POINT('Ctrl Pts',(-0.121287416627594,0.153609486509697,
0.422359089507494));
#7570=CARTESIAN_POINT('Ctrl Pts',(-0.167209015877504,0.117350579153232,
0.425710403267523));
#7571=CARTESIAN_POINT('Ctrl Pts',(-0.19526267760737,0.0584620801725425,
0.429061717027551));
#7572=CARTESIAN_POINT('Ctrl Pts',(-0.195647655240959,-0.000106560329145428,
0.43241303078758));
#7573=CARTESIAN_POINT('Origin',(0.,0.,0.));
#7574=CARTESIAN_POINT('',(-0.195488415809582,0.000168817958016994,0.512586969212423));
#7575=CARTESIAN_POINT('',(-0.19545977166257,0.000173536236839715,0.502413030787579));
#7576=CARTESIAN_POINT('',(-0.1954,-2.39295984553393E-17,0.));
#7577=CARTESIAN_POINT('Ctrl Pts',(-0.195488415809582,0.000168817958016994,
0.512586969212423));
#7578=CARTESIAN_POINT('Ctrl Pts',(-0.195599493209505,0.0123590955640317,
0.511890916174299));
#7579=CARTESIAN_POINT('Ctrl Pts',(-0.194557059515437,0.0245304346389609,
0.511194863136174));
#7580=CARTESIAN_POINT('Ctrl Pts',(-0.192292612985525,0.0364700080869448,
0.51049881009805));
#7581=CARTESIAN_POINT('Ctrl Pts',(-0.180239569305636,0.100021166565142,
0.506793905804125));
#7582=CARTESIAN_POINT('Ctrl Pts',(-0.133565088753798,0.157006060936268,
0.503089001510199));
#7583=CARTESIAN_POINT('Ctrl Pts',(-0.0736332638087015,0.181341261050928,
0.499384097216274));
#7584=CARTESIAN_POINT('Ctrl Pts',(-0.0137014388636053,0.205676461165589,
0.495679192922349));
#7585=CARTESIAN_POINT('Ctrl Pts',(0.0594877304747487,0.197361967023783,
0.491974288628423));
#7586=CARTESIAN_POINT('Ctrl Pts',(0.112433706788561,0.160203533283279,0.488269384334498));
#7587=CARTESIAN_POINT('Ctrl Pts',(0.165379683102374,0.123045099542775,0.484564480040572));
#7588=CARTESIAN_POINT('Ctrl Pts',(0.198082466391645,0.0570427262035733,
0.480859575746647));
#7589=CARTESIAN_POINT('Ctrl Pts',(0.195573164057203,-0.00759262795856141,
0.477154671452722));
#7590=CARTESIAN_POINT('Ctrl Pts',(0.193063861722761,-0.0722279821206961,
0.473449767158796));
#7591=CARTESIAN_POINT('Ctrl Pts',(0.155342473764606,-0.135496317105764,
0.469744862864871));
#7592=CARTESIAN_POINT('Ctrl Pts',(0.0996750353101687,-0.168438112773147,
0.466039958570945));
#7593=CARTESIAN_POINT('Ctrl Pts',(0.0440075968557312,-0.201379908440531,
0.46233505427702));
#7594=CARTESIAN_POINT('Ctrl Pts',(-0.0296058920949886,-0.20399516479023,
0.458630149983094));
#7595=CARTESIAN_POINT('Ctrl Pts',(-0.0874706722853638,-0.17508681272046,
0.454925245689169));
#7596=CARTESIAN_POINT('Ctrl Pts',(-0.14533545247574,-0.146178460650689,
0.451220341395244));
#7597=CARTESIAN_POINT('Ctrl Pts',(-0.18745152390577,-0.0857465001614493,
0.447515437101318));
#7598=CARTESIAN_POINT('Ctrl Pts',(-0.194541293461784,-0.0214521709129621,
0.443810532807393));
#7599=CARTESIAN_POINT('Ctrl Pts',(-0.195321771015971,-0.014374327205417,
0.443402678275736));
#7600=CARTESIAN_POINT('Ctrl Pts',(-0.195677774776043,-0.00724967654898506,
0.44299482374408));
#7601=CARTESIAN_POINT('Ctrl Pts',(-0.195626364086859,-0.000119838590748017,
0.442586969212423));
#7602=CARTESIAN_POINT('Ctrl Pts',(-0.195647655240959,-0.000106560329145428,
0.43241303078758));
#7603=CARTESIAN_POINT('Ctrl Pts',(-0.195688273475104,-0.00628602257813338,
0.432766621321477));
#7604=CARTESIAN_POINT('Ctrl Pts',(-0.195420885419549,-0.0124619241798928,
0.433120211855374));
#7605=CARTESIAN_POINT('Ctrl Pts',(-0.19483398000204,-0.0186073107818865,
0.433473802389271));
#7606=CARTESIAN_POINT('Ctrl Pts',(-0.188684413786296,-0.0829983705725154,
0.437178706683196));
#7607=CARTESIAN_POINT('Ctrl Pts',(-0.147455848775841,-0.144039266123401,
0.440883610977121));
#7608=CARTESIAN_POINT('Ctrl Pts',(-0.0900196439067171,-0.173790032766202,
0.444588515271047));
#7609=CARTESIAN_POINT('Ctrl Pts',(-0.0325834390375927,-0.203540799409003,
0.448293419564972));
#7610=CARTESIAN_POINT('Ctrl Pts',(0.0410604056902019,-0.202001437143719,
0.451998323858898));
#7611=CARTESIAN_POINT('Ctrl Pts',(0.097203236411656,-0.169876551086573,
0.455703228152823));
#7612=CARTESIAN_POINT('Ctrl Pts',(0.153346067133109,-0.137751665029427,
0.459408132446748));
#7613=CARTESIAN_POINT('Ctrl Pts',(0.191987883848223,-0.0750412551804201,
0.463113036740674));
#7614=CARTESIAN_POINT('Ctrl Pts',(0.195441347863866,-0.0104494652075844,
0.466817941034599));
#7615=CARTESIAN_POINT('Ctrl Pts',(0.19889481187951,0.0541423247652522,0.470522845328524));
#7616=CARTESIAN_POINT('Ctrl Pts',(0.167159923195683,0.120615494861917,0.47422774962245));
#7617=CARTESIAN_POINT('Ctrl Pts',(0.11476254452422,0.158543590700778,0.477932653916375));
#7618=CARTESIAN_POINT('Ctrl Pts',(0.0623651658527581,0.196471686539638,
0.4816375582103));
#7619=CARTESIAN_POINT('Ctrl Pts',(-0.0106947028063393,0.205854708120693,
0.485342462504226));
#7620=CARTESIAN_POINT('Ctrl Pts',(-0.0709757082326437,0.182397808700773,
0.489047366798152));
#7621=CARTESIAN_POINT('Ctrl Pts',(-0.131256713658948,0.158940909280854,
0.492752271092077));
#7622=CARTESIAN_POINT('Ctrl Pts',(-0.17875885585246,0.102644088859959,0.496457175386002));
#7623=CARTESIAN_POINT('Ctrl Pts',(-0.191739200628169,0.0392758287046884,
0.500162079679927));
#7624=CARTESIAN_POINT('Ctrl Pts',(-0.194367979415473,0.026442491766192,
0.500912396715811));
#7625=CARTESIAN_POINT('Ctrl Pts',(-0.195580869792883,0.0133191244610842,
0.501662713751695));
#7626=CARTESIAN_POINT('Ctrl Pts',(-0.19545977166257,0.000173536236839714,
0.502413030787579));
#7627=CARTESIAN_POINT('Origin',(0.,0.,0.));
#7628=CARTESIAN_POINT('',(-0.195080329080103,1.51580434829407E-5,0.582586969212423));
#7629=CARTESIAN_POINT('',(-0.195079254985845,-5.12448512575846E-7,0.57241303078758));
#7630=CARTESIAN_POINT('',(-0.1954,-2.39295984553393E-17,0.));
#7631=CARTESIAN_POINT('Ctrl Pts',(-0.195080329080103,1.51580434829407E-5,
0.582586969212423));
#7632=CARTESIAN_POINT('Ctrl Pts',(-0.195102259420329,0.0317059890063944,
0.580787008604518));
#7633=CARTESIAN_POINT('Ctrl Pts',(-0.187819394734967,0.0633873169979506,
0.578987047996612));
#7634=CARTESIAN_POINT('Ctrl Pts',(-0.173177087283773,0.0911932395442308,
0.577187087388707));
#7635=CARTESIAN_POINT('Ctrl Pts',(-0.14303845674339,0.148426870872502,0.573482183094781));
#7636=CARTESIAN_POINT('Ctrl Pts',(-0.0817200554256732,0.189241561623651,
0.569777278800856));
#7637=CARTESIAN_POINT('Ctrl Pts',(-0.0172888694204259,0.19495539359768,
0.566072374506931));
#7638=CARTESIAN_POINT('Ctrl Pts',(0.0471423165848214,0.200669225571709,
0.562367470213006));
#7639=CARTESIAN_POINT('Ctrl Pts',(0.1146862872776,0.17128219876862,0.55866256591908));
#7640=CARTESIAN_POINT('Ctrl Pts',(0.154426455709376,0.120245500022675,0.554957661625155));
#7641=CARTESIAN_POINT('Ctrl Pts',(0.194166624141151,0.0692088012767304,
0.551252757331229));
#7642=CARTESIAN_POINT('Ctrl Pts',(0.206102990311925,-0.0034775694120695,
0.547547853037304));
#7643=CARTESIAN_POINT('Ctrl Pts',(0.184771976958126,-0.0645432183087307,
0.543842948743378));
#7644=CARTESIAN_POINT('Ctrl Pts',(0.163440963604328,-0.125608867205391,
0.540138044449453));
#7645=CARTESIAN_POINT('Ctrl Pts',(0.10884257072596,-0.175053794309913,0.536433140155528));
#7646=CARTESIAN_POINT('Ctrl Pts',(0.0459678662652951,-0.1902458035534,0.532728235861602));
#7647=CARTESIAN_POINT('Ctrl Pts',(-0.0169068381953713,-0.205437812796887,
0.529023331567677));
#7648=CARTESIAN_POINT('Ctrl Pts',(-0.088057854238333,-0.186376904179337,
0.525318427273751));
#7649=CARTESIAN_POINT('Ctrl Pts',(-0.134917558855844,-0.141787738577927,
0.521613522979826));
#7650=CARTESIAN_POINT('Ctrl Pts',(-0.172973570536371,-0.105575691984742,
0.518604671724025));
#7651=CARTESIAN_POINT('Ctrl Pts',(-0.195008257896402,-0.052526494143854,
0.515595820468224));
#7652=CARTESIAN_POINT('Ctrl Pts',(-0.195488415809582,0.000168817958016994,
0.512586969212423));
#7653=CARTESIAN_POINT('Ctrl Pts',(-0.19545977166257,0.000173536236839714,
0.502413030787579));
#7654=CARTESIAN_POINT('Ctrl Pts',(-0.194982913247146,-0.0515909654461778,
0.505367618045621));
#7655=CARTESIAN_POINT('Ctrl Pts',(-0.173821026745911,-0.103700028070894,
0.508322205303663));
#7656=CARTESIAN_POINT('Ctrl Pts',(-0.136974911436022,-0.139801235384611,
0.511276792561704));
#7657=CARTESIAN_POINT('Ctrl Pts',(-0.0907717301102581,-0.185070339428992,
0.514981696855629));
#7658=CARTESIAN_POINT('Ctrl Pts',(-0.0199068201008233,-0.205168847628107,
0.518686601149554));
#7659=CARTESIAN_POINT('Ctrl Pts',(0.0431831535659995,-0.190897163483548,
0.52239150544348));
#7660=CARTESIAN_POINT('Ctrl Pts',(0.106273127232821,-0.176625479338991,
0.526096409737405));
#7661=CARTESIAN_POINT('Ctrl Pts',(0.161588164557031,-0.127983602850761,
0.529801314031331));
#7662=CARTESIAN_POINT('Ctrl Pts',(0.183809171273742,-0.0672361534713996,
0.533506218325256));
#7663=CARTESIAN_POINT('Ctrl Pts',(0.206030177990453,-0.00648870409203645,
0.537211122619182));
#7664=CARTESIAN_POINT('Ctrl Pts',(0.195157154099664,0.0663643181784591,
0.540916026913107));
#7665=CARTESIAN_POINT('Ctrl Pts',(0.156166958158329,0.117976238953206,0.544620931207032));
#7666=CARTESIAN_POINT('Ctrl Pts',(0.117176762216995,0.169588159727953,0.548325835500957));
#7667=CARTESIAN_POINT('Ctrl Pts',(0.0500693942251149,0.19995897900695,0.552030739794883));
#7668=CARTESIAN_POINT('Ctrl Pts',(-0.014438402988479,0.195187203210435,
0.555735644088809));
#7669=CARTESIAN_POINT('Ctrl Pts',(-0.0789462002020729,0.19041542741392,
0.559440548382734));
#7670=CARTESIAN_POINT('Ctrl Pts',(-0.140854426637381,0.150501056541893,
0.563145452676659));
#7671=CARTESIAN_POINT('Ctrl Pts',(-0.171826118302126,0.0937139095715946,
0.566850356970585));
#7672=CARTESIAN_POINT('Ctrl Pts',(-0.18732678126338,0.0652931686173718,
0.56870458157625));
#7673=CARTESIAN_POINT('Ctrl Pts',(-0.19507850314188,0.0326461576927833,
0.570558806181915));
#7674=CARTESIAN_POINT('Ctrl Pts',(-0.195079266632945,-5.12429904213991E-7,
0.57241303078758));
#7675=CARTESIAN_POINT('Origin',(0.,0.,0.));
#7676=CARTESIAN_POINT('',(-0.195432764861167,-0.000176589099362662,0.652586969212424));
#7677=CARTESIAN_POINT('',(-0.195461653185843,-0.000173273723800459,0.64241303078758));
#7678=CARTESIAN_POINT('',(-0.1954,-2.39295984553393E-17,0.));
#7679=CARTESIAN_POINT('Ctrl Pts',(-0.195432764861167,-0.000176589099362662,
0.652586969212424));
#7680=CARTESIAN_POINT('Ctrl Pts',(-0.19496258822817,0.050717369554878,0.649683101034737));
#7681=CARTESIAN_POINT('Ctrl Pts',(-0.174597076629887,0.101944751897959,
0.646779232857051));
#7682=CARTESIAN_POINT('Ctrl Pts',(-0.138871424621133,0.137917504046295,
0.643875364679364));
#7683=CARTESIAN_POINT('Ctrl Pts',(-0.0932908013175052,0.183813390410141,
0.640170460385439));
#7684=CARTESIAN_POINT('Ctrl Pts',(-0.0227069904956954,0.204877838448089,
0.636465556091513));
#7685=CARTESIAN_POINT('Ctrl Pts',(0.040572009039235,0.19146911652061,0.632760651797588));
#7686=CARTESIAN_POINT('Ctrl Pts',(0.103851008574166,0.178060394593131,0.629055747503662));
#7687=CARTESIAN_POINT('Ctrl Pts',(0.159825196822218,0.130178502700225,0.625350843209737));
#7688=CARTESIAN_POINT('Ctrl Pts',(0.182873769437794,0.0697401960871604,
0.621645938915812));
#7689=CARTESIAN_POINT('Ctrl Pts',(0.205922342053369,0.00930188947409603,
0.617941034621886));
#7690=CARTESIAN_POINT('Ctrl Pts',(0.196045299036468,-0.0636928318591254,
0.614236130327961));
#7691=CARTESIAN_POINT('Ctrl Pts',(0.157763613259938,-0.115832434273962,
0.610531226034036));
#7692=CARTESIAN_POINT('Ctrl Pts',(0.119481927483407,-0.167972036688798,
0.60682632174011));
#7693=CARTESIAN_POINT('Ctrl Pts',(0.0527955989472468,-0.199256520185249,
0.603121417446185));
#7694=CARTESIAN_POINT('Ctrl Pts',(-0.0117713499477233,-0.195366183918996,
0.599416513152259));
#7695=CARTESIAN_POINT('Ctrl Pts',(-0.0763382988426937,-0.191475847652744,
0.595711608858334));
#7696=CARTESIAN_POINT('Ctrl Pts',(-0.138785868096474,-0.152410691623788,
0.592006704564409));
#7697=CARTESIAN_POINT('Ctrl Pts',(-0.170530222841839,-0.0960518276566117,
0.588301800270483));
#7698=CARTESIAN_POINT('Ctrl Pts',(-0.186852158131264,-0.0670738963665755,
0.586396856584463));
#7699=CARTESIAN_POINT('Ctrl Pts',(-0.195057119648206,-0.0335240472493347,
0.584491912898443));
#7700=CARTESIAN_POINT('Ctrl Pts',(-0.195080329080103,1.51580434829407E-5,
0.582586969212423));
#7701=CARTESIAN_POINT('Ctrl Pts',(-0.195079266632945,-5.12429904213991E-7,
0.57241303078758));
#7702=CARTESIAN_POINT('Ctrl Pts',(-0.195080028664364,-0.0325847684584389,
0.57426371047584));
#7703=CARTESIAN_POINT('Ctrl Pts',(-0.187359440633393,-0.0651686849869207,
0.5761143901641));
#7704=CARTESIAN_POINT('Ctrl Pts',(-0.17191549678333,-0.0935498463051126,
0.577965069852361));
#7705=CARTESIAN_POINT('Ctrl Pts',(-0.140998026705607,-0.150366532142949,
0.581669974146286));
#7706=CARTESIAN_POINT('Ctrl Pts',(-0.0791279296559783,-0.190339980750052,
0.585374878440212));
#7707=CARTESIAN_POINT('Ctrl Pts',(-0.0146247168406994,-0.195173331772808,
0.589079782734137));
#7708=CARTESIAN_POINT('Ctrl Pts',(0.0498784959745796,-0.200006682795564,
0.592784687028062));
#7709=CARTESIAN_POINT('Ctrl Pts',(0.11701482455551,-0.169699936233974,0.596489591321988));
#7710=CARTESIAN_POINT('Ctrl Pts',(0.156054270077791,-0.118125257961442,
0.600194495615913));
#7711=CARTESIAN_POINT('Ctrl Pts',(0.195093715600072,-0.0665505796889094,
0.603899399909839));
#7712=CARTESIAN_POINT('Ctrl Pts',(0.206036278063704,0.00629203029456468,
0.607604304203764));
#7713=CARTESIAN_POINT('Ctrl Pts',(0.183873269344836,0.0670606635697158,
0.611309208497689));
#7714=CARTESIAN_POINT('Ctrl Pts',(0.161710260625969,0.127829296844866,0.615014112791615));
#7715=CARTESIAN_POINT('Ctrl Pts',(0.106441680724601,0.176523953411694,0.61871901708554));
#7716=CARTESIAN_POINT('Ctrl Pts',(0.0433653591659573,0.190855855038238,
0.622423921379465));
#7717=CARTESIAN_POINT('Ctrl Pts',(-0.0197109623926868,0.205187756664782,
0.626128825673391));
#7718=CARTESIAN_POINT('Ctrl Pts',(-0.0905950256086064,0.185156903351043,
0.629833729967317));
#7719=CARTESIAN_POINT('Ctrl Pts',(-0.136841398547571,0.139931924240018,
0.633538634261242));
#7720=CARTESIAN_POINT('Ctrl Pts',(-0.173766207647965,0.103822633627155,
0.636496766436688));
#7721=CARTESIAN_POINT('Ctrl Pts',(-0.194984453966749,0.0516520517928096,
0.639454898612134));
#7722=CARTESIAN_POINT('Ctrl Pts',(-0.195461653185843,-0.000173273723800459,
0.64241303078758));
#7723=CARTESIAN_POINT('Origin',(0.,0.,0.));
#7724=CARTESIAN_POINT('',(-0.195665606136028,9.31787759667347E-5,0.722586969212424));
#7725=CARTESIAN_POINT('',(-0.195646327283704,0.000107461668706292,0.712413030787581));
#7726=CARTESIAN_POINT('',(-0.1954,-2.39295984553393E-17,0.));
#7727=CARTESIAN_POINT('Ctrl Pts',(-0.195665606136028,9.31787759667347E-5,
0.722586969212424));
#7728=CARTESIAN_POINT('Ctrl Pts',(-0.195696782701144,0.0053849756768864,
0.722284097758882));
#7729=CARTESIAN_POINT('Ctrl Pts',(-0.1955007119948,0.0106744267763307,0.72198122630534));
#7730=CARTESIAN_POINT('Ctrl Pts',(-0.19506992917185,0.0159446928961413,
0.721678354851798));
#7731=CARTESIAN_POINT('Ctrl Pts',(-0.189800336703391,0.0804137319853543,
0.717973450557872));
#7732=CARTESIAN_POINT('Ctrl Pts',(-0.149409263832838,0.142011999441816,
0.714268546263947));
#7733=CARTESIAN_POINT('Ctrl Pts',(-0.0923847281217706,0.172544407352221,
0.710563641970021));
#7734=CARTESIAN_POINT('Ctrl Pts',(-0.0353601924107021,0.203076815262627,
0.706858737676096));
#7735=CARTESIAN_POINT('Ctrl Pts',(0.0382978061408807,0.202543363626974,
0.70315383338217));
#7736=CARTESIAN_POINT('Ctrl Pts',(0.0948741351041633,0.171188226776551,
0.699448929088245));
#7737=CARTESIAN_POINT('Ctrl Pts',(0.151450464067444,0.139833089926128,0.695744024794319));
#7738=CARTESIAN_POINT('Ctrl Pts',(0.190945123442426,0.0776562678609379,
0.692039120500394));
#7739=CARTESIAN_POINT('Ctrl Pts',(0.195280406839545,0.0131176675992589,
0.688334216206469));
#7740=CARTESIAN_POINT('Ctrl Pts',(0.199615690236664,-0.0514209326624214,
0.684629311912544));
#7741=CARTESIAN_POINT('Ctrl Pts',(0.168791597655919,-0.118321311120591,
0.680924407618618));
#7742=CARTESIAN_POINT('Ctrl Pts',(0.116917097353215,-0.156961469301105,
0.677219503324692));
#7743=CARTESIAN_POINT('Ctrl Pts',(0.0650425970505132,-0.195601627481618,
0.673514599030767));
#7744=CARTESIAN_POINT('Ctrl Pts',(-0.0078823109741457,-0.205981565384478,
0.669809694736841));
#7745=CARTESIAN_POINT('Ctrl Pts',(-0.0684780484026163,-0.183350122404191,
0.666104790442916));
#7746=CARTESIAN_POINT('Ctrl Pts',(-0.129073785831088,-0.160718679423904,
0.662399886148991));
#7747=CARTESIAN_POINT('Ctrl Pts',(-0.17734035266337,-0.105075855560469,
0.658694981855066));
#7748=CARTESIAN_POINT('Ctrl Pts',(-0.191184918186788,-0.0418907812838809,
0.65499007756114));
#7749=CARTESIAN_POINT('Ctrl Pts',(-0.194178247060648,-0.0282295575416714,
0.654189041444902));
#7750=CARTESIAN_POINT('Ctrl Pts',(-0.195562463745895,-0.0142157590911969,
0.653388005328663));
#7751=CARTESIAN_POINT('Ctrl Pts',(-0.195432764861167,-0.000176589099362662,
0.652586969212424));
#7752=CARTESIAN_POINT('Ctrl Pts',(-0.195461653185843,-0.000173273723800459,
0.64241303078758));
#7753=CARTESIAN_POINT('Ctrl Pts',(-0.195582120781827,-0.0132564308755209,
0.643159802906059));
#7754=CARTESIAN_POINT('Ctrl Pts',(-0.194380770210329,-0.026317584988001,
0.643906575024539));
#7755=CARTESIAN_POINT('Ctrl Pts',(-0.19177660491574,-0.0390927817501061,
0.644653347143018));
#7756=CARTESIAN_POINT('Ctrl Pts',(-0.178856755682938,-0.102473403720895,
0.648358251436943));
#7757=CARTESIAN_POINT('Ctrl Pts',(-0.131408374555326,-0.158815542754161,
0.652063155730869));
#7758=CARTESIAN_POINT('Ctrl Pts',(-0.0711497879157472,-0.182329974106052,
0.655768060024794));
#7759=CARTESIAN_POINT('Ctrl Pts',(-0.0108912012761686,-0.205844405457942,
0.65947296431872));
#7760=CARTESIAN_POINT('Ctrl Pts',(0.0621775908753766,-0.196531129128456,
0.663177868612645));
#7761=CARTESIAN_POINT('Ctrl Pts',(0.114611150809846,-0.158653067691778,
0.66688277290657));
#7762=CARTESIAN_POINT('Ctrl Pts',(0.167044710744316,-0.1207750062551,0.670587677200496));
#7763=CARTESIAN_POINT('Ctrl Pts',(0.19884303846171,-0.0543321597112302,
0.674292581494421));
#7764=CARTESIAN_POINT('Ctrl Pts',(0.195451233596986,0.0102628974167111,
0.677997485788347));
#7765=CARTESIAN_POINT('Ctrl Pts',(0.192059428732261,0.0748579545446525,
0.681702390082272));
#7766=CARTESIAN_POINT('Ctrl Pts',(0.153477491285418,0.137605222256665,0.685407294376197));
#7767=CARTESIAN_POINT('Ctrl Pts',(0.0973653516911611,0.16978368610684,0.689112198670123));
#7768=CARTESIAN_POINT('Ctrl Pts',(0.0412532120969042,0.201962149957014,
0.692817102964048));
#7769=CARTESIAN_POINT('Ctrl Pts',(-0.0323891296447666,0.203571809945351,
0.696522007257973));
#7770=CARTESIAN_POINT('Ctrl Pts',(-0.089853707623677,0.173875883906447,
0.700226911551899));
#7771=CARTESIAN_POINT('Ctrl Pts',(-0.147318285602587,0.144179957867542,
0.703931815845824));
#7772=CARTESIAN_POINT('Ctrl Pts',(-0.188605099818737,0.0831784458013958,
0.70763672013975));
#7773=CARTESIAN_POINT('Ctrl Pts',(-0.194816129198604,0.0187932855574017,
0.711341624433676));
#7774=CARTESIAN_POINT('Ctrl Pts',(-0.195414843390564,0.0125868571488267,
0.711698759884977));
#7775=CARTESIAN_POINT('Ctrl Pts',(-0.195687631335538,0.00634898768321266,
0.712055895336279));
#7776=CARTESIAN_POINT('Ctrl Pts',(-0.195646327283704,0.000107461668706292,
0.712413030787581));
#7777=CARTESIAN_POINT('Origin',(0.,0.,0.));
#7778=CARTESIAN_POINT('',(-0.195153751526609,0.000118248258768078,0.792586969212424));
#7779=CARTESIAN_POINT('',(-0.195137151677628,0.000105948740446043,0.78241303078758));
#7780=CARTESIAN_POINT('',(-0.1954,-2.39295984553393E-17,0.));
#7781=CARTESIAN_POINT('Ctrl Pts',(-0.195153751526609,0.000118248258768078,
0.792586969212424));
#7782=CARTESIAN_POINT('Ctrl Pts',(-0.195290424219172,0.0248632703434088,
0.7911801901891));
#7783=CARTESIAN_POINT('Ctrl Pts',(-0.190927662847405,0.0495618887102773,
0.789773411165777));
#7784=CARTESIAN_POINT('Ctrl Pts',(-0.181844484105553,0.0723815867403318,
0.788366632142454));
#7785=CARTESIAN_POINT('Ctrl Pts',(-0.157922953171942,0.132479722848387,
0.784661727848529));
#7786=CARTESIAN_POINT('Ctrl Pts',(-0.101261124890318,0.179545873498893,
0.780956823554603));
#7787=CARTESIAN_POINT('Ctrl Pts',(-0.0377945538744258,0.192036668884086,
0.777251919260678));
#7788=CARTESIAN_POINT('Ctrl Pts',(0.0256720171414684,0.204527464269279,
0.773547014966752));
#7789=CARTESIAN_POINT('Ctrl Pts',(0.0959433308916326,0.182442904389159,
0.769842110672827));
#7790=CARTESIAN_POINT('Ctrl Pts',(0.140854426399365,0.135891651923026,0.766137206378902));
#7791=CARTESIAN_POINT('Ctrl Pts',(0.185765521907095,0.0893403994568938,
0.762432302084977));
#7792=CARTESIAN_POINT('Ctrl Pts',(0.205316399172396,0.0183224544047523,
0.758727397791051));
#7793=CARTESIAN_POINT('Ctrl Pts',(0.190558126252222,-0.04465547019017,0.755022493497126));
#7794=CARTESIAN_POINT('Ctrl Pts',(0.175799853332047,-0.107633394785094,
0.7513175892032));
#7795=CARTESIAN_POINT('Ctrl Pts',(0.126732430226394,-0.162571298922797,
0.747612684909275));
#7796=CARTESIAN_POINT('Ctrl Pts',(0.065815259857937,-0.184322711754398,
0.74390778061535));
#7797=CARTESIAN_POINT('Ctrl Pts',(0.00489808948948139,-0.206074124586,0.740202876321424));
#7798=CARTESIAN_POINT('Ctrl Pts',(-0.0678688281417779,-0.194639046111501,
0.736497972027499));
#7799=CARTESIAN_POINT('Ctrl Pts',(-0.119178230924225,-0.155251601513269,
0.732793067733573));
#7800=CARTESIAN_POINT('Ctrl Pts',(-0.166293151968891,-0.119084032963209,
0.72939103489319));
#7801=CARTESIAN_POINT('Ctrl Pts',(-0.195315412358655,-0.0593474407707721,
0.725989002052807));
#7802=CARTESIAN_POINT('Ctrl Pts',(-0.195665606136028,9.31787759667347E-5,
0.722586969212424));
#7803=CARTESIAN_POINT('Ctrl Pts',(-0.195646327283704,0.000107461668706292,
0.712413030787581));
#7804=CARTESIAN_POINT('Ctrl Pts',(-0.19525914528511,-0.0584002732694843,
0.715760799630204));
#7805=CARTESIAN_POINT('Ctrl Pts',(-0.167272421555789,-0.117229312394887,
0.719108568472827));
#7806=CARTESIAN_POINT('Ctrl Pts',(-0.121433992833904,-0.153493638833617,
0.722456337315451));
#7807=CARTESIAN_POINT('Ctrl Pts',(-0.0707055825457531,-0.193626594558799,
0.726161241609376));
#7808=CARTESIAN_POINT('Ctrl Pts',(0.00188648257413163,-0.206123697587321,
0.729866145903302));
#7809=CARTESIAN_POINT('Ctrl Pts',(0.0631149748393498,-0.185264707186764,
0.733571050197227));
#7810=CARTESIAN_POINT('Ctrl Pts',(0.124343467104567,-0.164405716786208,
0.737275954491153));
#7811=CARTESIAN_POINT('Ctrl Pts',(0.174208386515118,-0.110190632956576,
0.740980858785078));
#7812=CARTESIAN_POINT('Ctrl Pts',(0.189885295881042,-0.0474350733754927,
0.744685763079003));
#7813=CARTESIAN_POINT('Ctrl Pts',(0.205562205246967,0.0153204862055921,
0.748390667372929));
#7814=CARTESIAN_POINT('Ctrl Pts',(0.187051104568262,0.0866165215381275,
0.752095571666854));
#7815=CARTESIAN_POINT('Ctrl Pts',(0.142824993696378,0.133819030610743,0.75580047596078));
#7816=CARTESIAN_POINT('Ctrl Pts',(0.0985988828244949,0.181021539683357,
0.759505380254705));
#7817=CARTESIAN_POINT('Ctrl Pts',(0.0286577617594329,0.204130522496052,
0.76321028454863));
#7818=CARTESIAN_POINT('Ctrl Pts',(-0.0349845460811521,0.192568412034438,
0.766915188842556));
#7819=CARTESIAN_POINT('Ctrl Pts',(-0.0986268539217371,0.181006301572824,
0.770620093136481));
#7820=CARTESIAN_POINT('Ctrl Pts',(-0.155970348537846,0.1347730978369,0.774324997430407));
#7821=CARTESIAN_POINT('Ctrl Pts',(-0.180767459361033,0.0750309097247715,
0.778029901724332));
#7822=CARTESIAN_POINT('Ctrl Pts',(-0.190546293802352,0.0514713518844925,
0.779490944745415));
#7823=CARTESIAN_POINT('Ctrl Pts',(-0.195263680442012,0.025810945614826,
0.780951987766498));
#7824=CARTESIAN_POINT('Ctrl Pts',(-0.195137151677628,0.000105948740446043,
0.78241303078758));
#7825=CARTESIAN_POINT('Origin',(0.,0.,0.));
#7826=CARTESIAN_POINT('',(-0.195235475305001,-0.000156905063299573,0.862586969212423));
#7827=CARTESIAN_POINT('',(-0.195259979386646,-0.000163936101596873,0.85241303078758));
#7828=CARTESIAN_POINT('',(-0.1954,-2.39295984553393E-17,0.));
#7829=CARTESIAN_POINT('Ctrl Pts',(-0.195235475305001,-0.000156905063299573,
0.862586969212423));
#7830=CARTESIAN_POINT('Ctrl Pts',(-0.194902940139162,0.0439592076248328,
0.860076282619319));
#7831=CARTESIAN_POINT('Ctrl Pts',(-0.18009730434855,0.0882774316754031,
0.857565596026215));
#7832=CARTESIAN_POINT('Ctrl Pts',(-0.152668645933159,0.122469567842785,
0.855054909433111));
#7833=CARTESIAN_POINT('Ctrl Pts',(-0.112193441015542,0.172925324627786,
0.851350005139186));
#7834=CARTESIAN_POINT('Ctrl Pts',(-0.0442309197344043,0.201330975868051,
0.84764510084526));
#7835=CARTESIAN_POINT('Ctrl Pts',(0.0201107497513655,0.194684535192451,
0.843940196551335));
#7836=CARTESIAN_POINT('Ctrl Pts',(0.0844524192371344,0.188038094516851,
0.84023529225741));
#7837=CARTESIAN_POINT('Ctrl Pts',(0.145173236927535,0.14633956192539,0.836530387963485));
#7838=CARTESIAN_POINT('Ctrl Pts',(0.174479745901743,0.0886754124248997,
0.832825483669559));
#7839=CARTESIAN_POINT('Ctrl Pts',(0.203786254875951,0.0310112629244105,
0.829120579375634));
#7840=CARTESIAN_POINT('Ctrl Pts',(0.201678455133965,-0.0426185034851084,
0.825415675081708));
#7841=CARTESIAN_POINT('Ctrl Pts',(0.169121140029283,-0.0985116769416633,
0.821710770787783));
#7842=CARTESIAN_POINT('Ctrl Pts',(0.136563824924599,-0.15440485039822,0.818005866493857));
#7843=CARTESIAN_POINT('Ctrl Pts',(0.0735569944572206,-0.192561430901813,
0.814300962199932));
#7844=CARTESIAN_POINT('Ctrl Pts',(0.00894047152349694,-0.195516184669199,
0.810596057906007));
#7845=CARTESIAN_POINT('Ctrl Pts',(-0.0556760514102258,-0.198470938436586,
0.806891153612081));
#7846=CARTESIAN_POINT('Ctrl Pts',(-0.121902266810292,-0.166223865467764,
0.803186249318156));
#7847=CARTESIAN_POINT('Ctrl Pts',(-0.159424757717526,-0.11353526820055,
0.799481345024231));
#7848=CARTESIAN_POINT('Ctrl Pts',(-0.182699686765289,-0.0808529133416383,
0.797183219753628));
#7849=CARTESIAN_POINT('Ctrl Pts',(-0.194930481941712,-0.0403054143289745,
0.794885094483026));
#7850=CARTESIAN_POINT('Ctrl Pts',(-0.195153751526609,0.000118248258768078,
0.792586969212424));
#7851=CARTESIAN_POINT('Ctrl Pts',(-0.195137151677628,0.000105948740446043,
0.78241303078758));
#7852=CARTESIAN_POINT('Ctrl Pts',(-0.194942829545969,-0.0393716341730415,
0.784656892060423));
#7853=CARTESIAN_POINT('Ctrl Pts',(-0.183323340652406,-0.0789543913210836,
0.786900753333265));
#7854=CARTESIAN_POINT('Ctrl Pts',(-0.161066679056451,-0.111193689909524,
0.789144614606108));
#7855=CARTESIAN_POINT('Ctrl Pts',(-0.124318060898417,-0.164424928943361,
0.792849518900033));
#7856=CARTESIAN_POINT('Ctrl Pts',(-0.0585700975520817,-0.197636234522699,
0.796554423193959));
#7857=CARTESIAN_POINT('Ctrl Pts',(0.00608270210726663,-0.195625950510262,
0.800259327487884));
#7858=CARTESIAN_POINT('Ctrl Pts',(0.070735501766615,-0.193615666497825,
0.80396423178181));
#7859=CARTESIAN_POINT('Ctrl Pts',(0.134293137738976,-0.156383792893612,
0.807669136075735));
#7860=CARTESIAN_POINT('Ctrl Pts',(0.167663669490968,-0.100972301700975,
0.811374040369661));
#7861=CARTESIAN_POINT('Ctrl Pts',(0.20103420124296,-0.0455608105083384,
0.815078944663586));
#7862=CARTESIAN_POINT('Ctrl Pts',(0.204217628774584,0.0280302982727214,
0.818783848957511));
#7863=CARTESIAN_POINT('Ctrl Pts',(0.175756816636647,0.0861165093563451,
0.822488753251437));
#7864=CARTESIAN_POINT('Ctrl Pts',(0.147296004498709,0.14420272043997,0.826193657545363));
#7865=CARTESIAN_POINT('Ctrl Pts',(0.0871909526912083,0.186784033826158,
0.829898561839288));
#7866=CARTESIAN_POINT('Ctrl Pts',(0.022953266486877,0.194369903368684,0.833603466133213));
#7867=CARTESIAN_POINT('Ctrl Pts',(-0.0412844197174542,0.201955772911211,
0.837308370427139));
#7868=CARTESIAN_POINT('Ctrl Pts',(-0.109654740318616,0.174546198610077,
0.841013274721063));
#7869=CARTESIAN_POINT('Ctrl Pts',(-0.150862867075323,0.124687237180806,
0.844718179014989));
#7870=CARTESIAN_POINT('Ctrl Pts',(-0.179391757618137,0.0901692679076088,
0.847283129605853));
#7871=CARTESIAN_POINT('Ctrl Pts',(-0.194901910843352,0.0448913918449987,
0.849848080196716));
#7872=CARTESIAN_POINT('Ctrl Pts',(-0.195259979386646,-0.000163936101596873,
0.85241303078758));
#7873=CARTESIAN_POINT('Origin',(0.,0.,0.));
#7874=CARTESIAN_POINT('',(-0.195715067010162,-2.931307771456E-5,0.932586969212424));
#7875=CARTESIAN_POINT('',(-0.195719607651052,-1.17545938899131E-5,0.922413030787581));
#7876=CARTESIAN_POINT('',(-0.1954,-2.39295984553393E-17,0.));
#7877=CARTESIAN_POINT('Ctrl Pts',(-0.195715067010162,-2.931307771456E-5,
0.932586969212424));
#7878=CARTESIAN_POINT('Ctrl Pts',(-0.195582961786627,0.0630827139603783,
0.928972375049538));
#7879=CARTESIAN_POINT('Ctrl Pts',(-0.162276589664832,0.126314497964337,
0.925357780886653));
#7880=CARTESIAN_POINT('Ctrl Pts',(-0.110101557926667,0.161815195333392,
0.921743186723768));
#7881=CARTESIAN_POINT('Ctrl Pts',(-0.0566229402972577,0.19820287267501,
0.918038282429843));
#7882=CARTESIAN_POINT('Ctrl Pts',(0.0166789772399235,0.205456437773955,
0.914333378135918));
#7883=CARTESIAN_POINT('Ctrl Pts',(0.076252049559439,0.180255750079291,0.910628473841992));
#7884=CARTESIAN_POINT('Ctrl Pts',(0.135825121878954,0.155055062384626,0.906923569548067));
#7885=CARTESIAN_POINT('Ctrl Pts',(0.181669348980803,0.0974001218963517,
0.903218665254141));
#7886=CARTESIAN_POINT('Ctrl Pts',(0.192800666428956,0.0336810558506326,
0.899513760960216));
#7887=CARTESIAN_POINT('Ctrl Pts',(0.203931983877108,-0.0300380101950847,
0.895808856666291));
#7888=CARTESIAN_POINT('Ctrl Pts',(0.180350391671563,-0.0998212017982479,
0.892103952372366));
#7889=CARTESIAN_POINT('Ctrl Pts',(0.13284978212173,-0.143726983857839,0.88839904807844));
#7890=CARTESIAN_POINT('Ctrl Pts',(0.0853491725718961,-0.187632765917432,
0.884694143784515));
#7891=CARTESIAN_POINT('Ctrl Pts',(0.013929545677772,-0.205661138433453,
0.880989239490589));
#7892=CARTESIAN_POINT('Ctrl Pts',(-0.048718525559727,-0.189560058466833,
0.877284335196664));
#7893=CARTESIAN_POINT('Ctrl Pts',(-0.111366596797226,-0.173458978500212,
0.873579430902738));
#7894=CARTESIAN_POINT('Ctrl Pts',(-0.165243112378099,-0.123228446050951,
0.869874526608813));
#7895=CARTESIAN_POINT('Ctrl Pts',(-0.185687425891486,-0.0618602486614515,
0.866169622314888));
#7896=CARTESIAN_POINT('Ctrl Pts',(-0.192277329203931,-0.0420791742325638,
0.864975404614066));
#7897=CARTESIAN_POINT('Ctrl Pts',(-0.195393646931154,-0.0211409031490452,
0.863781186913245));
#7898=CARTESIAN_POINT('Ctrl Pts',(-0.195235475305001,-0.000156905063299573,
0.862586969212423));
#7899=CARTESIAN_POINT('Ctrl Pts',(-0.195259979386646,-0.000163936101596873,
0.85241303078758));
#7900=CARTESIAN_POINT('Ctrl Pts',(-0.19541911756394,-0.0201880987963234,
0.853552984490642));
#7901=CARTESIAN_POINT('Ctrl Pts',(-0.192585379153193,-0.0401683032463519,
0.854692938193704));
#7902=CARTESIAN_POINT('Ctrl Pts',(-0.186571486394569,-0.0591404450650352,
0.855832891896766));
#7903=CARTESIAN_POINT('Ctrl Pts',(-0.167026046044856,-0.120800817324193,
0.859537796190691));
#7904=CARTESIAN_POINT('Ctrl Pts',(-0.11388923243318,-0.171813213285104,
0.863242700484616));
#7905=CARTESIAN_POINT('Ctrl Pts',(-0.0514831116350698,-0.188827966663681,
0.866947604778541));
#7906=CARTESIAN_POINT('Ctrl Pts',(0.0109230091630432,-0.205842720042259,
0.870652509072467));
#7907=CARTESIAN_POINT('Ctrl Pts',(0.0825984371475908,-0.188859830838501,
0.874357413366393));
#7908=CARTESIAN_POINT('Ctrl Pts',(0.130735512676577,-0.145652797786935,
0.878062317660318));
#7909=CARTESIAN_POINT('Ctrl Pts',(0.178872588205563,-0.10244576473537,0.881767221954244));
#7910=CARTESIAN_POINT('Ctrl Pts',(0.203471311278988,-0.0330145878359957,
0.885472126248168));
#7911=CARTESIAN_POINT('Ctrl Pts',(0.193272223015147,0.0308603238601364,
0.889177030542094));
#7912=CARTESIAN_POINT('Ctrl Pts',(0.183073134751306,0.0947352355562703,
0.892881934836019));
#7913=CARTESIAN_POINT('Ctrl Pts',(0.138076235150198,0.153053882049163,0.896586839129945));
#7914=CARTESIAN_POINT('Ctrl Pts',(0.0788777453795076,0.179122341046043,
0.900291743423871));
#7915=CARTESIAN_POINT('Ctrl Pts',(0.0196792556088182,0.205190800042922,
0.903996647717796));
#7916=CARTESIAN_POINT('Ctrl Pts',(-0.0537208243314517,0.199009071543789,
0.907701552011721));
#7917=CARTESIAN_POINT('Ctrl Pts',(-0.107725417896538,0.163406689327535,
0.911406456305646));
#7918=CARTESIAN_POINT('Ctrl Pts',(-0.161204584453802,0.128150693444819,
0.915075314466291));
#7919=CARTESIAN_POINT('Ctrl Pts',(-0.195663837766578,0.0640437437643291,
0.918744172626936));
#7920=CARTESIAN_POINT('Ctrl Pts',(-0.195719607651052,-1.17545938899131E-5,
0.922413030787581));
#7921=CARTESIAN_POINT('Origin',(0.,0.,0.));
#7922=CARTESIAN_POINT('',(-0.195321337055717,0.000175186119862003,1.00258696921242));
#7923=CARTESIAN_POINT('',(-0.195294337528581,0.000171262189333537,0.99241303078758));
#7924=CARTESIAN_POINT('',(-0.1954,-2.39295984553393E-17,0.));
#7925=CARTESIAN_POINT('Ctrl Pts',(-0.195321337055717,0.000175186119862003,
1.00258696921242));
#7926=CARTESIAN_POINT('Ctrl Pts',(-0.195476146868043,0.0179656372844682,
1.00157337177368));
#7927=CARTESIAN_POINT('Ctrl Pts',(-0.193245700725841,0.0357179689540282,
1.00055977433494));
#7928=CARTESIAN_POINT('Ctrl Pts',(-0.188475369241895,0.0527593184925091,
0.999546176896202));
#7929=CARTESIAN_POINT('Ctrl Pts',(-0.171038839784721,0.115048908685087,
0.995841272602277));
#7930=CARTESIAN_POINT('Ctrl Pts',(-0.119668151355893,0.167839416275189,
0.992136368308351));
#7931=CARTESIAN_POINT('Ctrl Pts',(-0.0578769697811842,0.186967288228745,
0.988431464014425));
#7932=CARTESIAN_POINT('Ctrl Pts',(0.00391421179352416,0.206095160182302,
0.9847265597205));
#7933=CARTESIAN_POINT('Ctrl Pts',(0.0761258865141124,0.191560396499312,
0.981021655426575));
#7934=CARTESIAN_POINT('Ctrl Pts',(0.125704941019021,0.150015926828012,0.977316751132649));
#7935=CARTESIAN_POINT('Ctrl Pts',(0.175283995523929,0.108471457156712,0.973611846838724));
#7936=CARTESIAN_POINT('Ctrl Pts',(0.202230429813157,0.0399172814971016,
0.969906942544799));
#7937=CARTESIAN_POINT('Ctrl Pts',(0.194210178090586,-0.0242676167903992,
0.966202038250873));
#7938=CARTESIAN_POINT('Ctrl Pts',(0.186189926368015,-0.0884525150779,0.962497133956948));
#7939=CARTESIAN_POINT('Ctrl Pts',(0.143202988633645,-0.148268135993291,
0.958792229663022));
#7940=CARTESIAN_POINT('Ctrl Pts',(0.084925575576374,-0.176335354117331,
0.955087325369097));
#7941=CARTESIAN_POINT('Ctrl Pts',(0.0266481625191027,-0.20440257224137,
0.951382421075171));
#7942=CARTESIAN_POINT('Ctrl Pts',(-0.0469197258610698,-0.200721387574058,
0.947677516781246));
#7943=CARTESIAN_POINT('Ctrl Pts',(-0.102104202844174,-0.166976771618745,
0.943972612487321));
#7944=CARTESIAN_POINT('Ctrl Pts',(-0.157288679827278,-0.133232155663433,
0.940267708193395));
#7945=CARTESIAN_POINT('Ctrl Pts',(-0.194089745413313,-0.0694241084201192,
0.93656280389947));
#7946=CARTESIAN_POINT('Ctrl Pts',(-0.195662619345512,-0.00475919000631662,
0.932857899605544));
#7947=CARTESIAN_POINT('Ctrl Pts',(-0.195700959458955,-0.00318292870714216,
0.932767589474504));
#7948=CARTESIAN_POINT('Ctrl Pts',(-0.195718367640748,-0.0016061582711675,
0.932677279343464));
#7949=CARTESIAN_POINT('Ctrl Pts',(-0.195715067010162,-2.931307771456E-5,
0.932586969212424));
#7950=CARTESIAN_POINT('Ctrl Pts',(-0.195719607651052,-1.17545938899131E-5,
0.922413030787581));
#7951=CARTESIAN_POINT('Ctrl Pts',(-0.195720155584114,-0.000641092913902824,
0.922449076920861));
#7952=CARTESIAN_POINT('Ctrl Pts',(-0.195717382600782,-0.00127042626739718,
0.922485123054142));
#7953=CARTESIAN_POINT('Ctrl Pts',(-0.195711274111555,-0.00189972724385319,
0.922521169187423));
#7954=CARTESIAN_POINT('Ctrl Pts',(-0.195083429571586,-0.0665807256656151,
0.926226073481348));
#7955=CARTESIAN_POINT('Ctrl Pts',(-0.159218633301743,-0.130919686575766,
0.929930977775273));
#7956=CARTESIAN_POINT('Ctrl Pts',(-0.104533111367734,-0.165467037218143,
0.933635882069199));
#7957=CARTESIAN_POINT('Ctrl Pts',(-0.0498475894337254,-0.20001438786052,
0.937340786363124));
#7958=CARTESIAN_POINT('Ctrl Pts',(0.0236586581644487,-0.204770128235125,
0.94104569065705));
#7959=CARTESIAN_POINT('Ctrl Pts',(0.0823399592547179,-0.177557435462165,
0.944750594950975));
#7960=CARTESIAN_POINT('Ctrl Pts',(0.141021260344988,-0.150344742689204,
0.9484554992449));
#7961=CARTESIAN_POINT('Ctrl Pts',(0.184877614927351,-0.091163616768676,
0.952160403538825));
#7962=CARTESIAN_POINT('Ctrl Pts',(0.193834858190581,-0.0271027586825891,
0.955865307832751));
#7963=CARTESIAN_POINT('Ctrl Pts',(0.202792101453811,0.0369580994034978,
0.959570212126676));
#7964=CARTESIAN_POINT('Ctrl Pts',(0.17685023339791,0.105898689655145,0.963275116420602));
#7965=CARTESIAN_POINT('Ctrl Pts',(0.12788350439832,0.14816315696142,0.966980020714527));
#7966=CARTESIAN_POINT('Ctrl Pts',(0.0789167753987302,0.190427624267694,
0.970684925008453));
#7967=CARTESIAN_POINT('Ctrl Pts',(0.00692518545545543,0.206015968628597,
0.974389829302378));
#7968=CARTESIAN_POINT('Ctrl Pts',(-0.0551388904494672,0.187793009821907,
0.978094733596303));
#7969=CARTESIAN_POINT('Ctrl Pts',(-0.11720296635439,0.169570051015217,0.981799637890228));
#7970=CARTESIAN_POINT('Ctrl Pts',(-0.169339528220959,0.117535789040932,
0.985504542184154));
#7971=CARTESIAN_POINT('Ctrl Pts',(-0.187684350543733,0.0555076241515194,
0.98920944647808));
#7972=CARTESIAN_POINT('Ctrl Pts',(-0.192971863192861,0.0376292985572852,
0.99027730791458));
#7973=CARTESIAN_POINT('Ctrl Pts',(-0.195452091727079,0.0189207190229355,
0.99134516935108));
#7974=CARTESIAN_POINT('Ctrl Pts',(-0.195294337528581,0.000171262189333537,
0.99241303078758));
#7975=CARTESIAN_POINT('Origin',(0.,0.,0.));
#7976=CARTESIAN_POINT('',(-0.195106169435837,-7.43721989362317E-5,1.07258696921242));
#7977=CARTESIAN_POINT('',(-0.195118116536412,-8.83829588442778E-5,1.06241303078758));
#7978=CARTESIAN_POINT('',(-0.1954,-2.39295984553393E-17,0.));
#7979=CARTESIAN_POINT('Ctrl Pts',(-0.195106169435837,-7.43721989362317E-5,
1.07258696921242));
#7980=CARTESIAN_POINT('Ctrl Pts',(-0.194978635044518,0.037194947633429,
1.0704694642039));
#7981=CARTESIAN_POINT('Ctrl Pts',(-0.184712313824149,0.0745293372596056,
1.06835195919538));
#7982=CARTESIAN_POINT('Ctrl Pts',(-0.164756101436382,0.105650071169628,
1.06623445418686));
#7983=CARTESIAN_POINT('Ctrl Pts',(-0.129839604583541,0.160100634558776,
1.06252954989293));
#7984=CARTESIAN_POINT('Ctrl Pts',(-0.0652594983148889,0.195529368597717,
1.05882464559901));
#7985=CARTESIAN_POINT('Ctrl Pts',(-0.000575733727790552,0.195719643953635,
1.05511974130508));
#7986=CARTESIAN_POINT('Ctrl Pts',(0.0641080308593078,0.195909919309552,
1.05141483701116));
#7987=CARTESIAN_POINT('Ctrl Pts',(0.128895453764853,0.160861735982445,1.04770993271723));
#7988=CARTESIAN_POINT('Ctrl Pts',(0.164131689813376,0.106617535601179,1.04400502842331));
#7989=CARTESIAN_POINT('Ctrl Pts',(0.199367925861899,0.0523733352199126,
1.04030012412938));
#7990=CARTESIAN_POINT('Ctrl Pts',(0.205052975053401,-0.0210668822155132,
1.03659521983546));
#7991=CARTESIAN_POINT('Ctrl Pts',(0.178584646313934,-0.0800876682117171,
1.03289031554153));
#7992=CARTESIAN_POINT('Ctrl Pts',(0.152116317574466,-0.13910845420792,1.0291854112476));
#7993=CARTESIAN_POINT('Ctrl Pts',(0.0934946109040307,-0.183709808764902,
1.02548050695368));
#7994=CARTESIAN_POINT('Ctrl Pts',(0.0295521669181964,-0.193476561704776,
1.02177560265975));
#7995=CARTESIAN_POINT('Ctrl Pts',(-0.0343902770676398,-0.20324331464465,
1.01807069836583));
#7996=CARTESIAN_POINT('Ctrl Pts',(-0.103653458368875,-0.178175465967414,
1.0143657940719));
#7997=CARTESIAN_POINT('Ctrl Pts',(-0.146533863776733,-0.129747205231268,
1.01066088977798));
#7998=CARTESIAN_POINT('Ctrl Pts',(-0.177682935350993,-0.0945680751475137,
1.00796958292279));
#7999=CARTESIAN_POINT('Ctrl Pts',(-0.19491028559363,-0.0470620713416631,
1.00527827606761));
#8000=CARTESIAN_POINT('Ctrl Pts',(-0.195321337055717,0.000175186119862003,
1.00258696921242));
#8001=CARTESIAN_POINT('Ctrl Pts',(-0.195294337528581,0.000171262189333537,
0.99241303078758));
#8002=CARTESIAN_POINT('Ctrl Pts',(-0.194904769586374,-0.0461298022874415,
0.995050073645006));
#8003=CARTESIAN_POINT('Ctrl Pts',(-0.178428147697951,-0.0926801463785582,
0.997687116502431));
#8004=CARTESIAN_POINT('Ctrl Pts',(-0.148414044317209,-0.127592253790654,
1.00032415935986));
#8005=CARTESIAN_POINT('Ctrl Pts',(-0.106245832988932,-0.176641899038874,
1.00402906365378));
#8006=CARTESIAN_POINT('Ctrl Pts',(-0.0373563275533994,-0.20271912173077,
1.00773396794771));
#8007=CARTESIAN_POINT('Ctrl Pts',(0.026721999693282,-0.193887716244123,
1.01143887224163));
#8008=CARTESIAN_POINT('Ctrl Pts',(0.0908003269399634,-0.185056310757476,
1.01514377653556));
#8009=CARTESIAN_POINT('Ctrl Pts',(0.150067475997793,-0.141316277092285,
1.01884868082948));
#8010=CARTESIAN_POINT('Ctrl Pts',(0.177395370914998,-0.0826885370284158,
1.02255358512341));
#8011=CARTESIAN_POINT('Ctrl Pts',(0.204723265832202,-0.0240607969645466,
1.02625848941733));
#8012=CARTESIAN_POINT('Ctrl Pts',(0.200111906608781,0.0494546494980005,
1.02996339371126));
#8013=CARTESIAN_POINT('Ctrl Pts',(0.165672029213017,0.10420791963383,1.03366829800518));
#8014=CARTESIAN_POINT('Ctrl Pts',(0.131232151817251,0.158961189769659,1.03737320229911));
#8015=CARTESIAN_POINT('Ctrl Pts',(0.0669637562491417,0.194952283578771,
1.04107810659304));
#8016=CARTESIAN_POINT('Ctrl Pts',(0.00228411571967282,0.195707165411358,
1.04478301088696));
#8017=CARTESIAN_POINT('Ctrl Pts',(-0.0623955248097952,0.196462047243945,
1.04848791518089));
#8018=CARTESIAN_POINT('Ctrl Pts',(-0.127486410300622,0.161980717100009,
1.05219281947481));
#8019=CARTESIAN_POINT('Ctrl Pts',(-0.163194793062323,0.108046153542432,
1.05589772376874));
#8020=CARTESIAN_POINT('Ctrl Pts',(-0.184126604735147,0.0764303804457572,
1.05806949277502));
#8021=CARTESIAN_POINT('Ctrl Pts',(-0.194962120753271,0.0381301666874187,
1.0602412617813));
#8022=CARTESIAN_POINT('Ctrl Pts',(-0.195118116536412,-8.83829588442778E-5,
1.06241303078758));
#8023=CARTESIAN_POINT('Origin',(0.,0.,0.));
#8024=CARTESIAN_POINT('',(-0.195593625707714,-0.000136366597080911,1.14258696921242));
#8025=CARTESIAN_POINT('',(-0.195617452784838,-0.000124751278337231,1.13241303078758));
#8026=CARTESIAN_POINT('',(-0.1954,-2.39295984553393E-17,0.));
#8027=CARTESIAN_POINT('Ctrl Pts',(-0.195593625707714,-0.000136366597080911,
1.14258696921242));
#8028=CARTESIAN_POINT('Ctrl Pts',(-0.195145973734063,0.0562028893414784,
1.13936555663412));
#8029=CARTESIAN_POINT('Ctrl Pts',(-0.169481039857298,0.112897892820961,
1.13614414405582));
#8030=CARTESIAN_POINT('Ctrl Pts',(-0.12658533900641,0.149273783523079,1.13292273147752));
#8031=CARTESIAN_POINT('Ctrl Pts',(-0.0772515568811993,0.191109217632128,
1.12921782718359));
#8032=CARTESIAN_POINT('Ctrl Pts',(-0.00512664276562529,0.206068565381736,
1.12551292288966));
#8033=CARTESIAN_POINT('Ctrl Pts',(0.0567760025061769,0.187304554237428,
1.12180801859574));
#8034=CARTESIAN_POINT('Ctrl Pts',(0.118678647777978,0.168540543093119,1.11810311430181));
#8035=CARTESIAN_POINT('Ctrl Pts',(0.170359024206009,0.116053173054895,1.11439821000789));
#8036=CARTESIAN_POINT('Ctrl Pts',(0.188161713919774,0.0538672434178332,
1.11069330571396));
#8037=CARTESIAN_POINT('Ctrl Pts',(0.205964403633538,-0.00831868621922783,
1.10698840142004));
#8038=CARTESIAN_POINT('Ctrl Pts',(0.189889406633038,-0.0802031754551247,
1.10328349712611));
#8039=CARTESIAN_POINT('Ctrl Pts',(0.147294656385406,-0.128882872015517,
1.09957859283219));
#8040=CARTESIAN_POINT('Ctrl Pts',(0.104699906137772,-0.17756256857591,1.09587368853826));
#8041=CARTESIAN_POINT('Ctrl Pts',(0.0355854026430044,-0.203037472460795,
1.09216878424434));
#8042=CARTESIAN_POINT('Ctrl Pts',(-0.0284133944896331,-0.193647074628664,
1.08846387995041));
#8043=CARTESIAN_POINT('Ctrl Pts',(-0.0924121916222716,-0.184256676796532,
1.08475897565649));
#8044=CARTESIAN_POINT('Ctrl Pts',(-0.15129528239278,-0.140000977247382,
1.08105407136256));
#8045=CARTESIAN_POINT('Ctrl Pts',(-0.178110384059518,-0.0811369311031284,
1.07734916706864));
#8046=CARTESIAN_POINT('Ctrl Pts',(-0.189599553508132,-0.0559161055777398,
1.07576176778323));
#8047=CARTESIAN_POINT('Ctrl Pts',(-0.1952017762943,-0.0280135229595192,
1.07417436849783));
#8048=CARTESIAN_POINT('Ctrl Pts',(-0.195106169435837,-7.43721989362317E-5,
1.07258696921242));
#8049=CARTESIAN_POINT('Ctrl Pts',(-0.195118116536412,-8.83829588442778E-5,
1.06241303078758));
#8050=CARTESIAN_POINT('Ctrl Pts',(-0.195228239960756,-0.0270683273893077,
1.06394616607522));
#8051=CARTESIAN_POINT('Ctrl Pts',(-0.190016233850183,-0.0540075745812006,
1.06547930136287));
#8052=CARTESIAN_POINT('Ctrl Pts',(-0.179276917571505,-0.0785257830526336,
1.06701243665051));
#8053=CARTESIAN_POINT('Ctrl Pts',(-0.153324779286411,-0.137775359118912,
1.07071734094444));
#8054=CARTESIAN_POINT('Ctrl Pts',(-0.0950946226836461,-0.182886714280253,
1.07442224523836));
#8055=CARTESIAN_POINT('Ctrl Pts',(-0.0312398659909398,-0.193211238158751,
1.07812714953229));
#8056=CARTESIAN_POINT('Ctrl Pts',(0.0326148907017665,-0.203535762037249,
1.08183205382621));
#8057=CARTESIAN_POINT('Ctrl Pts',(0.102094247484414,-0.179073454632905,
1.08553695812014));
#8058=CARTESIAN_POINT('Ctrl Pts',(0.145395742152504,-0.131021333918916,
1.08924186241407));
#8059=CARTESIAN_POINT('Ctrl Pts',(0.188697236820593,-0.0829692132049272,
1.09294676670799));
#8060=CARTESIAN_POINT('Ctrl Pts',(0.205820869374125,-0.0113272791812923,
1.09665167100191));
#8061=CARTESIAN_POINT('Ctrl Pts',(0.188928719280947,0.0511121395446363,
1.10035657529584));
#8062=CARTESIAN_POINT('Ctrl Pts',(0.172036569187769,0.113551558270567,1.10406147958977));
#8063=CARTESIAN_POINT('Ctrl Pts',(0.12112863644788,0.166788461698791,1.10776638388369));
#8064=CARTESIAN_POINT('Ctrl Pts',(0.0595067718820099,0.186454970108474,
1.11147128817762));
#8065=CARTESIAN_POINT('Ctrl Pts',(-0.00211509268385834,0.206121478518155,
1.11517619247154));
#8066=CARTESIAN_POINT('Ctrl Pts',(-0.0744508890757059,0.192217591909296,
1.11888109676547));
#8067=CARTESIAN_POINT('Ctrl Pts',(-0.124390690297799,0.151107471506893,
1.12258600105939));
#8068=CARTESIAN_POINT('Ctrl Pts',(-0.168544769350431,0.114760120061932,
1.12586167763545));
#8069=CARTESIAN_POINT('Ctrl Pts',(-0.195191579266694,0.0571452672802262,
1.12913735421152));
#8070=CARTESIAN_POINT('Ctrl Pts',(-0.195617452784838,-0.000124751278337231,
1.13241303078758));
#8071=CARTESIAN_POINT('Origin',(0.,0.,0.));
#8072=CARTESIAN_POINT('',(-0.195527484430252,0.000159769955907059,1.21258696921242));
#8073=CARTESIAN_POINT('',(-0.195499582979996,0.000166550639662629,1.20241303078758));
#8074=CARTESIAN_POINT('',(-0.1954,-2.39295984553393E-17,0.));
#8075=CARTESIAN_POINT('Ctrl Pts',(-0.195527484430252,0.000159769955907059,
1.21258696921242));
#8076=CARTESIAN_POINT('Ctrl Pts',(-0.195623513973876,0.0110197689033327,
1.21196655335827));
#8077=CARTESIAN_POINT('Ctrl Pts',(-0.194796702694689,0.0218651394014599,
1.21134613750411));
#8078=CARTESIAN_POINT('Ctrl Pts',(-0.192995482122666,0.0325461883928473,
1.21072572164995));
#8079=CARTESIAN_POINT('Ctrl Pts',(-0.182239229220893,0.0963296394548849,
1.20702081735602));
#8080=CARTESIAN_POINT('Ctrl Pts',(-0.136734990958994,0.154253292839981,
1.2033159130621));
#8081=CARTESIAN_POINT('Ctrl Pts',(-0.077311210265647,0.179804024609917,
1.19961100876817));
#8082=CARTESIAN_POINT('Ctrl Pts',(-0.0178874295722999,0.205354756379854,
1.19590610447425));
#8083=CARTESIAN_POINT('Ctrl Pts',(0.0554558935524948,0.19853256653463,1.19220120018032));
#8084=CARTESIAN_POINT('Ctrl Pts',(0.109147661596632,0.162460144240518,1.1884962958864));
#8085=CARTESIAN_POINT('Ctrl Pts',(0.162839429640769,0.126387721946406,1.18479139159247));
#8086=CARTESIAN_POINT('Ctrl Pts',(0.196879642604248,0.0610650672034059,
1.18108648729854));
#8087=CARTESIAN_POINT('Ctrl Pts',(0.195687232435581,-0.00360798563825114,
1.17738158300462));
#8088=CARTESIAN_POINT('Ctrl Pts',(0.194494822266914,-0.0682810384799082,
1.17367667871069));
#8089=CARTESIAN_POINT('Ctrl Pts',(0.158069788966098,-0.132304489420224,
1.16997177441677));
#8090=CARTESIAN_POINT('Ctrl Pts',(0.103084793284309,-0.166373182611243,
1.16626687012285));
#8091=CARTESIAN_POINT('Ctrl Pts',(0.0480997976025185,-0.200441875802263,
1.16256196582892));
#8092=CARTESIAN_POINT('Ctrl Pts',(-0.0254451604602465,-0.204555811243987,
1.15885706153499));
#8093=CARTESIAN_POINT('Ctrl Pts',(-0.083886689971347,-0.17683193643772,
1.15515215724107));
#8094=CARTESIAN_POINT('Ctrl Pts',(-0.142328219482446,-0.149108061631455,
1.15144725294714));
#8095=CARTESIAN_POINT('Ctrl Pts',(-0.18566632044188,-0.0895463765772016,
1.14774234865322));
#8096=CARTESIAN_POINT('Ctrl Pts',(-0.194064045854175,-0.0254097738158312,
1.14403744435929));
#8097=CARTESIAN_POINT('Ctrl Pts',(-0.195159952885721,-0.0170399176351585,
1.14355395264367));
#8098=CARTESIAN_POINT('Ctrl Pts',(-0.195660812389172,-0.00859214891261325,
1.14307046092805));
#8099=CARTESIAN_POINT('Ctrl Pts',(-0.195593625707714,-0.000136366597080911,
1.14258696921242));
#8100=CARTESIAN_POINT('Ctrl Pts',(-0.195617452784838,-0.000124751278337231,
1.13241303078758));
#8101=CARTESIAN_POINT('Ctrl Pts',(-0.195673257048185,-0.00762911832956361,
1.13284225850544));
#8102=CARTESIAN_POINT('Ctrl Pts',(-0.19527884452345,-0.0151275645336468,
1.13327148622331));
#8103=CARTESIAN_POINT('Ctrl Pts',(-0.194414610465335,-0.0225714646308396,
1.13370071394117));
#8104=CARTESIAN_POINT('Ctrl Pts',(-0.186954923358439,-0.0868239261702202,
1.1374056182351));
#8105=CARTESIAN_POINT('Ctrl Pts',(-0.144491743092308,-0.147012495053033,
1.14111052252902));
#8106=CARTESIAN_POINT('Ctrl Pts',(-0.0864615432906266,-0.175587338124856,
1.14481542682294));
#8107=CARTESIAN_POINT('Ctrl Pts',(-0.028431343488945,-0.204162181196678,
1.14852033111687));
#8108=CARTESIAN_POINT('Ctrl Pts',(0.0451658758482873,-0.20112329845751,
1.1522252354108));
#8109=CARTESIAN_POINT('Ctrl Pts',(0.100642802478808,-0.167861663542278,
1.15593013970472));
#8110=CARTESIAN_POINT('Ctrl Pts',(0.156119729109329,-0.134600028627046,
1.15963504399865));
#8111=CARTESIAN_POINT('Ctrl Pts',(0.193476363033138,-0.0711156415357493,
1.16333994829257));
#8112=CARTESIAN_POINT('Ctrl Pts',(0.195613626287182,-0.00646691493278147,
1.1670448525865));
#8113=CARTESIAN_POINT('Ctrl Pts',(0.197750889541227,0.0581818116701864,
1.17074975688042));
#8114=CARTESIAN_POINT('Ctrl Pts',(0.164668782125508,0.123994877784826,1.17445466117435));
#8115=CARTESIAN_POINT('Ctrl Pts',(0.111509822903934,0.160847975349094,1.17815956546828));
#8116=CARTESIAN_POINT('Ctrl Pts',(0.0583508636823605,0.197701072913362,
1.1818644697622));
#8117=CARTESIAN_POINT('Ctrl Pts',(-0.0148849473450669,0.205594201927258,
1.18556937405613));
#8118=CARTESIAN_POINT('Ctrl Pts',(-0.0746757236775608,0.180914477229441,
1.18927427835005));
#8119=CARTESIAN_POINT('Ctrl Pts',(-0.134466500010055,0.156234752531623,
1.19297918264398));
#8120=CARTESIAN_POINT('Ctrl Pts',(-0.180812241647615,0.098982174122092,
1.1966840869379));
#8121=CARTESIAN_POINT('Ctrl Pts',(-0.192499328242851,0.0353626979177265,
1.20038899123183));
#8122=CARTESIAN_POINT('Ctrl Pts',(-0.194627599644181,0.0237773031600198,
1.20106367108374));
#8123=CARTESIAN_POINT('Ctrl Pts',(-0.195606518663776,0.011980768958621,
1.20173835093566));
#8124=CARTESIAN_POINT('Ctrl Pts',(-0.195499582979996,0.000166550639662629,
1.20241303078758));
#8125=CARTESIAN_POINT('Origin',(0.,0.,0.));
#8126=CARTESIAN_POINT('',(-0.195085605073228,3.67867518197285E-5,1.28258696921242));
#8127=CARTESIAN_POINT('',(-0.19508137714814,2.13056907460231E-5,1.27241303078758));
#8128=CARTESIAN_POINT('',(-0.1954,-2.39295984553393E-17,0.));
#8129=CARTESIAN_POINT('Ctrl Pts',(-0.195085605073228,3.67867518197285E-5,
1.28258696921242));
#8130=CARTESIAN_POINT('Ctrl Pts',(-0.195136667969355,0.0303938707492628,
1.28086264578848));
#8131=CARTESIAN_POINT('Ctrl Pts',(-0.188480024483457,0.0607297539874398,
1.27913832236455));
#8132=CARTESIAN_POINT('Ctrl Pts',(-0.174998421369655,0.0876473788358303,
1.27741399894061));
#8133=CARTESIAN_POINT('Ctrl Pts',(-0.146031669209427,0.145482946397307,
1.27370909464668));
#8134=CARTESIAN_POINT('Ctrl Pts',(-0.0855572231025935,0.187537989963383,
1.27000419035276));
#8135=CARTESIAN_POINT('Ctrl Pts',(-0.0212557694531386,0.194562850420161,
1.26629928605883));
#8136=CARTESIAN_POINT('Ctrl Pts',(0.0430456841963182,0.201587710876938,
1.2625943817649));
#8137=CARTESIAN_POINT('Ctrl Pts',(0.111174145388397,0.173582388224419,1.25888947747098));
#8138=CARTESIAN_POINT('Ctrl Pts',(0.151945491062064,0.123365628294801,1.25518457317705));
#8139=CARTESIAN_POINT('Ctrl Pts',(0.192716836735728,0.0731488683651866,
1.25147966888313));
#8140=CARTESIAN_POINT('Ctrl Pts',(0.206131066890981,0.000720671158477647,
1.2477747645892));
#8141=CARTESIAN_POINT('Ctrl Pts',(0.186048148469522,-0.0607667421351959,
1.24406986029528));
#8142=CARTESIAN_POINT('Ctrl Pts',(0.165965230048063,-0.122254155428872,
1.24036495600135));
#8143=CARTESIAN_POINT('Ctrl Pts',(0.112385163049889,-0.172800784809512,
1.23666005170743));
#8144=CARTESIAN_POINT('Ctrl Pts',(0.0498329018575594,-0.189270157159331,
1.2329551474135));
#8145=CARTESIAN_POINT('Ctrl Pts',(-0.0127193593347688,-0.205739529509149,
1.22925024311958));
#8146=CARTESIAN_POINT('Ctrl Pts',(-0.0842438147212514,-0.188131644828148,
1.22554533882565));
#8147=CARTESIAN_POINT('Ctrl Pts',(-0.132001908643669,-0.144506078118158,
1.22184043453172));
#8148=CARTESIAN_POINT('Ctrl Pts',(-0.171762527791251,-0.108185961451209,
1.21875594609196));
#8149=CARTESIAN_POINT('Ctrl Pts',(-0.195050059465688,-0.0538323080748223,
1.21567145765219));
#8150=CARTESIAN_POINT('Ctrl Pts',(-0.195527484430252,0.000159769955907059,
1.21258696921242));
#8151=CARTESIAN_POINT('Ctrl Pts',(-0.195499582979996,0.000166550639662629,
1.20241303078758));
#8152=CARTESIAN_POINT('Ctrl Pts',(-0.195019297224031,-0.0528952578782005,
1.20544325522959));
#8153=CARTESIAN_POINT('Ctrl Pts',(-0.172634890521839,-0.106313794647688,
1.2084734796716));
#8154=CARTESIAN_POINT('Ctrl Pts',(-0.134099291878761,-0.142561887247553,
1.2115037041136));
#8155=CARTESIAN_POINT('Ctrl Pts',(-0.0869837373665235,-0.186880622209269,
1.21520860840753));
#8156=CARTESIAN_POINT('Ctrl Pts',(-0.0157241967891372,-0.205531718133499,
1.21891351270145));
#8157=CARTESIAN_POINT('Ctrl Pts',(0.0470620324162366,-0.189978095797443,
1.22261841699538));
#8158=CARTESIAN_POINT('Ctrl Pts',(0.10984826162161,-0.174424473461387,1.2263233212893));
#8159=CARTESIAN_POINT('Ctrl Pts',(0.16416117945497,-0.124666132865044,1.23002822558323));
#8160=CARTESIAN_POINT('Ctrl Pts',(0.185140387136073,-0.0634787273744072,
1.23373312987716));
#8161=CARTESIAN_POINT('Ctrl Pts',(0.206119594817175,-0.00229132188377159,
1.23743803417108));
#8162=CARTESIAN_POINT('Ctrl Pts',(0.19376509234602,0.0703251485011587,1.24114293846501));
#8163=CARTESIAN_POINT('Ctrl Pts',(0.153731848566424,0.12113228518574,1.24484784275893));
#8164=CARTESIAN_POINT('Ctrl Pts',(0.113698604786827,0.171939421870322,1.24855274705286));
#8165=CARTESIAN_POINT('Ctrl Pts',(0.0459866196987903,0.200937224854556,
1.25225765134678));
#8166=CARTESIAN_POINT('Ctrl Pts',(-0.0184106153029644,0.194852664908991,
1.25596255564071));
#8167=CARTESIAN_POINT('Ctrl Pts',(-0.0828078503047191,0.188768104963426,
1.25966745993463));
#8168=CARTESIAN_POINT('Ctrl Pts',(-0.14389033522019,0.147601182088061,1.26337236422856));
#8169=CARTESIAN_POINT('Ctrl Pts',(-0.173699068875,0.0901950400516983,1.26707726852248));
#8170=CARTESIAN_POINT('Ctrl Pts',(-0.188009138590469,0.0626364760365528,
1.26885585594418));
#8171=CARTESIAN_POINT('Ctrl Pts',(-0.195111844846784,0.0313354139177859,
1.27063444336588));
#8172=CARTESIAN_POINT('Ctrl Pts',(-0.19508137714814,2.13056907460231E-5,
1.27241303078758));
#8173=CARTESIAN_POINT('Origin',(0.,0.,0.));
#8174=CARTESIAN_POINT('',(-0.195392498133114,-0.000178699422991063,1.35258696921242));
#8175=CARTESIAN_POINT('',(-0.195421369810842,-0.000177481533986374,1.34241303078758));
#8176=CARTESIAN_POINT('',(-0.1954,-2.39295984553393E-17,0.));
#8177=CARTESIAN_POINT('Ctrl Pts',(-0.195392498133114,-0.000178699422991063,
1.35258696921242));
#8178=CARTESIAN_POINT('Ctrl Pts',(-0.194938084649759,0.0494157798589555,
1.3497587382187));
#8179=CARTESIAN_POINT('Ctrl Pts',(-0.17572581092509,0.099323482715635,1.34693050722498));
#8180=CARTESIAN_POINT('Ctrl Pts',(-0.141651466296104,0.135060625627259,
1.34410227623126));
#8181=CARTESIAN_POINT('Ctrl Pts',(-0.0970150182800354,0.181875293354148,
1.34039737193734));
#8182=CARTESIAN_POINT('Ctrl Pts',(-0.0268748485034288,0.204372891114381,
1.33669246764341));
#8183=CARTESIAN_POINT('Ctrl Pts',(0.0366641099768968,0.192255698324562,
1.33298756334949));
#8184=CARTESIAN_POINT('Ctrl Pts',(0.100203068457222,0.180138505534742,1.32928265905556));
#8185=CARTESIAN_POINT('Ctrl Pts',(0.157140815641268,0.133406522194869,1.32557775476164));
#8186=CARTESIAN_POINT('Ctrl Pts',(0.181415501841872,0.0734501612668376,
1.32187285046771));
#8187=CARTESIAN_POINT('Ctrl Pts',(0.205690188042477,0.0134938003388052,
1.31816794617379));
#8188=CARTESIAN_POINT('Ctrl Pts',(0.197301813259641,-0.0596869381773843,
1.31446304187986));
#8189=CARTESIAN_POINT('Ctrl Pts',(0.160089949192665,-0.112595375864876,
1.31075813758593));
#8190=CARTESIAN_POINT('Ctrl Pts',(0.12287808512569,-0.165503813552367,1.30705323329201));
#8191=CARTESIAN_POINT('Ctrl Pts',(0.0568427317745747,-0.19813995041116,
1.30334832899808));
#8192=CARTESIAN_POINT('Ctrl Pts',(-0.00779005629774907,-0.19556539960213,
1.29964342470416));
#8193=CARTESIAN_POINT('Ctrl Pts',(-0.0724228443700711,-0.1929908487931,
1.29593852041023));
#8194=CARTESIAN_POINT('Ctrl Pts',(-0.135653067163603,-0.155205610316251,
1.29223361611631));
#8195=CARTESIAN_POINT('Ctrl Pts',(-0.168538649453556,-0.0995049452993885,
1.28852871182238));
#8196=CARTESIAN_POINT('Ctrl Pts',(-0.186118740601559,-0.0697282863560552,
1.2865481309524));
#8197=CARTESIAN_POINT('Ctrl Pts',(-0.195026953550068,-0.0348317645878951,
1.28456755008241));
#8198=CARTESIAN_POINT('Ctrl Pts',(-0.195085605073228,3.67867518197285E-5,
1.28258696921242));
#8199=CARTESIAN_POINT('Ctrl Pts',(-0.19508137714814,2.13056907460231E-5,
1.27241303078758));
#8200=CARTESIAN_POINT('Ctrl Pts',(-0.1950483788028,-0.0338937520008573,
1.27433934765981));
#8201=CARTESIAN_POINT('Ctrl Pts',(-0.186648032317626,-0.0678241130245367,
1.27626566453203));
#8202=CARTESIAN_POINT('Ctrl Pts',(-0.169974591739146,-0.0970316955488254,
1.27819198140426));
#8203=CARTESIAN_POINT('Ctrl Pts',(-0.137906398554337,-0.153206927915627,
1.28189688569818));
#8204=CARTESIAN_POINT('Ctrl Pts',(-0.0752350297905721,-0.19191203145187,
1.28560178999211));
#8205=CARTESIAN_POINT('Ctrl Pts',(-0.0106467590218702,-0.195430699482706,
1.28930669428604));
#8206=CARTESIAN_POINT('Ctrl Pts',(0.0539415117468317,-0.198949367513541,
1.29301159857996));
#8207=CARTESIAN_POINT('Ctrl Pts',(0.120446684520471,-0.16728160003897,1.29671650287389));
#8208=CARTESIAN_POINT('Ctrl Pts',(0.158427656481215,-0.114922536692502,
1.30042140716781));
#8209=CARTESIAN_POINT('Ctrl Pts',(0.19640862844196,-0.0625634733460332,
1.30412631146174));
#8210=CARTESIAN_POINT('Ctrl Pts',(0.205865399589811,0.0104868858723325,
1.30783121575566));
#8211=CARTESIAN_POINT('Ctrl Pts',(0.182469366136063,0.0707915404541595,
1.31153612004959));
#8212=CARTESIAN_POINT('Ctrl Pts',(0.159073332682314,0.131096195035986,1.31524102434351));
#8213=CARTESIAN_POINT('Ctrl Pts',(0.102824494626968,0.178655144981275,1.31894592863744));
#8214=CARTESIAN_POINT('Ctrl Pts',(0.039469370492038,0.19169945375752,1.32265083293136));
#8215=CARTESIAN_POINT('Ctrl Pts',(-0.0238857536428916,0.204743762533765,
1.32635573722529));
#8216=CARTESIAN_POINT('Ctrl Pts',(-0.0943471638574042,0.183273430140967,
1.33006064151922));
#8217=CARTESIAN_POINT('Ctrl Pts',(-0.139662887206028,0.137115971772969,
1.33376554581314));
#8218=CARTESIAN_POINT('Ctrl Pts',(-0.174919491756342,0.101204479326771,
1.33664804080462));
#8219=CARTESIAN_POINT('Ctrl Pts',(-0.194954975303473,0.0503494407490454,
1.3395305357961));
#8220=CARTESIAN_POINT('Ctrl Pts',(-0.195421369810842,-0.000177481533986374,
1.34241303078758));
#8221=CARTESIAN_POINT('Origin',(0.,0.,0.));
#8222=CARTESIAN_POINT('',(-0.195688377393879,7.16972608892641E-5,1.42258696921242));
#8223=CARTESIAN_POINT('',(-0.195672555088735,8.72824817547956E-5,1.41241303078758));
#8224=CARTESIAN_POINT('',(-0.1954,-2.39295984553393E-17,0.));
#8225=CARTESIAN_POINT('Ctrl Pts',(-0.195688377393879,7.16972608892641E-5,
1.42258696921242));
#8226=CARTESIAN_POINT('Ctrl Pts',(-0.195707099359798,0.0040407295163859,
1.42235973494285));
#8227=CARTESIAN_POINT('Ctrl Pts',(-0.195596806193923,0.00800870147258908,
1.42213250067327));
#8228=CARTESIAN_POINT('Ctrl Pts',(-0.195354201126062,0.0119685672100241,
1.4219052664037));
#8229=CARTESIAN_POINT('Ctrl Pts',(-0.191398686144431,0.0765315558885256,
1.41820036210977));
#8230=CARTESIAN_POINT('Ctrl Pts',(-0.152270508849115,0.138939656827576,
1.41449545781585));
#8231=CARTESIAN_POINT('Ctrl Pts',(-0.0958796274951682,0.170627100807728,
1.41079055352192));
#8232=CARTESIAN_POINT('Ctrl Pts',(-0.0394887461412211,0.20231454478788,
1.40708564922799));
#8233=CARTESIAN_POINT('Ctrl Pts',(0.034164839271357,0.203281331809134,1.40338074493407));
#8234=CARTESIAN_POINT('Ctrl Pts',(0.0913680163193032,0.173084938953504,
1.39967584064014));
#8235=CARTESIAN_POINT('Ctrl Pts',(0.148571193367249,0.142888546097875,1.39597093634622));
#8236=CARTESIAN_POINT('Ctrl Pts',(0.189323962050564,0.0815289733653608,
1.39226603205229));
#8237=CARTESIAN_POINT('Ctrl Pts',(0.194972747468802,0.0170920520456009,
1.38856112775837));
#8238=CARTESIAN_POINT('Ctrl Pts',(0.200621532887041,-0.0473448692741589,
1.38485622346444));
#8239=CARTESIAN_POINT('Ctrl Pts',(0.171166335040203,-0.114859139181165,
1.38115131917052));
#8240=CARTESIAN_POINT('Ctrl Pts',(0.120089544376728,-0.154547765529148,
1.37744641487659));
#8241=CARTESIAN_POINT('Ctrl Pts',(0.0690127537132543,-0.194236391877132,
1.37374151058267));
#8242=CARTESIAN_POINT('Ctrl Pts',(-0.00368562976685627,-0.206099374666093,
1.37003660628874));
#8243=CARTESIAN_POINT('Ctrl Pts',(-0.0647297137696226,-0.184706726065852,
1.36633170199482));
#8244=CARTESIAN_POINT('Ctrl Pts',(-0.125773797772389,-0.16331407746561,
1.36262679770089));
#8245=CARTESIAN_POINT('Ctrl Pts',(-0.175163582297811,-0.108665797476165,
1.35892189340696));
#8246=CARTESIAN_POINT('Ctrl Pts',(-0.190292111432757,-0.0457757886346702,
1.35521698911304));
#8247=CARTESIAN_POINT('Ctrl Pts',(-0.193871900952753,-0.030894434832521,
1.35434031581283));
#8248=CARTESIAN_POINT('Ctrl Pts',(-0.195533353731187,-0.0155516148321636,
1.35346364251263));
#8249=CARTESIAN_POINT('Ctrl Pts',(-0.195392498133114,-0.000178699422991063,
1.35258696921242));
#8250=CARTESIAN_POINT('Ctrl Pts',(-0.195421369810842,-0.000177481533986374,
1.34241303078758));
#8251=CARTESIAN_POINT('Ctrl Pts',(-0.19555443758116,-0.0145933993525209,
1.34323544009003));
#8252=CARTESIAN_POINT('Ctrl Pts',(-0.194094528316993,-0.0289826076128833,
1.34405784939247));
#8253=CARTESIAN_POINT('Ctrl Pts',(-0.190940659847886,-0.0429904198028263,
1.34488025869492));
#8254=CARTESIAN_POINT('Ctrl Pts',(-0.176732672658387,-0.106094768667428,
1.34858516298884));
#8255=CARTESIAN_POINT('Ctrl Pts',(-0.128146661796655,-0.161458882053436,
1.35229006728277));
#8256=CARTESIAN_POINT('Ctrl Pts',(-0.0674216756023477,-0.183741202338891,
1.35599497157669));
#8257=CARTESIAN_POINT('Ctrl Pts',(-0.00669668940803995,-0.206023522624345,
1.35969987587062));
#8258=CARTESIAN_POINT('Ctrl Pts',(0.0661672721188413,-0.195224049809246,
1.36340478016454));
#8259=CARTESIAN_POINT('Ctrl Pts',(0.117818527416568,-0.156285976259422,
1.36710968445847));
#8260=CARTESIAN_POINT('Ctrl Pts',(0.169469782714294,-0.117347902709599,
1.3708145887524));
#8261=CARTESIAN_POINT('Ctrl Pts',(0.199908331782865,-0.0502712284250506,
1.37451949304632));
#8262=CARTESIAN_POINT('Ctrl Pts',(0.195201679401558,0.0142413530530136,
1.37822439734025));
#8263=CARTESIAN_POINT('Ctrl Pts',(0.190495027020252,0.0787539345310777,
1.38192930163417));
#8264=CARTESIAN_POINT('Ctrl Pts',(0.150643173189068,0.140702423202659,1.3856342059281));
#8265=CARTESIAN_POINT('Ctrl Pts',(0.0938873212514722,0.171731426029694,
1.38933911022202));
#8266=CARTESIAN_POINT('Ctrl Pts',(0.0371314693138761,0.202760428856729,
1.39304401451595));
#8267=CARTESIAN_POINT('Ctrl Pts',(-0.0365283807301298,0.202869945839216,
1.39674891880987));
#8268=CARTESIAN_POINT('Ctrl Pts',(-0.0933762489767357,0.172009848279114,
1.4004538231038));
#8269=CARTESIAN_POINT('Ctrl Pts',(-0.150224117223341,0.141149750719013,
1.40415872739772));
#8270=CARTESIAN_POINT('Ctrl Pts',(-0.190260003672545,0.0793200386163227,
1.40786363169165));
#8271=CARTESIAN_POINT('Ctrl Pts',(-0.195158468588232,0.014821737963731,
1.41156853598557));
#8272=CARTESIAN_POINT('Ctrl Pts',(-0.195530653475337,0.009921163363317,
1.41185003425291));
#8273=CARTESIAN_POINT('Ctrl Pts',(-0.195699991939521,0.00500518314638453,
1.41213153252024));
#8274=CARTESIAN_POINT('Ctrl Pts',(-0.195672555088735,8.72824817547956E-5,
1.41241303078758));
#8275=CARTESIAN_POINT('Origin',(0.,0.,0.));
#8276=CARTESIAN_POINT('',(-0.195179950177078,0.000133868047100166,1.49258696921242));
#8277=CARTESIAN_POINT('',(-0.195160806943041,0.000122850585401665,1.48241303078758));
#8278=CARTESIAN_POINT('',(-0.1954,-2.39295984553393E-17,0.));
#8279=CARTESIAN_POINT('Ctrl Pts',(-0.195179950177078,0.000133868047100166,
1.49258696921242));
#8280=CARTESIAN_POINT('Ctrl Pts',(-0.19532758311484,0.0235405577971841,
1.49125582737307));
#8281=CARTESIAN_POINT('Ctrl Pts',(-0.191434166902591,0.0468997728483757,
1.48992468553371));
#8282=CARTESIAN_POINT('Ctrl Pts',(-0.183280900003334,0.0686631064883505,
1.48859354369435));
#8283=CARTESIAN_POINT('Ctrl Pts',(-0.160588296817507,0.129235966471356,
1.48488863940043));
#8284=CARTESIAN_POINT('Ctrl Pts',(-0.104896775936504,0.177446336966025,
1.4811837351065));
#8285=CARTESIAN_POINT('Ctrl Pts',(-0.041697757689242,0.191227109747421,
1.47747883081258));
#8286=CARTESIAN_POINT('Ctrl Pts',(0.02150126055802,0.205007882528817,1.47377392651865));
#8287=CARTESIAN_POINT('Ctrl Pts',(0.0922077761715412,0.184359057596941,
1.47006902222473));
#8288=CARTESIAN_POINT('Ctrl Pts',(0.138057625253759,0.138732125363795,1.4663641179308));
#8289=CARTESIAN_POINT('Ctrl Pts',(0.183907474335976,0.0931051931306484,
1.46265921363688));
#8290=CARTESIAN_POINT('Ctrl Pts',(0.20490065688689,0.0225001535962327,1.45895430934295));
#8291=CARTESIAN_POINT('Ctrl Pts',(0.191428061286251,-0.0407652775146975,
1.45524940504902));
#8292=CARTESIAN_POINT('Ctrl Pts',(0.177955465685611,-0.104030708625628,
1.4515445007551));
#8293=CARTESIAN_POINT('Ctrl Pts',(0.130017091933419,-0.159956531313072,
1.44783959646117));
#8294=CARTESIAN_POINT('Ctrl Pts',(0.0695555484531877,-0.182944079374106,
1.44413469216725));
#8295=CARTESIAN_POINT('Ctrl Pts',(0.00909400497295641,-0.205931627435139,
1.44042978787332));
#8296=CARTESIAN_POINT('Ctrl Pts',(-0.063890708235314,-0.195980900869761,
1.4367248835794));
#8297=CARTESIAN_POINT('Ctrl Pts',(-0.115991638505476,-0.157646599378095,
1.43301997928547));
#8298=CARTESIAN_POINT('Ctrl Pts',(-0.164897043089976,-0.121663469821813,
1.42954230926112));
#8299=CARTESIAN_POINT('Ctrl Pts',(-0.195401850102924,-0.0606717131691646,
1.42606463923677));
#8300=CARTESIAN_POINT('Ctrl Pts',(-0.195688377393879,7.16972608892641E-5,
1.42258696921242));
#8301=CARTESIAN_POINT('Ctrl Pts',(-0.195672555088735,8.72824817547956E-5,
1.41241303078758));
#8302=CARTESIAN_POINT('Ctrl Pts',(-0.195338885254029,-0.0597211523368212,
1.41583643681417));
#8303=CARTESIAN_POINT('Ctrl Pts',(-0.16590233426085,-0.119813619535752,
1.41925984284076));
#8304=CARTESIAN_POINT('Ctrl Pts',(-0.118282735433092,-0.155934942448556,
1.42268324886735));
#8305=CARTESIAN_POINT('Ctrl Pts',(-0.0667474939800966,-0.195026433005756,
1.42638815316128));
#8306=CARTESIAN_POINT('Ctrl Pts',(0.00608403230806285,-0.206042524917664,
1.4300930574552));
#8307=CARTESIAN_POINT('Ctrl Pts',(0.0668750083003318,-0.183940873768719,
1.43379796174913));
#8308=CARTESIAN_POINT('Ctrl Pts',(0.127665984292602,-0.161839222619775,
1.43750286604305));
#8309=CARTESIAN_POINT('Ctrl Pts',(0.176416409988978,-0.106619828409975,
1.44120777033698));
#8310=CARTESIAN_POINT('Ctrl Pts',(0.190811980213718,-0.0435580071271506,
1.4449126746309));
#8311=CARTESIAN_POINT('Ctrl Pts',(0.205207550438459,0.019503814155676,1.44861757892483));
#8312=CARTESIAN_POINT('Ctrl Pts',(0.185248265191562,0.0904080625115289,
1.45232248321875));
#8313=CARTESIAN_POINT('Ctrl Pts',(0.140069995098299,0.136700066756136,1.45602738751268));
#8314=CARTESIAN_POINT('Ctrl Pts',(0.0948917250050361,0.182992071000741,
1.4597322918066));
#8315=CARTESIAN_POINT('Ctrl Pts',(0.0244944700654076,0.204671831134102,
1.46343719610053));
#8316=CARTESIAN_POINT('Ctrl Pts',(-0.0388991622701212,0.191815971578626,
1.46714210039445));
#8317=CARTESIAN_POINT('Ctrl Pts',(-0.10229279460565,0.178960112023149,1.47084700468838));
#8318=CARTESIAN_POINT('Ctrl Pts',(-0.15868280433708,0.131568632778834,1.47455190898231));
#8319=CARTESIAN_POINT('Ctrl Pts',(-0.182258055088965,0.0713338147946472,
1.47825681327623));
#8320=CARTESIAN_POINT('Ctrl Pts',(-0.191073745701187,0.0488097057185394,
1.47964221911335));
#8321=CARTESIAN_POINT('Ctrl Pts',(-0.195300951932749,0.0244897139044186,
1.48102762495046));
#8322=CARTESIAN_POINT('Ctrl Pts',(-0.195160806943041,0.000122850585401665,
1.48241303078758));
#8323=CARTESIAN_POINT('Origin',(0.,0.,0.));
#8324=CARTESIAN_POINT('',(-0.195203598247727,-0.000145069483009505,1.56258696921242));
#8325=CARTESIAN_POINT('',(-0.195226188848194,-0.00015379427405286,1.55241303078758));
#8326=CARTESIAN_POINT('',(-0.1954,-2.39295984553393E-17,0.));
#8327=CARTESIAN_POINT('Ctrl Pts',(-0.195203598247727,-0.000145069483009505,
1.56258696921242));
#8328=CARTESIAN_POINT('Ctrl Pts',(-0.194908648709454,0.0426596016193331,
1.56015191980329));
#8329=CARTESIAN_POINT('Ctrl Pts',(-0.181052651050772,0.0856379285438176,
1.55771687039415));
#8330=CARTESIAN_POINT('Ctrl Pts',(-0.155131211310912,0.119334897560907,
1.55528182098501));
#8331=CARTESIAN_POINT('Ctrl Pts',(-0.11569198965218,0.170604512351969,1.55157691669109));
#8332=CARTESIAN_POINT('Ctrl Pts',(-0.0483220775946747,0.200388405157253,
1.54787201239716));
#8333=CARTESIAN_POINT('Ctrl Pts',(0.0161416089610767,0.195053733516717,
1.54416710810323));
#8334=CARTESIAN_POINT('Ctrl Pts',(0.0806052955168263,0.189719061876181,
1.54046220380931));
#8335=CARTESIAN_POINT('Ctrl Pts',(0.14216275657082,0.149265825789827,1.53675729951538));
#8336=CARTESIAN_POINT('Ctrl Pts',(0.172637582334195,0.0922104964983205,
1.53305239522146));
#8337=CARTESIAN_POINT('Ctrl Pts',(0.20311240809757,0.0351551672068159,1.52934749092753));
#8338=CARTESIAN_POINT('Ctrl Pts',(0.202504598570326,-0.0385022552898431,
1.52564258663361));
#8339=CARTESIAN_POINT('Ctrl Pts',(0.17109236357496,-0.0950469022377724,
1.52193768233968));
#8340=CARTESIAN_POINT('Ctrl Pts',(0.139680128579593,-0.151591549185703,
1.51823277804576));
#8341=CARTESIAN_POINT('Ctrl Pts',(0.077463468116105,-0.191023420584907,
1.51452787375183));
#8342=CARTESIAN_POINT('Ctrl Pts',(0.0129205242471798,-0.195293549693381,
1.51082296945791));
#8343=CARTESIAN_POINT('Ctrl Pts',(-0.0516224196217455,-0.199563678801854,
1.50711806516398));
#8344=CARTESIAN_POINT('Ctrl Pts',(-0.118491646896106,-0.168672065619597,
1.50341316087006));
#8345=CARTESIAN_POINT('Ctrl Pts',(-0.157079417787961,-0.116758584292797,
1.49970825657613));
#8346=CARTESIAN_POINT('Ctrl Pts',(-0.181802917906106,-0.0834971926121641,
1.49733449412156));
#8347=CARTESIAN_POINT('Ctrl Pts',(-0.194916683322746,-0.0416061777329493,
1.49496073166699));
#8348=CARTESIAN_POINT('Ctrl Pts',(-0.195179950177078,0.000133868047100166,
1.49258696921242));
#8349=CARTESIAN_POINT('Ctrl Pts',(-0.195160806943041,0.000122850585401665,
1.48241303078758));
#8350=CARTESIAN_POINT('Ctrl Pts',(-0.194926170940615,-0.0406730666480617,
1.48473252924439));
#8351=CARTESIAN_POINT('Ctrl Pts',(-0.182449537937005,-0.0816003680531453,
1.4870520277012));
#8352=CARTESIAN_POINT('Ctrl Pts',(-0.158768687450683,-0.114450931246349,
1.48937152615801));
#8353=CARTESIAN_POINT('Ctrl Pts',(-0.120943577288175,-0.166922702579101,
1.49307643045193));
#8354=CARTESIAN_POINT('Ctrl Pts',(-0.0545328651908197,-0.198788088520544,
1.49678133474586));
#8355=CARTESIAN_POINT('Ctrl Pts',(0.0100655830687197,-0.195461494457236,
1.50048623903978));
#8356=CARTESIAN_POINT('Ctrl Pts',(0.074664031328259,-0.192134900393928,
1.50419114333371));
#8357=CARTESIAN_POINT('Ctrl Pts',(0.13745021574998,-0.153616326325868,1.50789604762764));
#8358=CARTESIAN_POINT('Ctrl Pts',(0.169685308723794,-0.0975366996636656,
1.51160095192156));
#8359=CARTESIAN_POINT('Ctrl Pts',(0.201920401697606,-0.0414570730014645,
1.51530585621549));
#8360=CARTESIAN_POINT('Ctrl Pts',(0.203604403223511,0.0321836062548823,
1.51901076050941));
#8361=CARTESIAN_POINT('Ctrl Pts',(0.173966503130547,0.0896781331568551,
1.52271566480334));
#8362=CARTESIAN_POINT('Ctrl Pts',(0.144328603037582,0.147172660058829,1.52642056909726));
#8363=CARTESIAN_POINT('Ctrl Pts',(0.0833688013257482,0.188521034606432,
1.53012547339119));
#8364=CARTESIAN_POINT('Ctrl Pts',(0.0189899439583294,0.194797058002499,
1.53383037768511));
#8365=CARTESIAN_POINT('Ctrl Pts',(-0.0453889134090893,0.201073081398565,
1.53753528197904));
#8366=CARTESIAN_POINT('Ctrl Pts',(-0.113186826432091,0.172276753643094,
1.54124018627296));
#8367=CARTESIAN_POINT('Ctrl Pts',(-0.153370972322708,0.121588883647957,
1.54494509056689));
#8368=CARTESIAN_POINT('Ctrl Pts',(-0.180370572089492,0.0875318650758873,
1.54743440397379));
#8369=CARTESIAN_POINT('Ctrl Pts',(-0.19490406552098,0.0435920118983492,
1.54992371738068));
#8370=CARTESIAN_POINT('Ctrl Pts',(-0.195226188848194,-0.00015379427405286,
1.55241303078758));
#8371=CARTESIAN_POINT('Origin',(0.,0.,0.));
#8372=CARTESIAN_POINT('',(-0.195702834179537,-5.31785447526745E-5,1.63258696921242));
#8373=CARTESIAN_POINT('',(-0.195712283470102,-3.61459064724743E-5,1.62241303078758));
#8374=CARTESIAN_POINT('',(-0.1954,-2.39295984553393E-17,0.));
#8375=CARTESIAN_POINT('Ctrl Pts',(-0.195702834179537,-5.31785447526745E-5,
1.63258696921242));
#8376=CARTESIAN_POINT('Ctrl Pts',(-0.195478917826867,0.061748543580026,
1.62904801223351));
#8377=CARTESIAN_POINT('Ctrl Pts',(-0.163739035867485,0.12374830482208,1.62550905525459));
#8378=CARTESIAN_POINT('Ctrl Pts',(-0.113374270159849,0.15953929097368,1.62197009827567));
#8379=CARTESIAN_POINT('Ctrl Pts',(-0.0606478205747536,0.197008573326304,
1.61826519398174));
#8380=CARTESIAN_POINT('Ctrl Pts',(0.0124911663215799,0.205753509978468,
1.61456028968782));
#8381=CARTESIAN_POINT('Ctrl Pts',(0.0725651228866868,0.181771321828013,
1.61085538539389));
#8382=CARTESIAN_POINT('Ctrl Pts',(0.132639079451794,0.157789133677557,1.60715048109997));
#8383=CARTESIAN_POINT('Ctrl Pts',(0.179648005685674,0.10107982072448,1.60344557680604));
#8384=CARTESIAN_POINT('Ctrl Pts',(0.192074724846121,0.0376006725199113,
1.59974067251212));
#8385=CARTESIAN_POINT('Ctrl Pts',(0.204501444006568,-0.0258784756846574,
1.59603576821819));
#8386=CARTESIAN_POINT('Ctrl Pts',(0.182345956093582,-0.0961274591407182,
1.59233086392426));
#8387=CARTESIAN_POINT('Ctrl Pts',(0.13574938934442,-0.140991538013031,1.58862595963034));
#8388=CARTESIAN_POINT('Ctrl Pts',(0.0891528225952577,-0.185855616885343,
1.58492105533641));
#8389=CARTESIAN_POINT('Ctrl Pts',(0.0181151770099195,-0.205334791173908,
1.58121615104249));
#8390=CARTESIAN_POINT('Ctrl Pts',(-0.0448478169351064,-0.190512949205082,
1.57751124674856));
#8391=CARTESIAN_POINT('Ctrl Pts',(-0.107810810880132,-0.175691107236256,
1.57380634245464));
#8392=CARTESIAN_POINT('Ctrl Pts',(-0.162699153184846,-0.126568249010039,
1.57010143816071));
#8393=CARTESIAN_POINT('Ctrl Pts',(-0.184389058707223,-0.0656291515085119,
1.56639653386679));
#8394=CARTESIAN_POINT('Ctrl Pts',(-0.191823267607932,-0.0447422933071413,
1.565126678982));
#8395=CARTESIAN_POINT('Ctrl Pts',(-0.195357411599742,-0.0224672944395423,
1.56385682409721));
#8396=CARTESIAN_POINT('Ctrl Pts',(-0.195203598247727,-0.000145069483009505,
1.56258696921242));
#8397=CARTESIAN_POINT('Ctrl Pts',(-0.195226188848194,-0.00015379427405286,
1.55241303078758));
#8398=CARTESIAN_POINT('Ctrl Pts',(-0.195383489323086,-0.0215159109049027,
1.55362862167461));
#8399=CARTESIAN_POINT('Ctrl Pts',(-0.192151945114518,-0.0428317550682234,
1.55484421256164));
#8400=CARTESIAN_POINT('Ctrl Pts',(-0.185328327706693,-0.0629279169161807,
1.55605980344866));
#8401=CARTESIAN_POINT('Ctrl Pts',(-0.164531158441829,-0.124177435250376,
1.55976470774259));
#8402=CARTESIAN_POINT('Ctrl Pts',(-0.110366441153868,-0.174097059683963,
1.56346961203652));
#8403=CARTESIAN_POINT('Ctrl Pts',(-0.0476267394780286,-0.189837313151712,
1.56717451633044));
#8404=CARTESIAN_POINT('Ctrl Pts',(0.0151129621978108,-0.205577566619462,
1.57087942062437));
#8405=CARTESIAN_POINT('Ctrl Pts',(0.0864276482615303,-0.187138449121373,
1.57458432491829));
#8406=CARTESIAN_POINT('Ctrl Pts',(0.133674779789486,-0.142960011983078,
1.57828922921222));
#8407=CARTESIAN_POINT('Ctrl Pts',(0.180921911317442,-0.0987815748447818,
1.58199413350614));
#8408=CARTESIAN_POINT('Ctrl Pts',(0.204101488309635,-0.0288638180662828,
1.58569903780007));
#8409=CARTESIAN_POINT('Ctrl Pts',(0.192603631006867,0.0347901293607817,
1.58940394209399));
#8410=CARTESIAN_POINT('Ctrl Pts',(0.181105773704099,0.0984440767878479,
1.59310884638792));
#8411=CARTESIAN_POINT('Ctrl Pts',(0.134930482106364,0.155834214863477,1.59681375068184));
#8412=CARTESIAN_POINT('Ctrl Pts',(0.0752133572586277,0.180691623125853,
1.60051865497577));
#8413=CARTESIAN_POINT('Ctrl Pts',(0.0154962324108934,0.205549031388229,
1.60422355926969));
#8414=CARTESIAN_POINT('Ctrl Pts',(-0.0577627256868428,0.197873709837356,
1.60792846356362));
#8415=CARTESIAN_POINT('Ctrl Pts',(-0.111031035533165,0.161178847639516,
1.61163336785754));
#8416=CARTESIAN_POINT('Ctrl Pts',(-0.162693586883228,0.125590141933467,
1.61522658883422));
#8417=CARTESIAN_POINT('Ctrl Pts',(-0.195552549538933,0.0627050974813158,
1.6188198098109));
#8418=CARTESIAN_POINT('Ctrl Pts',(-0.195712283470102,-3.61459064724743E-5,
1.62241303078758));
#8419=CARTESIAN_POINT('Origin',(0.,0.,0.));
#8420=CARTESIAN_POINT('',(-0.19536023340508,0.000178280042280071,1.70258696921242));
#8421=CARTESIAN_POINT('',(-0.195332200326426,0.000176344485861957,1.69241303078758));
#8422=CARTESIAN_POINT('',(-0.1954,-2.39295984553393E-17,0.));
#8423=CARTESIAN_POINT('Ctrl Pts',(-0.19536023340508,0.000178280042280071,
1.70258696921242));
#8424=CARTESIAN_POINT('Ctrl Pts',(-0.19550841731601,0.016632826172098,1.70164900895765));
#8425=CARTESIAN_POINT('Ctrl Pts',(-0.193603054742847,0.0330535488509283,
1.70071104870287));
#8426=CARTESIAN_POINT('Ctrl Pts',(-0.189510780251034,0.0489098626792897,
1.6997730884481));
#8427=CARTESIAN_POINT('Ctrl Pts',(-0.17334646490881,0.11154164786371,1.69606818415418));
#8428=CARTESIAN_POINT('Ctrl Pts',(-0.123061569409359,0.165367427987009,
1.69236327986025));
#8429=CARTESIAN_POINT('Ctrl Pts',(-0.0616727646407164,0.185749779542894,
1.68865837556633));
#8430=CARTESIAN_POINT('Ctrl Pts',(-0.000283959872074024,0.206132131098779,
1.6849534712724));
#8431=CARTESIAN_POINT('Ctrl Pts',(0.0722087541657616,0.193071054087249,
1.68124856697847));
#8432=CARTESIAN_POINT('Ctrl Pts',(0.122623625294196,0.152544934423833,1.67754366268455));
#8433=CARTESIAN_POINT('Ctrl Pts',(0.173038496422631,0.112018814760415,1.67383875839062));
#8434=CARTESIAN_POINT('Ctrl Pts',(0.201375524641664,0.0440276524451133,
1.6701338540967));
#8435=CARTESIAN_POINT('Ctrl Pts',(0.194664134075893,-0.0203072746360924,
1.66642894980277));
#8436=CARTESIAN_POINT('Ctrl Pts',(0.187952743510121,-0.0846422017172963,
1.66272404550885));
#8437=CARTESIAN_POINT('Ctrl Pts',(0.146192934159544,-0.145320893564402,
1.65901914121492));
#8438=CARTESIAN_POINT('Ctrl Pts',(0.088499228956397,-0.174569175322524,
1.655314236921));
#8439=CARTESIAN_POINT('Ctrl Pts',(0.0308055237532497,-0.203817457080646,
1.65160933262707));
#8440=CARTESIAN_POINT('Ctrl Pts',(-0.0428220773024696,-0.201635328749786,
1.64790442833315));
#8441=CARTESIAN_POINT('Ctrl Pts',(-0.0986823554860735,-0.169021605762054,
1.64419952403922));
#8442=CARTESIAN_POINT('Ctrl Pts',(-0.154542633669677,-0.136407882774321,
1.64049461974529));
#8443=CARTESIAN_POINT('Ctrl Pts',(-0.192635588981168,-0.0733625651297149,
1.63678971545137));
#8444=CARTESIAN_POINT('Ctrl Pts',(-0.195525110499984,-0.00874309228087092,
1.63308481115744));
#8445=CARTESIAN_POINT('Ctrl Pts',(-0.195654535796742,-0.00584870495917813,
1.63291886384244));
#8446=CARTESIAN_POINT('Ctrl Pts',(-0.195713333973045,-0.00295115947825913,
1.63275291652743));
#8447=CARTESIAN_POINT('Ctrl Pts',(-0.195702834179537,-5.31785447526745E-5,
1.63258696921242));
#8448=CARTESIAN_POINT('Ctrl Pts',(-0.195712283470102,-3.61459064724743E-5,
1.62241303078758));
#8449=CARTESIAN_POINT('Ctrl Pts',(-0.195717248267821,-0.00198624867923799,
1.62252471410483));
#8450=CARTESIAN_POINT('Ctrl Pts',(-0.195690623309908,-0.0039362125300576,
1.62263639742207));
#8451=CARTESIAN_POINT('Ctrl Pts',(-0.195631991350833,-0.00588521351159191,
1.62274808073932));
#8452=CARTESIAN_POINT('Ctrl Pts',(-0.193686975727267,-0.0705400096200497,
1.62645298503325));
#8453=CARTESIAN_POINT('Ctrl Pts',(-0.156519282885226,-0.134135198992158,
1.63015788932717));
#8454=CARTESIAN_POINT('Ctrl Pts',(-0.101141507666876,-0.167561651951873,
1.6338627936211));
#8455=CARTESIAN_POINT('Ctrl Pts',(-0.0457637324485236,-0.200988104911589,
1.63756769791502));
#8456=CARTESIAN_POINT('Ctrl Pts',(0.0278241251461387,-0.204245821458907,
1.64127260220895));
#8457=CARTESIAN_POINT('Ctrl Pts',(0.0859390379816513,-0.175843662179669,
1.64497750650287));
#8458=CARTESIAN_POINT('Ctrl Pts',(0.144053950817164,-0.147441502900431,
1.6486824107968));
#8459=CARTESIAN_POINT('Ctrl Pts',(0.186695918893525,-0.0873794677946378,
1.65238731509072));
#8460=CARTESIAN_POINT('Ctrl Pts',(0.19434663287583,-0.0231494723006056,
1.65609221938465));
#8461=CARTESIAN_POINT('Ctrl Pts',(0.201997346858136,0.0410805231934266,
1.65979712367858));
#8462=CARTESIAN_POINT('Ctrl Pts',(0.174656806746383,0.1094784790757,1.6635020279725));
#8463=CARTESIAN_POINT('Ctrl Pts',(0.124839470558294,0.15073691773648,1.66720693226643));
#8464=CARTESIAN_POINT('Ctrl Pts',(0.0750221343702045,0.19199535639726,1.67091183656035));
#8465=CARTESIAN_POINT('Ctrl Pts',(0.00272800210577999,0.20611427783655,
1.67461674085428));
#8466=CARTESIAN_POINT('Ctrl Pts',(-0.058952069966136,0.186631093938489,
1.6783216451482));
#8467=CARTESIAN_POINT('Ctrl Pts',(-0.120632142038052,0.167147910040428,
1.68202654944213));
#8468=CARTESIAN_POINT('Ctrl Pts',(-0.171698153917458,0.114062620805016,
1.68573145373605));
#8469=CARTESIAN_POINT('Ctrl Pts',(-0.188775897955746,0.0516737082951384,
1.68943635802998));
#8470=CARTESIAN_POINT('Ctrl Pts',(-0.193349552352469,0.0349651006846826,
1.69042858228251));
#8471=CARTESIAN_POINT('Ctrl Pts',(-0.19548542556344,0.0175891981745919,
1.69142080653505));
#8472=CARTESIAN_POINT('Ctrl Pts',(-0.195332200326426,0.000176344485861957,
1.69241303078758));
#8473=CARTESIAN_POINT('Origin',(0.,0.,0.));
#8474=CARTESIAN_POINT('',(-0.195093080635393,-5.39352580709168E-5,1.77258696921242));
#8475=CARTESIAN_POINT('',(-0.1951020484266,-6.86943200097011E-5,1.76241303078758));
#8476=CARTESIAN_POINT('',(-0.1954,-2.39295984553393E-17,0.));
#8477=CARTESIAN_POINT('Ctrl Pts',(-0.195093080635393,-5.39352580709168E-5,
1.77258696921242));
#8478=CARTESIAN_POINT('Ctrl Pts',(-0.195004235779033,0.0358901483346491,
1.77054510138787));
#8479=CARTESIAN_POINT('Ctrl Pts',(-0.185501828716737,0.0718779233040721,
1.76850323356331));
#8480=CARTESIAN_POINT('Ctrl Pts',(-0.166873611769098,0.102272714806047,
1.76646136573876));
#8481=CARTESIAN_POINT('Ctrl Pts',(-0.133073303968799,0.157423098290437,
1.76275646144483));
#8482=CARTESIAN_POINT('Ctrl Pts',(-0.0692281383564483,0.194159730542236,
1.75905155715091));
#8483=CARTESIAN_POINT('Ctrl Pts',(-0.0045616650676435,0.195667324074495,
1.75534665285698));
#8484=CARTESIAN_POINT('Ctrl Pts',(0.0601048082211613,0.197174917606755,
1.75164174856306));
#8485=CARTESIAN_POINT('Ctrl Pts',(0.12559258918642,0.163453472419475,1.74793684426913));
#8486=CARTESIAN_POINT('Ctrl Pts',(0.161926261021679,0.109938148475413,1.74423193997521));
#8487=CARTESIAN_POINT('Ctrl Pts',(0.198259932856938,0.0564228245313505,
1.74052703568128));
#8488=CARTESIAN_POINT('Ctrl Pts',(0.205439495562197,-0.0168863781694949,
1.73682213138736));
#8489=CARTESIAN_POINT('Ctrl Pts',(0.180178681357328,-0.0764339798976696,
1.73311722709343));
#8490=CARTESIAN_POINT('Ctrl Pts',(0.154917867152459,-0.135981581625844,
1.7294123227995));
#8491=CARTESIAN_POINT('Ctrl Pts',(0.097216676037462,-0.181767582381348,
1.72570741850558));
#8492=CARTESIAN_POINT('Ctrl Pts',(0.0334864053323433,-0.192834569402327,
1.72200251421165));
#8493=CARTESIAN_POINT('Ctrl Pts',(-0.0302438653727754,-0.203901556423306,
1.71829760991773));
#8494=CARTESIAN_POINT('Ctrl Pts',(-0.100003215668016,-0.180249529709759,
1.7145927056238));
#8495=CARTESIAN_POINT('Ctrl Pts',(-0.143861023223137,-0.132704621230215,
1.71088780132988));
#8496=CARTESIAN_POINT('Ctrl Pts',(-0.176615472341799,-0.097196524212656,
1.70812085729073));
#8497=CARTESIAN_POINT('Ctrl Pts',(-0.194923096983834,-0.0483619519122345,
1.70535391325157));
#8498=CARTESIAN_POINT('Ctrl Pts',(-0.19536023340508,0.000178280042280071,
1.70258696921242));
#8499=CARTESIAN_POINT('Ctrl Pts',(-0.195332200326426,0.000176344485861957,
1.69241303078758));
#8500=CARTESIAN_POINT('Ctrl Pts',(-0.194913291958459,-0.0474293258497361,
1.69512571082897));
#8501=CARTESIAN_POINT('Ctrl Pts',(-0.177384701551267,-0.0953111847948915,
1.69783839087036));
#8502=CARTESIAN_POINT('Ctrl Pts',(-0.14578470180404,-0.130588408742416,
1.70055107091176));
#8503=CARTESIAN_POINT('Ctrl Pts',(-0.102626285416879,-0.178769077485746,
1.70425597520568));
#8504=CARTESIAN_POINT('Ctrl Pts',(-0.0332199764453863,-0.203437879188069,
1.70796087949961));
#8505=CARTESIAN_POINT('Ctrl Pts',(0.030665198740133,-0.193303278203442,
1.71166578379353));
#8506=CARTESIAN_POINT('Ctrl Pts',(0.0945503739256559,-0.183168677218815,
1.71537068808746));
#8507=CARTESIAN_POINT('Ctrl Pts',(0.152914415325207,-0.138230673547234,
1.71907559238138));
#8508=CARTESIAN_POINT('Ctrl Pts',(0.179042622246928,-0.0790585301970201,
1.72278049667531));
#8509=CARTESIAN_POINT('Ctrl Pts',(0.205170829168648,-0.0198863868468077,
1.72648540096923));
#8510=CARTESIAN_POINT('Ctrl Pts',(0.199063201612543,0.053519896182033,1.73019030526316));
#8511=CARTESIAN_POINT('Ctrl Pts',(0.163515355478164,0.107560403033919,1.73389520955708));
#8512=CARTESIAN_POINT('Ctrl Pts',(0.127967509343785,0.161600909885804,1.73760011385101));
#8513=CARTESIAN_POINT('Ctrl Pts',(0.0629794446311314,0.196275640560732,
1.74130501814494));
#8514=CARTESIAN_POINT('Ctrl Pts',(-0.00170215464495672,0.195713092172021,
1.74500992243886));
#8515=CARTESIAN_POINT('Ctrl Pts',(-0.0663837539210485,0.19515054378331,
1.74871482673279));
#8516=CARTESIAN_POINT('Ctrl Pts',(-0.130758887760577,0.159350716330956,
1.75241973102671));
#8517=CARTESIAN_POINT('Ctrl Pts',(-0.165361426140981,0.104700098006593,
1.75612463532064));
#8518=CARTESIAN_POINT('Ctrl Pts',(-0.184938580117925,0.0737802979009116,
1.75822076714295));
#8519=CARTESIAN_POINT('Ctrl Pts',(-0.194985580686779,0.0368263940799281,
1.76031689896526));
#8520=CARTESIAN_POINT('Ctrl Pts',(-0.1951020484266,-6.86943200097011E-5,
1.76241303078758));
#8521=CARTESIAN_POINT('Origin',(0.,0.,0.));
#8522=CARTESIAN_POINT('',(-0.195557989435191,-0.000150381408634326,1.84258696921242));
#8523=CARTESIAN_POINT('',(-0.195583821122648,-0.000140590296505579,1.83241303078758));
#8524=CARTESIAN_POINT('',(-0.1954,-2.39295984553393E-17,0.));
#8525=CARTESIAN_POINT('Ctrl Pts',(-0.195557989435191,-0.000150381408634326,
1.84258696921242));
#8526=CARTESIAN_POINT('Ctrl Pts',(-0.195089679602252,0.054892193728964,
1.83944119381809));
#8527=CARTESIAN_POINT('Ctrl Pts',(-0.170755613617913,0.110297227528981,
1.83629541842375));
#8528=CARTESIAN_POINT('Ctrl Pts',(-0.129599212359622,0.14666476964298,1.83314964302941));
#8529=CARTESIAN_POINT('Ctrl Pts',(-0.0811276882899435,0.189496264599762,
1.82944473873549));
#8530=CARTESIAN_POINT('Ctrl Pts',(-0.00932239762518191,0.205921414639302,
1.82573983444156));
#8531=CARTESIAN_POINT('Ctrl Pts',(0.0529495585532175,0.18842201237563,1.82203493014764));
#8532=CARTESIAN_POINT('Ctrl Pts',(0.115221514731615,0.17092261011196,1.81833002585371));
#8533=CARTESIAN_POINT('Ctrl Pts',(0.167960136423649,0.119498655545081,1.81462512155979));
#8534=CARTESIAN_POINT('Ctrl Pts',(0.187025620085586,0.0576881957619144,
1.81092021726586));
#8535=CARTESIAN_POINT('Ctrl Pts',(0.206091103747522,-0.00412226402125245,
1.80721531297194));
#8536=CARTESIAN_POINT('Ctrl Pts',(0.191483449379358,-0.0763192290207106,
1.80351040867801));
#8537=CARTESIAN_POINT('Ctrl Pts',(0.149888950542983,-0.125856318887,1.79980550438409));
#8538=CARTESIAN_POINT('Ctrl Pts',(0.108294451706606,-0.17539340875329,1.79610060009016));
#8539=CARTESIAN_POINT('Ctrl Pts',(0.0397131084020174,-0.202270623486414,
1.79239569579624));
#8540=CARTESIAN_POINT('Ctrl Pts',(-0.0244636606908309,-0.194185580835104,
1.78869079150231));
#8541=CARTESIAN_POINT('Ctrl Pts',(-0.0886404297836792,-0.186100538183794,
1.78498588720838));
#8542=CARTESIAN_POINT('Ctrl Pts',(-0.148412624664785,-0.14305323814805,
1.78128098291446));
#8543=CARTESIAN_POINT('Ctrl Pts',(-0.176420997111215,-0.0847475207716867,
1.77757607862053));
#8544=CARTESIAN_POINT('Ctrl Pts',(-0.188993236805098,-0.0585755803713125,
1.77591304215116));
#8545=CARTESIAN_POINT('Ctrl Pts',(-0.195165441948141,-0.0293292493376349,
1.77425000568179));
#8546=CARTESIAN_POINT('Ctrl Pts',(-0.195093080635393,-5.39352580709168E-5,
1.77258696921242));
#8547=CARTESIAN_POINT('Ctrl Pts',(-0.1951020484266,-6.86943200097011E-5,
1.76241303078758));
#8548=CARTESIAN_POINT('Ctrl Pts',(-0.195191436933401,-0.0283855214983397,
1.76402180325919));
#8549=CARTESIAN_POINT('Ctrl Pts',(-0.189431246293547,-0.0566677034601064,
1.7656305757308));
#8550=CARTESIAN_POINT('Ctrl Pts',(-0.177640467639129,-0.0821606720695544,
1.76723934820241));
#8551=CARTESIAN_POINT('Ctrl Pts',(-0.150487027835591,-0.14086941462497,
1.77094425249634));
#8552=CARTESIAN_POINT('Ctrl Pts',(-0.0913502053072345,-0.18478549053943,
1.77464915679026));
#8553=CARTESIAN_POINT('Ctrl Pts',(-0.0272984222508209,-0.193807399034674,
1.77835406108419));
#8554=CARTESIAN_POINT('Ctrl Pts',(0.0367533608055927,-0.202829307529917,
1.78205896537811));
#8555=CARTESIAN_POINT('Ctrl Pts',(0.105720104390061,-0.176957048605944,
1.78576386967204));
#8556=CARTESIAN_POINT('Ctrl Pts',(0.148033982348499,-0.128033010774619,
1.78946877396596));
#8557=CARTESIAN_POINT('Ctrl Pts',(0.190347860306936,-0.0791089729432942,
1.79317367825989));
#8558=CARTESIAN_POINT('Ctrl Pts',(0.206008872639341,-0.00713315620461422,
1.79687858255381));
#8559=CARTESIAN_POINT('Ctrl Pts',(0.187848577151528,0.0549492842548083,
1.80058348684774));
#8560=CARTESIAN_POINT('Ctrl Pts',(0.169688281663715,0.117031724714231,1.80428839114167));
#8561=CARTESIAN_POINT('Ctrl Pts',(0.117706678355686,0.169220788894399,1.80799329543559));
#8562=CARTESIAN_POINT('Ctrl Pts',(0.0556970642739923,0.187628219650532,
1.81169819972952));
#8563=CARTESIAN_POINT('Ctrl Pts',(-0.00631254980769992,0.206035650406663,
1.81540310402344));
#8564=CARTESIAN_POINT('Ctrl Pts',(-0.0783501746630549,0.190661447738761,
1.81910800831737));
#8565=CARTESIAN_POINT('Ctrl Pts',(-0.127442363964252,0.148542773789816,
1.82281291261129));
#8566=CARTESIAN_POINT('Ctrl Pts',(-0.169844792514325,0.112163584184181,
1.82601295200339));
#8567=CARTESIAN_POINT('Ctrl Pts',(-0.195129223210545,0.0558321996894708,
1.82921299139548));
#8568=CARTESIAN_POINT('Ctrl Pts',(-0.195583821122648,-0.000140590296505579,
1.83241303078758));
#8569=CARTESIAN_POINT('Origin',(0.,0.,0.));
#8570=CARTESIAN_POINT('',(-0.195564939510846,0.000147924627282119,1.91258696921242));
#8571=CARTESIAN_POINT('',(-0.195538264906755,0.000156701382499669,1.90241303078758));
#8572=CARTESIAN_POINT('',(-0.1954,-2.39295984553393E-17,0.));
#8573=CARTESIAN_POINT('Ctrl Pts',(-0.195564939510846,0.000147924627282119,
1.91258696921242));
#8574=CARTESIAN_POINT('Ctrl Pts',(-0.195645138896524,0.00967919899870748,
1.91204219054223));
#8575=CARTESIAN_POINT('Ctrl Pts',(-0.195008580056017,0.0191997185565135,
1.91149741187204));
#8576=CARTESIAN_POINT('Ctrl Pts',(-0.193618292474229,0.0286088678214767,
1.91095263320185));
#8577=CARTESIAN_POINT('Ctrl Pts',(-0.184163292281677,0.0925981526840929,
1.90724772890792));
#8578=CARTESIAN_POINT('Ctrl Pts',(-0.139848172472072,0.151436537073306,
1.903542824614));
#8579=CARTESIAN_POINT('Ctrl Pts',(-0.0809570863262455,0.178192201491052,
1.89983792032007));
#8580=CARTESIAN_POINT('Ctrl Pts',(-0.0220660001804177,0.204947865908799,
1.89613301602615));
#8581=CARTESIAN_POINT('Ctrl Pts',(0.0514010523016335,0.199620810355078,
1.89242811173222));
#8582=CARTESIAN_POINT('Ctrl Pts',(0.105816339545683,0.164649363144276,1.8887232074383));
#8583=CARTESIAN_POINT('Ctrl Pts',(0.16023162678973,0.129677915933475,1.88501830314437));
#8584=CARTESIAN_POINT('Ctrl Pts',(0.19559514879578,0.0650620770655954,1.88131339885044));
#8585=CARTESIAN_POINT('Ctrl Pts',(0.195720125430942,0.000378153354130759,
1.87760849455652));
#8586=CARTESIAN_POINT('Ctrl Pts',(0.195845102066104,-0.0643057703573357,
1.87390359026259));
#8587=CARTESIAN_POINT('Ctrl Pts',(0.160731533330379,-0.129057778912385,
1.87019868596867));
#8588=CARTESIAN_POINT('Ctrl Pts',(0.106451789411018,-0.164239237181177,
1.86649378167474));
#8589=CARTESIAN_POINT('Ctrl Pts',(0.0521720454916558,-0.199420695449971,
1.86278887738082));
#8590=CARTESIAN_POINT('Ctrl Pts',(-0.0212738736113445,-0.2050316034325,
1.85908397308689));
#8591=CARTESIAN_POINT('Ctrl Pts',(-0.080267909606869,-0.1785037063649,1.85537906879297));
#8592=CARTESIAN_POINT('Ctrl Pts',(-0.139261945602394,-0.1519758092973,1.85167416449904));
#8593=CARTESIAN_POINT('Ctrl Pts',(-0.183804098490444,-0.0933091071795703,
1.84796926020512));
#8594=CARTESIAN_POINT('Ctrl Pts',(-0.193506296197169,-0.0293568361836938,
1.84426435591119));
#8595=CARTESIAN_POINT('Ctrl Pts',(-0.194970511922324,-0.0197054227944751,
1.8437052270116));
#8596=CARTESIAN_POINT('Ctrl Pts',(-0.195641226643426,-0.00993362738438461,
1.84314609811201));
#8597=CARTESIAN_POINT('Ctrl Pts',(-0.195557989435191,-0.000150381408634326,
1.84258696921242));
#8598=CARTESIAN_POINT('Ctrl Pts',(-0.195583821122648,-0.000140590296505579,
1.83241303078758));
#8599=CARTESIAN_POINT('Ctrl Pts',(-0.195655542280467,-0.0089713244403536,
1.83291789568941));
#8600=CARTESIAN_POINT('Ctrl Pts',(-0.195109227819557,-0.0177931328624295,
1.83342276059124));
#8601=CARTESIAN_POINT('Ctrl Pts',(-0.193914593457294,-0.0265262553380925,
1.83392762549307));
#8602=CARTESIAN_POINT('Ctrl Pts',(-0.185147879902098,-0.0906134652870637,
1.837632529787));
#8603=CARTESIAN_POINT('Ctrl Pts',(-0.141467699044668,-0.149924739955016,
1.84133743408092));
#8604=CARTESIAN_POINT('Ctrl Pts',(-0.0828675765180874,-0.177311805980279,
1.84504233837484));
#8605=CARTESIAN_POINT('Ctrl Pts',(-0.0242674539915072,-0.204698872005543,
1.84874724266877));
#8606=CARTESIAN_POINT('Ctrl Pts',(0.0492526102042225,-0.200161729388119,
1.8524521469627));
#8607=CARTESIAN_POINT('Ctrl Pts',(0.104040619690215,-0.165777143275077,
1.85615705125662));
#8608=CARTESIAN_POINT('Ctrl Pts',(0.158828629176207,-0.131392557162035,
1.85986195555055));
#8609=CARTESIAN_POINT('Ctrl Pts',(0.194884583952461,-0.0671605275533752,
1.86356685984447));
#8610=CARTESIAN_POINT('Ctrl Pts',(0.195704759860937,-0.00248168203892953,
1.8672717641384));
#8611=CARTESIAN_POINT('Ctrl Pts',(0.196524935769412,0.062197163475518,1.87097666843232));
#8612=CARTESIAN_POINT('Ctrl Pts',(0.162109332810106,0.127322824895751,1.87468157272625));
#8613=CARTESIAN_POINT('Ctrl Pts',(0.108210844547972,0.163085636707173,1.87838647702018));
#8614=CARTESIAN_POINT('Ctrl Pts',(0.0543123562858388,0.198848448518593,
1.8820913813141));
#8615=CARTESIAN_POINT('Ctrl Pts',(-0.0190690172791211,0.205248410721205,
1.88579628560802));
#8616=CARTESIAN_POINT('Ctrl Pts',(-0.0783447619841414,0.179356098439996,
1.88950118990195));
#8617=CARTESIAN_POINT('Ctrl Pts',(-0.13762050668916,0.153463786158788,1.89320609419588));
#8618=CARTESIAN_POINT('Ctrl Pts',(-0.18279062253424,0.0952791993937629,
1.8969109984898));
#8619=CARTESIAN_POINT('Ctrl Pts',(-0.193179602887536,0.031434897903176,
1.90061590278373));
#8620=CARTESIAN_POINT('Ctrl Pts',(-0.194859387846714,0.0211119697883842,
1.90121494545168));
#8621=CARTESIAN_POINT('Ctrl Pts',(-0.195629876801359,0.0106410776720159,
1.90181398811963));
#8622=CARTESIAN_POINT('Ctrl Pts',(-0.195538264906755,0.000156701382499669,
1.90241303078758));
#8623=CARTESIAN_POINT('Origin',(0.,0.,0.));
#8624=CARTESIAN_POINT('',(-0.195095239123403,5.78821923055833E-5,1.98258696921242));
#8625=CARTESIAN_POINT('',(-0.195087892673083,4.28153426326047E-5,1.97241303078758));
#8626=CARTESIAN_POINT('',(-0.1954,-2.39295984553393E-17,0.));
#8627=CARTESIAN_POINT('Ctrl Pts',(-0.195095239123403,5.78821923055833E-5,
1.98258696921242));
#8628=CARTESIAN_POINT('Ctrl Pts',(-0.19517227391142,0.0290797798957806,
1.98093828297245));
#8629=CARTESIAN_POINT('Ctrl Pts',(-0.189110562653447,0.0580710867028783,
1.97928959673248));
#8630=CARTESIAN_POINT('Ctrl Pts',(-0.176747162247964,0.0840651600602401,
1.97764091049251));
#8631=CARTESIAN_POINT('Ctrl Pts',(-0.148964304516005,0.14247867238501,1.97393600619858));
#8632=CARTESIAN_POINT('Ctrl Pts',(-0.0893588997550408,0.185756623405738,
1.97023110190465));
#8633=CARTESIAN_POINT('Ctrl Pts',(-0.0252138521235489,0.1940895982781,1.96652619761073));
#8634=CARTESIAN_POINT('Ctrl Pts',(0.0389311955079449,0.202422573150462,
1.9628212933168));
#8635=CARTESIAN_POINT('Ctrl Pts',(0.107615886009967,0.175810571874455,1.95911638902288));
#8636=CARTESIAN_POINT('Ctrl Pts',(0.149401496071477,0.12643458178152,1.95541148472895));
#8637=CARTESIAN_POINT('Ctrl Pts',(0.191187106132985,0.0770585916885855,
1.95170658043503));
#8638=CARTESIAN_POINT('Ctrl Pts',(0.206073635753984,0.00491861277872399,
1.9480016761411));
#8639=CARTESIAN_POINT('Ctrl Pts',(0.187247143102674,-0.0569650585758442,
1.94429677184718));
#8640=CARTESIAN_POINT('Ctrl Pts',(0.168420650451363,-0.118848729930418,
1.94059186755325));
#8641=CARTESIAN_POINT('Ctrl Pts',(0.115881135527736,-0.170476093729696,
1.93688696325933));
#8642=CARTESIAN_POINT('Ctrl Pts',(0.0536772656622717,-0.188215997326701,
1.9331820589654));
#8643=CARTESIAN_POINT('Ctrl Pts',(-0.00852660420318736,-0.205955900923705,
1.92947715467148));
#8644=CARTESIAN_POINT('Ctrl Pts',(-0.0803948290104825,-0.189808344318442,
1.92577225037755));
#8645=CARTESIAN_POINT('Ctrl Pts',(-0.129031501126381,-0.147164473347801,
1.92206734608362));
#8646=CARTESIAN_POINT('Ctrl Pts',(-0.170516511699694,-0.110791067003543,
1.91890722045989));
#8647=CARTESIAN_POINT('Ctrl Pts',(-0.195099722813576,-0.0551406283503992,
1.91574709483616));
#8648=CARTESIAN_POINT('Ctrl Pts',(-0.195564939510846,0.000147924627282119,
1.91258696921242));
#8649=CARTESIAN_POINT('Ctrl Pts',(-0.195538264906755,0.000156701382499669,
1.90241303078758));
#8650=CARTESIAN_POINT('Ctrl Pts',(-0.195063283936023,-0.0542017337207628,
1.90551889241355));
#8651=CARTESIAN_POINT('Ctrl Pts',(-0.171413995491211,-0.108922639612492,
1.90862475403953));
#8652=CARTESIAN_POINT('Ctrl Pts',(-0.131168044975528,-0.145263401293193,
1.9117306156655));
#8653=CARTESIAN_POINT('Ctrl Pts',(-0.0831596618487121,-0.188613382782822,
1.91543551995943));
#8654=CARTESIAN_POINT('Ctrl Pts',(-0.0115350507335688,-0.205809329545931,
1.91914042425335));
#8655=CARTESIAN_POINT('Ctrl Pts',(0.0509213888967292,-0.188980221004203,
1.92284532854728));
#8656=CARTESIAN_POINT('Ctrl Pts',(0.113377828527027,-0.172151112462475,
1.9265502328412));
#8657=CARTESIAN_POINT('Ctrl Pts',(0.166666096672482,-0.12129694861591,1.93025513713513));
#8658=CARTESIAN_POINT('Ctrl Pts',(0.186394802679598,-0.0596949689002616,
1.93396004142905));
#8659=CARTESIAN_POINT('Ctrl Pts',(0.206123508686714,0.00190701081538635,
1.93766494572298));
#8660=CARTESIAN_POINT('Ctrl Pts',(0.192292652555493,0.0742568064001138,
1.94136985001691));
#8661=CARTESIAN_POINT('Ctrl Pts',(0.151232967610728,0.124238083072873,1.94507475431083));
#8662=CARTESIAN_POINT('Ctrl Pts',(0.11017328266596,0.174219359745633,1.94877965860476));
#8663=CARTESIAN_POINT('Ctrl Pts',(0.041884768907644,0.201832117506419,1.95248456289868));
#8664=CARTESIAN_POINT('Ctrl Pts',(-0.0223751904878854,0.19443729742156,
1.95618946719261));
#8665=CARTESIAN_POINT('Ctrl Pts',(-0.086635149883413,0.187042477336701,
1.95989437148653));
#8666=CARTESIAN_POINT('Ctrl Pts',(-0.146866554916156,0.144640079406198,
1.96359927578046));
#8667=CARTESIAN_POINT('Ctrl Pts',(-0.175499965240401,0.0866387556384964,
1.96730418007438));
#8668=CARTESIAN_POINT('Ctrl Pts',(-0.188661242577225,0.0599785883945253,
1.96900713031211));
#8669=CARTESIAN_POINT('Ctrl Pts',(-0.195146625645364,0.0300227443028642,
1.97071008054985));
#8670=CARTESIAN_POINT('Ctrl Pts',(-0.195087892673083,4.28153426326047E-5,
1.97241303078758));
#8671=CARTESIAN_POINT('Origin',(0.,0.,0.));
#8672=CARTESIAN_POINT('',(-0.195352761517788,-0.000177909769055379,2.05258696921242));
#8673=CARTESIAN_POINT('',(-0.195381194231368,-0.000178768183475579,2.04241303078758));
#8674=CARTESIAN_POINT('',(-0.1954,-2.39295984553393E-17,0.));
#8675=CARTESIAN_POINT('Ctrl Pts',(-0.195352761517788,-0.000177909769055379,
2.05258696921242));
#8676=CARTESIAN_POINT('Ctrl Pts',(-0.194920193265683,0.0481152823703308,
2.04983437540267));
#8677=CARTESIAN_POINT('Ctrl Pts',(-0.176820579764667,0.0966981301161916,
2.04708178159292));
#8678=CARTESIAN_POINT('Ctrl Pts',(-0.144372747816328,0.132147721079886,
2.04432918778316));
#8679=CARTESIAN_POINT('Ctrl Pts',(-0.100698991271494,0.179861750412485,
2.04062428348924));
#8680=CARTESIAN_POINT('Ctrl Pts',(-0.0310315582308591,0.20378316539473,
2.03691937919531));
#8681=CARTESIAN_POINT('Ctrl Pts',(0.0327410018324499,0.192962528221534,
2.03321447490139));
#8682=CARTESIAN_POINT('Ctrl Pts',(0.096513561895759,0.182141891048337,2.02950957060746));
#8683=CARTESIAN_POINT('Ctrl Pts',(0.154391248981745,0.136579201719707,2.02580466631354));
#8684=CARTESIAN_POINT('Ctrl Pts',(0.179881979091815,0.0771296576985378,
2.02209976201961));
#8685=CARTESIAN_POINT('Ctrl Pts',(0.205372709201885,0.0176801136773685,
2.01839485772569));
#8686=CARTESIAN_POINT('Ctrl Pts',(0.198476482336034,-0.055656285036337,
2.01468995343176));
#8687=CARTESIAN_POINT('Ctrl Pts',(0.162349876281112,-0.109311610408804,
2.01098504913783));
#8688=CARTESIAN_POINT('Ctrl Pts',(0.12622327022619,-0.162966935781272,2.00728014484391));
#8689=CARTESIAN_POINT('Ctrl Pts',(0.0608662849821969,-0.196941187812501,
2.00357524054998));
#8690=CARTESIAN_POINT('Ctrl Pts',(-0.0038055311604717,-0.195683490441188,
1.99987033625606));
#8691=CARTESIAN_POINT('Ctrl Pts',(-0.0684773473031403,-0.194425793069875,
1.99616543196213));
#8692=CARTESIAN_POINT('Ctrl Pts',(-0.132463994344484,-0.15793614629602,
1.99246052766821));
#8693=CARTESIAN_POINT('Ctrl Pts',(-0.16647716251368,-0.102916786094686,
1.98875562337428));
#8694=CARTESIAN_POINT('Ctrl Pts',(-0.185354435693536,-0.072381098047782,
1.98669940532033));
#8695=CARTESIAN_POINT('Ctrl Pts',(-0.194999162430299,-0.0361378162802388,
1.98464318726638));
#8696=CARTESIAN_POINT('Ctrl Pts',(-0.195095239123403,5.78821923055833E-5,
1.98258696921242));
#8697=CARTESIAN_POINT('Ctrl Pts',(-0.195087892673083,4.28153426326047E-5,
1.97241303078758));
#8698=CARTESIAN_POINT('Ctrl Pts',(-0.195018847371885,-0.0352009863002633,
1.97441498484377));
#8699=CARTESIAN_POINT('Ctrl Pts',(-0.18590591169575,-0.0704780729444801,
1.97641693889997));
#8700=CARTESIAN_POINT('Ctrl Pts',(-0.167963177482808,-0.100473293903646,
1.97841889295616));
#8701=CARTESIAN_POINT('Ctrl Pts',(-0.13475756378522,-0.155983770073185,
1.98212379725009));
#8702=CARTESIAN_POINT('Ctrl Pts',(-0.0713109207742939,-0.19340447280736,
1.98582870154401));
#8703=CARTESIAN_POINT('Ctrl Pts',(-0.00666438469241006,-0.195606998225116,
1.98953360583794));
#8704=CARTESIAN_POINT('Ctrl Pts',(0.0579821513894738,-0.197809523642872,
1.99323851013186));
#8705=CARTESIAN_POINT('Ctrl Pts',(0.123828580542316,-0.164793871744207,
1.99694341442579));
#8706=CARTESIAN_POINT('Ctrl Pts',(0.160735323596081,-0.111672143018891,
2.00064831871971));
#8707=CARTESIAN_POINT('Ctrl Pts',(0.197642066649846,-0.0585504142935751,
2.00435322301364));
#8708=CARTESIAN_POINT('Ctrl Pts',(0.205609123604535,0.0146773912583926,
2.00805812730756));
#8709=CARTESIAN_POINT('Ctrl Pts',(0.180989770606949,0.0744930514451918,
2.01176303160149));
#8710=CARTESIAN_POINT('Ctrl Pts',(0.156370417609364,0.134308711631991,2.01546793589541));
#8711=CARTESIAN_POINT('Ctrl Pts',(0.0991646546595033,0.180712226453622,
2.01917284018934));
#8712=CARTESIAN_POINT('Ctrl Pts',(0.0355570090520971,0.192463531312391,
2.02287774448326));
#8713=CARTESIAN_POINT('Ctrl Pts',(-0.0280506365553108,0.20421483617116,
2.02658264877719));
#8714=CARTESIAN_POINT('Ctrl Pts',(-0.098060164820265,0.181313931067065,
2.03028755307112));
#8715=CARTESIAN_POINT('Ctrl Pts',(-0.142426440616362,0.134243140574553,
2.03399245736504));
#8716=CARTESIAN_POINT('Ctrl Pts',(-0.176038598375119,0.0985820261926483,
2.03679931517255));
#8717=CARTESIAN_POINT('Ctrl Pts',(-0.194932378367354,0.0490481979593188,
2.03960617298007));
#8718=CARTESIAN_POINT('Ctrl Pts',(-0.195381194231368,-0.000178768183475579,
2.04241303078758));
#8719=CARTESIAN_POINT('Origin',(0.,0.,0.));
#8720=CARTESIAN_POINT('',(-0.195705652066383,4.87247307793624E-5,2.12258696921242));
#8721=CARTESIAN_POINT('',(-0.195693853754418,6.53393013630089E-5,2.11241303078758));
#8722=CARTESIAN_POINT('',(-0.1954,-2.39295984553393E-17,0.));
#8723=CARTESIAN_POINT('Ctrl Pts',(-0.195705652066383,4.87247307793624E-5,
2.12258696921242));
#8724=CARTESIAN_POINT('Ctrl Pts',(-0.195714515890613,0.0026960020070379,
2.12243537212681));
#8725=CARTESIAN_POINT('Ctrl Pts',(-0.195665450924563,0.0053429432466519,
2.12228377504121));
#8726=CARTESIAN_POINT('Ctrl Pts',(-0.195557435859476,0.00798747668964042,
2.1221321779556));
#8727=CARTESIAN_POINT('Ctrl Pts',(-0.192917639211396,0.07261763279738,2.11842727366167));
#8728=CARTESIAN_POINT('Ctrl Pts',(-0.155068588696691,0.1358096789777,2.11472236936775));
#8729=CARTESIAN_POINT('Ctrl Pts',(-0.0993347538758449,0.168639014380346,
2.11101746507382));
#8730=CARTESIAN_POINT('Ctrl Pts',(-0.0436009190549989,0.201468349782991,
2.10731256077989));
#8731=CARTESIAN_POINT('Ctrl Pts',(0.030017700071986,0.203934974407961,2.10360765648597));
#8732=CARTESIAN_POINT('Ctrl Pts',(0.0878239960609676,0.174909851675304,
2.09990275219204));
#8733=CARTESIAN_POINT('Ctrl Pts',(0.145630292049948,0.145884728942649,2.09619784789812));
#8734=CARTESIAN_POINT('Ctrl Pts',(0.187624264900923,0.0853678588523708,
2.09249294360419));
#8735=CARTESIAN_POINT('Ctrl Pts',(0.194584209101134,0.0210593463327518,
2.08878803931027));
#8736=CARTESIAN_POINT('Ctrl Pts',(0.201544153301344,-0.0432491661868709,
2.08508313501634));
#8737=CARTESIAN_POINT('Ctrl Pts',(0.173470068850782,-0.111349321135837,
2.08137823072242));
#8738=CARTESIAN_POINT('Ctrl Pts',(0.123212175605713,-0.15206995193368,2.07767332642849));
#8739=CARTESIAN_POINT('Ctrl Pts',(0.0729542823606449,-0.192790582731522,
2.07396842213457));
#8740=CARTESIAN_POINT('Ctrl Pts',(0.000512580321072716,-0.206131689378248,
2.07026351784064));
#8741=CARTESIAN_POINT('Ctrl Pts',(-0.0609545278221702,-0.18598670930055,
2.06655861354672));
#8742=CARTESIAN_POINT('Ctrl Pts',(-0.122421635965411,-0.165841729222853,
2.06285370925279));
#8743=CARTESIAN_POINT('Ctrl Pts',(-0.172914150212319,-0.112210662420741,
2.05914880495886));
#8744=CARTESIAN_POINT('Ctrl Pts',(-0.189320367311259,-0.0496418071782075,
2.05544390066494));
#8745=CARTESIAN_POINT('Ctrl Pts',(-0.193537429699225,-0.0335590768016581,
2.05449159018077));
#8746=CARTESIAN_POINT('Ctrl Pts',(-0.195502416465111,-0.0168858283241024,
2.05353927969659));
#8747=CARTESIAN_POINT('Ctrl Pts',(-0.195352761517788,-0.000177909769055379,
2.05258696921242));
#8748=CARTESIAN_POINT('Ctrl Pts',(-0.195381194231368,-0.000178768183475579,
2.04241303078758));
#8749=CARTESIAN_POINT('Ctrl Pts',(-0.195524791640772,-0.0159288014993712,
2.04331107727399));
#8750=CARTESIAN_POINT('Ctrl Pts',(-0.193780247164878,-0.0316474224925252,
2.0442091237604));
#8751=CARTESIAN_POINT('Ctrl Pts',(-0.19002550838013,-0.0468702244805944,
2.04510717024682));
#8752=CARTESIAN_POINT('Ctrl Pts',(-0.174535277020564,-0.10967212316231,
2.04881207454074));
#8753=CARTESIAN_POINT('Ctrl Pts',(-0.124831790974193,-0.164035244644817,
2.05251697883467));
#8754=CARTESIAN_POINT('Ctrl Pts',(-0.0636655952897654,-0.18507621066562,
2.05622188312859));
#8755=CARTESIAN_POINT('Ctrl Pts',(-0.00249939960533398,-0.206117176686425,
2.05992678742252));
#8756=CARTESIAN_POINT('Ctrl Pts',(0.0701295057171544,-0.193835987245522,
2.06363169171644));
#8757=CARTESIAN_POINT('Ctrl Pts',(0.120977030297591,-0.1538540539548,2.06733659601037));
#8758=CARTESIAN_POINT('Ctrl Pts',(0.171824554878027,-0.113872120664079,
2.0710415003043));
#8759=CARTESIAN_POINT('Ctrl Pts',(0.200890698716412,-0.0461894435235373,
2.07474640459822));
#8760=CARTESIAN_POINT('Ctrl Pts',(0.194871151241538,0.0182139010618868,
2.07845130889215));
#8761=CARTESIAN_POINT('Ctrl Pts',(0.188851603766663,0.082617245647309,2.08215621318607));
#8762=CARTESIAN_POINT('Ctrl Pts',(0.147746364978535,0.143741257677616,2.08586111748));
#8763=CARTESIAN_POINT('Ctrl Pts',(0.090370344278156,0.173607927966511,2.08956602177392));
#8764=CARTESIAN_POINT('Ctrl Pts',(0.0329943235777734,0.203474598255409,
2.09327092606785));
#8765=CARTESIAN_POINT('Ctrl Pts',(-0.0406524790348606,0.20208392680289,
2.09697583036177));
#8766=CARTESIAN_POINT('Ctrl Pts',(-0.0968600557997058,0.170072459170759,
2.1006807346557));
#8767=CARTESIAN_POINT('Ctrl Pts',(-0.153067632564546,0.138060991538631,
2.10438563894962));
#8768=CARTESIAN_POINT('Ctrl Pts',(-0.1918359834816,0.0754287277268964,2.10809054324355));
#8769=CARTESIAN_POINT('Ctrl Pts',(-0.195419851939884,0.0108440419851374,
2.11179544753747));
#8770=CARTESIAN_POINT('Ctrl Pts',(-0.195618987729891,0.00725542745666287,
2.11200130862084));
#8771=CARTESIAN_POINT('Ctrl Pts',(-0.195709494543343,0.00366078499822498,
2.11220716970421));
#8772=CARTESIAN_POINT('Ctrl Pts',(-0.195693853754418,6.53393013630089E-5,
2.11241303078758));
#8773=CARTESIAN_POINT('Origin',(0.,0.,0.));
#8774=CARTESIAN_POINT('',(-0.195209426648116,0.000147489598137318,2.19258696921242));
#8775=CARTESIAN_POINT('',(-0.19518796491764,0.000137929913403057,2.18241303078758));
#8776=CARTESIAN_POINT('',(-0.1954,-2.39295984553393E-17,0.));
#8777=CARTESIAN_POINT('Ctrl Pts',(-0.195209426648116,0.000147489598137318,
2.19258696921242));
#8778=CARTESIAN_POINT('Ctrl Pts',(-0.195364342248075,0.0222157994033578,
2.19133146455703));
#8779=CARTESIAN_POINT('Ctrl Pts',(-0.191911630624569,0.0442370720435746,
2.19007595990164));
#8780=CARTESIAN_POINT('Ctrl Pts',(-0.184641287577456,0.0649161428649712,
2.18882045524625));
#8781=CARTESIAN_POINT('Ctrl Pts',(-0.163187026091501,0.125938599413976,
2.18511555095233));
#8782=CARTESIAN_POINT('Ctrl Pts',(-0.108488913443121,0.175273191802267,
2.1814106466584));
#8783=CARTESIAN_POINT('Ctrl Pts',(-0.0455836640180361,0.190338225595007,
2.17770574236448));
#8784=CARTESIAN_POINT('Ctrl Pts',(0.0173215854070469,0.205403259387747,
2.17400083807055));
#8785=CARTESIAN_POINT('Ctrl Pts',(0.0884339716088341,0.186198734584936,
2.17029593377663));
#8786=CARTESIAN_POINT('Ctrl Pts',(0.135203554581594,0.141515049546657,2.1665910294827));
#8787=CARTESIAN_POINT('Ctrl Pts',(0.181973137554356,0.0968313645083757,
2.16288612518878));
#8788=CARTESIAN_POINT('Ctrl Pts',(0.204399917298089,0.026668519234623,2.15918122089485));
#8789=CARTESIAN_POINT('Ctrl Pts',(0.192218587828263,-0.0368581744443589,
2.15547631660092));
#8790=CARTESIAN_POINT('Ctrl Pts',(0.180037258358437,-0.100384868123344,
2.151771412307));
#8791=CARTESIAN_POINT('Ctrl Pts',(0.133247819675049,-0.157275410207558,
2.14806650801307));
#8792=CARTESIAN_POINT('Ctrl Pts',(0.073266983822997,-0.181489557782437,
2.14436160371915));
#8793=CARTESIAN_POINT('Ctrl Pts',(0.0132861479709503,-0.205703705357315,
2.14065669942522));
#8794=CARTESIAN_POINT('Ctrl Pts',(-0.059886085049757,-0.197241458422864,
2.1369517951313));
#8795=CARTESIAN_POINT('Ctrl Pts',(-0.112756930169383,-0.159976201938061,
2.13324689083737));
#8796=CARTESIAN_POINT('Ctrl Pts',(-0.163464408735403,-0.12423576332421,
2.12969358362906));
#8797=CARTESIAN_POINT('Ctrl Pts',(-0.195497891538502,-0.0620012110604251,
2.12614027642074));
#8798=CARTESIAN_POINT('Ctrl Pts',(-0.195705652066383,4.87247307793624E-5,
2.12258696921242));
#8799=CARTESIAN_POINT('Ctrl Pts',(-0.195693853754418,6.53393013630089E-5,
2.11241303078758));
#8800=CARTESIAN_POINT('Ctrl Pts',(-0.195428005564947,-0.0610468420235385,
2.11591207399813));
#8801=CARTESIAN_POINT('Ctrl Pts',(-0.164495934165812,-0.122391080297918,
2.11941111720869));
#8802=CARTESIAN_POINT('Ctrl Pts',(-0.115082411738962,-0.158311560806047,
2.12291016041925));
#8803=CARTESIAN_POINT('Ctrl Pts',(-0.0627617170802516,-0.196345370183675,
2.12661506471318));
#8804=CARTESIAN_POINT('Ctrl Pts',(0.0102790582366786,-0.205875881267149,
2.1303199690071));
#8805=CARTESIAN_POINT('Ctrl Pts',(0.0706073005241847,-0.182540737619698,
2.13402487330103));
#8806=CARTESIAN_POINT('Ctrl Pts',(0.130935542811693,-0.159205593972247,
2.13772977759495));
#8807=CARTESIAN_POINT('Ctrl Pts',(0.178551252069776,-0.103004795593869,
2.14143468188888));
#8808=CARTESIAN_POINT('Ctrl Pts',(0.191659511540249,-0.0396628720499632,
2.1451395861828));
#8809=CARTESIAN_POINT('Ctrl Pts',(0.204767771010722,0.0236790514939429,
2.14884449047673));
#8810=CARTESIAN_POINT('Ctrl Pts',(0.183368580693586,0.0941621002033779,
2.15254939477065));
#8811=CARTESIAN_POINT('Ctrl Pts',(0.137256892346912,0.139524396685099,2.15625429906458));
#8812=CARTESIAN_POINT('Ctrl Pts',(0.091145204000239,0.184886693166819,2.1599592033585));
#8813=CARTESIAN_POINT('Ctrl Pts',(0.02032101762403,0.205128237420826,2.16366410765243));
#8814=CARTESIAN_POINT('Ctrl Pts',(-0.0427976421750205,0.190983961646384,
2.16736901194635));
#8815=CARTESIAN_POINT('Ctrl Pts',(-0.105916301974075,0.176839685871941,
2.17107391624028));
#8816=CARTESIAN_POINT('Ctrl Pts',(-0.161329435195969,0.128309590069043,
2.1747788205342));
#8817=CARTESIAN_POINT('Ctrl Pts',(-0.183673046253887,0.0676071289816255,
2.17848372482813));
#8818=CARTESIAN_POINT('Ctrl Pts',(-0.191572025293587,0.0461474165589195,
2.17979349348128));
#8819=CARTESIAN_POINT('Ctrl Pts',(-0.195338026112343,0.023166420569767,
2.18110326213443));
#8820=CARTESIAN_POINT('Ctrl Pts',(-0.19518796491764,0.000137929913403057,
2.18241303078758));
#8821=CARTESIAN_POINT('Origin',(0.,0.,0.));
#8822=CARTESIAN_POINT('',(-0.195174657492043,-0.000131013293013224,2.26258696921242));
#8823=CARTESIAN_POINT('',(-0.195195111391083,-0.000141315875587933,2.25241303078758));
#8824=CARTESIAN_POINT('',(-0.1954,-2.39295984553393E-17,0.));
#8825=CARTESIAN_POINT('Ctrl Pts',(-0.195174657492043,-0.000131013293013224,
2.26258696921242));
#8826=CARTESIAN_POINT('Ctrl Pts',(-0.194918943248225,0.0413594787080526,
2.26022755698725));
#8827=CARTESIAN_POINT('Ctrl Pts',(-0.181975540580321,0.0829956888567188,
2.25786814476208));
#8828=CARTESIAN_POINT('Ctrl Pts',(-0.157529455112694,0.116150705603978,
2.25550873253691));
#8829=CARTESIAN_POINT('Ctrl Pts',(-0.119142603483941,0.168212894059927,
2.25180382824299));
#8830=CARTESIAN_POINT('Ctrl Pts',(-0.052393188412561,0.199362710149808,
2.24809892394906));
#8831=CARTESIAN_POINT('Ctrl Pts',(0.0121657881897227,0.195342029196137,
2.24439401965513));
#8832=CARTESIAN_POINT('Ctrl Pts',(0.0767247647920027,0.191321348242465,
2.24068911536121));
#8833=CARTESIAN_POINT('Ctrl Pts',(0.139093302925189,0.152130170245245,2.23698421106728));
#8834=CARTESIAN_POINT('Ctrl Pts',(0.170723796521274,0.095707324392732,2.23327930677336));
#8835=CARTESIAN_POINT('Ctrl Pts',(0.202354290117362,0.0392844785402158,
2.22957440247943));
#8836=CARTESIAN_POINT('Ctrl Pts',(0.203246739176347,-0.0343700351675917,
2.22586949818551));
#8837=CARTESIAN_POINT('Ctrl Pts',(0.17299261862985,-0.0915426972318238,
2.22216459389158));
#8838=CARTESIAN_POINT('Ctrl Pts',(0.142738498083355,-0.148715359296053,
2.21845968959766));
#8839=CARTESIAN_POINT('Ctrl Pts',(0.0813378079313799,-0.189406169716704,
2.21475478530373));
#8840=CARTESIAN_POINT('Ctrl Pts',(0.0168952149404143,-0.194989904088049,
2.21104988100981));
#8841=CARTESIAN_POINT('Ctrl Pts',(-0.0475473780505532,-0.200573638459395,
2.20734497671588));
#8842=CARTESIAN_POINT('Ctrl Pts',(-0.115031873880513,-0.171050296781432,
2.20364007242196));
#8843=CARTESIAN_POINT('Ctrl Pts',(-0.154668916633727,-0.119933465587592,
2.19993516812803));
#8844=CARTESIAN_POINT('Ctrl Pts',(-0.180873900754785,-0.0861389224857415,
2.19748576848949));
#8845=CARTESIAN_POINT('Ctrl Pts',(-0.194907197410721,-0.0429062018620786,
2.19503636885096));
#8846=CARTESIAN_POINT('Ctrl Pts',(-0.195209426648116,0.000147489598137318,
2.19258696921242));
#8847=CARTESIAN_POINT('Ctrl Pts',(-0.19518796491764,0.000137929913403057,
2.18241303078758));
#8848=CARTESIAN_POINT('Ctrl Pts',(-0.194913552398402,-0.0419735976389966,
2.18480816642835));
#8849=CARTESIAN_POINT('Ctrl Pts',(-0.181543684570605,-0.0842439491042262,
2.18720330206913));
#8850=CARTESIAN_POINT('Ctrl Pts',(-0.156404834897329,-0.117660695730726,
2.18959843770991));
#8851=CARTESIAN_POINT('Ctrl Pts',(-0.117518923588915,-0.169351232983719,
2.19330334200383));
#8852=CARTESIAN_POINT('Ctrl Pts',(-0.0504730120781484,-0.199857481117771,
2.19700824629776));
#8853=CARTESIAN_POINT('Ctrl Pts',(0.0140442882391665,-0.195215956814723,
2.20071315059168));
#8854=CARTESIAN_POINT('Ctrl Pts',(0.0785615885564833,-0.190574432511675,
2.20441805488561));
#8855=CARTESIAN_POINT('Ctrl Pts',(0.140550277680348,-0.150785135771524,
2.20812295917953));
#8856=CARTESIAN_POINT('Ctrl Pts',(0.171636559439807,-0.0940606369606153,
2.21182786347346));
#8857=CARTESIAN_POINT('Ctrl Pts',(0.202722841199266,-0.0373361381497062,
2.21553276776738));
#8858=CARTESIAN_POINT('Ctrl Pts',(0.202906715594321,0.0363235627319613,
2.21923767206131));
#8859=CARTESIAN_POINT('Ctrl Pts',(0.17210402315838,0.0932025559367594,2.22294257635524));
#8860=CARTESIAN_POINT('Ctrl Pts',(0.14130133072244,0.150081549141557,2.22664748064916));
#8861=CARTESIAN_POINT('Ctrl Pts',(0.0795120714555056,0.190179834669486,
2.23035238494309));
#8862=CARTESIAN_POINT('Ctrl Pts',(0.0150187464949281,0.195143407566839,
2.23405728923701));
#8863=CARTESIAN_POINT('Ctrl Pts',(-0.0494745784656475,0.200106980464191,
2.23776219353094));
#8864=CARTESIAN_POINT('Ctrl Pts',(-0.116671969119866,0.16993584073097,2.24146709782486));
#8865=CARTESIAN_POINT('Ctrl Pts',(-0.155815460686541,0.118440090365932,
2.24517200211879));
#8866=CARTESIAN_POINT('Ctrl Pts',(-0.181316717232319,0.0848915670095187,
2.24758567834172));
#8867=CARTESIAN_POINT('Ctrl Pts',(-0.194911113219737,0.0422922816017406,
2.24999935456465));
#8868=CARTESIAN_POINT('Ctrl Pts',(-0.195195111391083,-0.000141315875587933,
2.25241303078758));
#8869=CARTESIAN_POINT('Origin',(0.,0.,0.));
#8870=CARTESIAN_POINT('',(-0.195681353759257,-7.39606064390219E-5,2.33258696921242));
#8871=CARTESIAN_POINT('',(-0.195697752751996,-5.95341972371984E-5,2.32241303078758));
#8872=CARTESIAN_POINT('',(-0.1954,-2.39295984553393E-17,0.));
#8873=CARTESIAN_POINT('Ctrl Pts',(-0.195681353759257,-7.39606064390219E-5,
2.33258696921242));
#8874=CARTESIAN_POINT('Ctrl Pts',(-0.195380276086469,0.060422861610312,
2.32912364941747));
#8875=CARTESIAN_POINT('Ctrl Pts',(-0.165164977787156,0.12117446104776,2.32566032962252));
#8876=CARTESIAN_POINT('Ctrl Pts',(-0.11660138687175,0.157196309339772,2.32219700982757));
#8877=CARTESIAN_POINT('Ctrl Pts',(-0.0646502338846034,0.195730868177439,
2.31849210553364));
#8878=CARTESIAN_POINT('Ctrl Pts',(0.00829826751356548,0.205965289678994,
2.31478720123972));
#8879=CARTESIAN_POINT('Ctrl Pts',(0.0688488487742365,0.183211962286636,
2.31108229694579));
#8880=CARTESIAN_POINT('Ctrl Pts',(0.129399430034907,0.160458634894278,2.30737739265187));
#8881=CARTESIAN_POINT('Ctrl Pts',(0.177552091158081,0.104717558608008,2.30367248835794));
#8882=CARTESIAN_POINT('Ctrl Pts',(0.191268709972338,0.0415044437598955,
2.29996758406402));
#8883=CARTESIAN_POINT('Ctrl Pts',(0.204985328786596,-0.0217086710882173,
2.29626267977009));
#8884=CARTESIAN_POINT('Ctrl Pts',(0.184265905291938,-0.0923938244981725,
2.29255777547616));
#8885=CARTESIAN_POINT('Ctrl Pts',(0.138592893132747,-0.138197475482013,
2.28885287118224));
#8886=CARTESIAN_POINT('Ctrl Pts',(0.0929198809735568,-0.184001126465853,
2.28514796688831));
#8887=CARTESIAN_POINT('Ctrl Pts',(0.0222932801498333,-0.204923275023578,
2.28144306259439));
#8888=CARTESIAN_POINT('Ctrl Pts',(-0.0409586140019971,-0.19138687945489,
2.27773815830046));
#8889=CARTESIAN_POINT('Ctrl Pts',(-0.104210508153827,-0.177850483886201,
2.27403325400654));
#8890=CARTESIAN_POINT('Ctrl Pts',(-0.160087695633765,-0.1298555441911,2.27032834971261));
#8891=CARTESIAN_POINT('Ctrl Pts',(-0.18301414528067,-0.0693707939325425,
2.26662344541869));
#8892=CARTESIAN_POINT('Ctrl Pts',(-0.191340232466025,-0.0474048414281955,
2.26527795334993));
#8893=CARTESIAN_POINT('Ctrl Pts',(-0.195320482576467,-0.0237916213548985,
2.26393246128118));
#8894=CARTESIAN_POINT('Ctrl Pts',(-0.195174657492043,-0.000131013293013224,
2.26258696921242));
#8895=CARTESIAN_POINT('Ctrl Pts',(-0.195195111391083,-0.000141315875587933,
2.25241303078758));
#8896=CARTESIAN_POINT('Ctrl Pts',(-0.195347039975153,-0.0228417309915556,
2.25370425885857));
#8897=CARTESIAN_POINT('Ctrl Pts',(-0.191689723357918,-0.045494728595087,
2.25499548692957));
#8898=CARTESIAN_POINT('Ctrl Pts',(-0.184008281643019,-0.0666892810800291,
2.25628671500056));
#8899=CARTESIAN_POINT('Ctrl Pts',(-0.16196801855369,-0.127502541164088,
2.25999161929449));
#8900=CARTESIAN_POINT('Ctrl Pts',(-0.106797899895904,-0.17630870033535,
2.26369652358841));
#8901=CARTESIAN_POINT('Ctrl Pts',(-0.0437506280009387,-0.190767918158648,
2.26740142788234));
#8902=CARTESIAN_POINT('Ctrl Pts',(0.0192966438940271,-0.205227135981945,
2.27110633217626));
#8903=CARTESIAN_POINT('Ctrl Pts',(0.0902210690261749,-0.185339412457277,
2.27481123647019));
#8904=CARTESIAN_POINT('Ctrl Pts',(0.136558628570232,-0.140207909463584,
2.27851614076412));
#8905=CARTESIAN_POINT('Ctrl Pts',(0.182896188114289,-0.0950764064698918,
2.28222104505804));
#8906=CARTESIAN_POINT('Ctrl Pts',(0.204646882070257,-0.0247011240071736,
2.28592594935197));
#8907=CARTESIAN_POINT('Ctrl Pts',(0.191855080140027,0.0387054769946518,
2.28963085364589));
#8908=CARTESIAN_POINT('Ctrl Pts',(0.179063278209797,0.102112077996479,2.29333575793982));
#8909=CARTESIAN_POINT('Ctrl Pts',(0.131728980393372,0.15854999753741,2.29704066223374));
#8910=CARTESIAN_POINT('Ctrl Pts',(0.0715178881091697,0.182186000086743,
2.30074556652767));
#8911=CARTESIAN_POINT('Ctrl Pts',(0.0113067958249691,0.205822002636076,
2.30445047082159));
#8912=CARTESIAN_POINT('Ctrl Pts',(-0.0617810909270064,0.196656088193809,
2.30815537511552));
#8913=CARTESIAN_POINT('Ctrl Pts',(-0.114290821684253,0.15888405075463,2.31186027940945));
#8914=CARTESIAN_POINT('Ctrl Pts',(-0.164145652799363,0.123021773034915,
2.31537786320216));
#8915=CARTESIAN_POINT('Ctrl Pts',(-0.195450592530455,0.0613729051733717,
2.31889544699487));
#8916=CARTESIAN_POINT('Ctrl Pts',(-0.195697752751996,-5.95341972371984E-5,
2.32241303078758));
#8917=CARTESIAN_POINT('Origin',(0.,0.,0.));
#8918=CARTESIAN_POINT('',(-0.1954,-2.39295984553393E-17,2.4));
#8919=CARTESIAN_POINT('',(-0.195373070919361,0.000178101583232409,2.39241303078758));
#8920=CARTESIAN_POINT('',(-0.1954,-2.39295984553393E-17,0.));
#8921=CARTESIAN_POINT('',(-0.190155688860645,0.0449663651403318,2.4));
#8922=CARTESIAN_POINT('Origin',(0.,0.,2.4));
#8923=CARTESIAN_POINT('Ctrl Pts',(-0.190155688860645,0.0449663651403318,
2.4));
#8924=CARTESIAN_POINT('Ctrl Pts',(-0.175202059751608,0.108202911730688,
2.39629509570607));
#8925=CARTESIAN_POINT('Ctrl Pts',(-0.126357437987047,0.162847509466655,
2.39259019141215));
#8926=CARTESIAN_POINT('Ctrl Pts',(-0.0654921592886404,0.184422161949795,
2.38888528711823));
#8927=CARTESIAN_POINT('Ctrl Pts',(-0.00462688059022985,0.205996814432936,
2.3851803828243));
#8928=CARTESIAN_POINT('Ctrl Pts',(0.0682590550420274,0.194501521663244,
2.38147547853037));
#8929=CARTESIAN_POINT('Ctrl Pts',(0.119524669012765,0.15503197640457,2.37777057423645));
#8930=CARTESIAN_POINT('Ctrl Pts',(0.1707902829835,0.115562431145897,2.37406566994252));
#8931=CARTESIAN_POINT('Ctrl Pts',(0.200435575292716,0.0481186333982456,
2.3703607656486));
#8932=CARTESIAN_POINT('Ctrl Pts',(0.195018846313631,-0.0163501344389201,
2.36665586135467));
#8933=CARTESIAN_POINT('Ctrl Pts',(0.189602117334546,-0.0808189022760859,
2.36295095706075));
#8934=CARTESIAN_POINT('Ctrl Pts',(0.149123367067157,-0.142312640202767,
2.35924605276682));
#8935=CARTESIAN_POINT('Ctrl Pts',(0.0920460129031269,-0.172724421142238,
2.3555411484729));
#8936=CARTESIAN_POINT('Ctrl Pts',(0.0349686587390981,-0.203136202081708,
2.35183624417897));
#8937=CARTESIAN_POINT('Ctrl Pts',(-0.0387072993215716,-0.202466026033974,
2.34813133988505));
#8938=CARTESIAN_POINT('Ctrl Pts',(-0.0952247602900568,-0.170999569986643,
2.34442643559112));
#8939=CARTESIAN_POINT('Ctrl Pts',(-0.151742221258544,-0.139533113939311,
2.34072153129719));
#8940=CARTESIAN_POINT('Ctrl Pts',(-0.191101185134843,-0.0772703778923819,
2.33701662700327));
#8941=CARTESIAN_POINT('Ctrl Pts',(-0.195303764784931,-0.0127216617820273,
2.33331172270934));
#8942=CARTESIAN_POINT('Ctrl Pts',(-0.195577801040289,-0.00851265447608656,
2.33307013821037));
#8943=CARTESIAN_POINT('Ctrl Pts',(-0.195702355486801,-0.0042939273868865,
2.3328285537114));
#8944=CARTESIAN_POINT('Ctrl Pts',(-0.195681353759257,-7.39606064390219E-5,
2.33258696921242));
#8945=CARTESIAN_POINT('Ctrl Pts',(-0.195697752751996,-5.95341972371984E-5,
2.32241303078758));
#8946=CARTESIAN_POINT('Ctrl Pts',(-0.195710914677712,-0.00333097164176583,
2.32260035128879));
#8947=CARTESIAN_POINT('Ctrl Pts',(-0.195636001710979,-0.00660179532972963,
2.32278767179001));
#8948=CARTESIAN_POINT('Ctrl Pts',(-0.195471124962234,-0.0098680783927403,
2.32297499229122));
#8949=CARTESIAN_POINT('Ctrl Pts',(-0.192210122720448,-0.0744700096648406,
2.32667989658515));
#8950=CARTESIAN_POINT('Ctrl Pts',(-0.153756543474356,-0.137295711772949,
2.33038480087907));
#8951=CARTESIAN_POINT('Ctrl Pts',(-0.0977087684767672,-0.169587100981169,
2.334089705173));
#8952=CARTESIAN_POINT('Ctrl Pts',(-0.0416609934791779,-0.20187849018939,
2.33779460946692));
#8953=CARTESIAN_POINT('Ctrl Pts',(0.0319809772699075,-0.203635566497722,
2.34149951376085));
#8954=CARTESIAN_POINT('Ctrl Pts',(0.0895040276926783,-0.174056293370152,
2.34520441805477));
#8955=CARTESIAN_POINT('Ctrl Pts',(0.147027078115449,-0.144477020242583,
2.3489093223487));
#8956=CARTESIAN_POINT('Ctrl Pts',(0.188431208211903,-0.0835613976791124,
2.35261422664262));
#8957=CARTESIAN_POINT('Ctrl Pts',(0.194774820151305,-0.0191878227159973,
2.35631913093655));
#8958=CARTESIAN_POINT('Ctrl Pts',(0.201118432090707,0.045185752247116,2.36002403523048));
#8959=CARTESIAN_POINT('Ctrl Pts',(0.172401525873055,0.113017279609876,2.3637289395244));
#8960=CARTESIAN_POINT('Ctrl Pts',(0.121749293910871,0.153250507222424,2.36743384381833));
#8961=CARTESIAN_POINT('Ctrl Pts',(0.0710970619486833,0.193483734834974,
2.37113874811225));
#8962=CARTESIAN_POINT('Ctrl Pts',(-0.00149049575803851,0.206118662697314,
2.37484365240618));
#8963=CARTESIAN_POINT('Ctrl Pts',(-0.0627515027614027,0.185387280299844,
2.3785485567001));
#8964=CARTESIAN_POINT('Ctrl Pts',(-0.124012509764765,0.164655897902375,
2.38225346099403));
#8965=CARTESIAN_POINT('Ctrl Pts',(-0.173946966064769,0.1105582052451,2.38595836528795));
#8966=CARTESIAN_POINT('Ctrl Pts',(-0.189769007749096,0.0478268239240077,
2.38966326958188));
#8967=CARTESIAN_POINT('Ctrl Pts',(-0.193683354154737,0.0323071860735817,
2.39057985665045));
#8968=CARTESIAN_POINT('Ctrl Pts',(-0.19550981867675,0.0162591153240736,
2.39149644371901));
#8969=CARTESIAN_POINT('Ctrl Pts',(-0.195373070919361,0.000178101583232409,
2.39241303078758));
#8970=CARTESIAN_POINT('Origin',(0.,0.,-0.129405622560373));
#8971=CARTESIAN_POINT('',(-0.155773974295048,-5.88770334001961E-5,2.35559437743962));
#8972=CARTESIAN_POINT('',(-0.155528562853156,0.000141779433378626,2.36940562256037));
#8973=CARTESIAN_POINT('',(-0.15555,4.36677073508985E-14,-0.129405622560373));
#8974=CARTESIAN_POINT('',(0.103461089470168,0.116496783315852,2.4));
#8975=CARTESIAN_POINT('Ctrl Pts',(-0.155773974295048,-5.88770334001795E-5,
2.35559437743962));
#8976=CARTESIAN_POINT('Ctrl Pts',(-0.15579069291695,-0.00341822111067628,
2.3558359619386));
#8977=CARTESIAN_POINT('Ctrl Pts',(-0.154170948464013,-0.0582798498405871,
2.3597824507315));
#8978=CARTESIAN_POINT('Ctrl Pts',(-0.0894637445537859,-0.160641476281263,
2.36743384381833));
#8979=CARTESIAN_POINT('Ctrl Pts',(0.0864875647042136,-0.162241976039076,
2.3785485567001));
#8980=CARTESIAN_POINT('Ctrl Pts',(0.180902522808575,-0.0188104557555769,
2.38940394209399));
#8981=CARTESIAN_POINT('Ctrl Pts',(0.139126171174338,0.0844901197987813,
2.39655442319396));
#8982=CARTESIAN_POINT('Ctrl Pts',(0.103461767481305,0.116497970106856,2.4));
#8983=CARTESIAN_POINT('',(0.143545299885862,-0.0599211930845659,2.4));
#8984=CARTESIAN_POINT('Origin',(0.,0.,2.4));
#8985=CARTESIAN_POINT('Ctrl Pts',(-0.155528562853156,0.00014177943337863,
2.36940562256037));
#8986=CARTESIAN_POINT('Ctrl Pts',(-0.155197405712005,-0.0388010349799734,
2.37219393978573));
#8987=CARTESIAN_POINT('Ctrl Pts',(-0.120746574532385,-0.130053255016983,
2.37868716130501));
#8988=CARTESIAN_POINT('Ctrl Pts',(0.0327466243405011,-0.180863000230457,
2.38888528711822));
#8989=CARTESIAN_POINT('Ctrl Pts',(0.123618421332056,-0.107657388085867,
2.39629509570608));
#8990=CARTESIAN_POINT('Ctrl Pts',(0.143545299885864,-0.0599211930845618,
2.4));
#8991=CARTESIAN_POINT('Origin',(0.,0.,-0.129405622560373));
#8992=CARTESIAN_POINT('',(-0.155370613986117,-0.00010429435887339,2.28559437743963));
#8993=CARTESIAN_POINT('',(-0.155787028866801,-4.73927552151754E-5,2.29940562256037));
#8994=CARTESIAN_POINT('',(-0.15555,4.36677073508985E-14,-0.129405622560373));
#8995=CARTESIAN_POINT('Ctrl Pts',(-0.155370613986117,-0.000104294358873382,
2.28559437743963));
#8996=CARTESIAN_POINT('Ctrl Pts',(-0.155486699410286,-0.0189395429977021,
2.28693986950838));
#8997=CARTESIAN_POINT('Ctrl Pts',(-0.143593460567012,-0.0894973367036735,
2.29199026587106));
#8998=CARTESIAN_POINT('Ctrl Pts',(-0.0384761925835495,-0.179786364575594,
2.30074556652767));
#8999=CARTESIAN_POINT('Ctrl Pts',(0.130192708513641,-0.129820547664333,
2.31186027940944));
#9000=CARTESIAN_POINT('Ctrl Pts',(0.179674381869752,0.0389881874367674,
2.32297499229122));
#9001=CARTESIAN_POINT('Ctrl Pts',(0.0646772513010348,0.172107804882976,
2.33408970517299));
#9002=CARTESIAN_POINT('Ctrl Pts',(-0.105750122905907,0.14819743592946,2.3449628335558));
#9003=CARTESIAN_POINT('Ctrl Pts',(-0.155534298593903,0.0481001848694375,
2.35213105764467));
#9004=CARTESIAN_POINT('Ctrl Pts',(-0.155773974295048,-5.88770334001795E-5,
2.35559437743962));
#9005=CARTESIAN_POINT('Ctrl Pts',(-0.155787028866801,-4.73927552151962E-5,
2.29940562256037));
#9006=CARTESIAN_POINT('Ctrl Pts',(-0.155797506541035,-0.00265165117128265,
2.29959294306158));
#9007=CARTESIAN_POINT('Ctrl Pts',(-0.154558381720229,-0.0567538846432019,
2.30348516785672));
#9008=CARTESIAN_POINT('Ctrl Pts',(-0.0917880045327959,-0.15930852573796,
2.31108229694579));
#9009=CARTESIAN_POINT('Ctrl Pts',(0.0840821369721223,-0.163504736890904,
2.32219700982757));
#9010=CARTESIAN_POINT('Ctrl Pts',(0.182962573561233,-0.0180273813676558,
2.33331172270934));
#9011=CARTESIAN_POINT('Ctrl Pts',(0.114381487141248,0.143966386512752,2.34442643559112));
#9012=CARTESIAN_POINT('Ctrl Pts',(-0.0589705282315283,0.174140844480832,
2.35554114847289));
#9013=CARTESIAN_POINT('Ctrl Pts',(-0.148306390161892,0.0773566926129291,
2.36386754412931));
#9014=CARTESIAN_POINT('Ctrl Pts',(-0.155637422186119,0.0129432210269571,
2.3684890354918));
#9015=CARTESIAN_POINT('Ctrl Pts',(-0.155528562853156,0.00014177943337863,
2.36940562256037));
#9016=CARTESIAN_POINT('Origin',(0.,0.,-0.129405622560373));
#9017=CARTESIAN_POINT('',(-0.155398292298436,0.000117410475919154,2.21559437743963));
#9018=CARTESIAN_POINT('',(-0.155386896504006,-0.000112495826188885,2.22940562256037));
#9019=CARTESIAN_POINT('',(-0.15555,4.36677073508985E-14,-0.129405622560373));
#9020=CARTESIAN_POINT('Ctrl Pts',(-0.155398292298436,0.000117410475919153,
2.21559437743963));
#9021=CARTESIAN_POINT('Ctrl Pts',(-0.155157699883514,-0.0341558838262174,
2.21804377707816));
#9022=CARTESIAN_POINT('Ctrl Pts',(-0.12708886065999,-0.120628244108591,
2.22419808101062));
#9023=CARTESIAN_POINT('Ctrl Pts',(0.0158711293274525,-0.18317085598959,
2.23405728923701));
#9024=CARTESIAN_POINT('Ctrl Pts',(0.162506912640762,-0.0859939538258468,
2.24517200211879));
#9025=CARTESIAN_POINT('Ctrl Pts',(0.160375585346118,0.0899061424983564,
2.25628671500056));
#9026=CARTESIAN_POINT('Ctrl Pts',(0.011428408683624,0.183501655356106,2.26740142788234));
#9027=CARTESIAN_POINT('Ctrl Pts',(-0.128683759207511,0.11811579007031,2.27717064869536));
#9028=CARTESIAN_POINT('Ctrl Pts',(-0.155167050267454,0.032924600373803,
2.28323496521446));
#9029=CARTESIAN_POINT('Ctrl Pts',(-0.155370613986117,-0.000104294358873382,
2.28559437743963));
#9030=CARTESIAN_POINT('Ctrl Pts',(-0.155386896504006,-0.000112495826188891,
2.22940562256037));
#9031=CARTESIAN_POINT('Ctrl Pts',(-0.155507840676234,-0.0181833738778352,
2.23069685063136));
#9032=CARTESIAN_POINT('Ctrl Pts',(-0.144242638453781,-0.0879587380741699,
2.23569298299629));
#9033=CARTESIAN_POINT('Ctrl Pts',(-0.0410987787696598,-0.179204792201909,
2.24439401965513));
#9034=CARTESIAN_POINT('Ctrl Pts',(0.128281379817428,-0.13170936649677,2.25550873253691));
#9035=CARTESIAN_POINT('Ctrl Pts',(0.18022591070051,0.0363593415954858,2.26662344541869));
#9036=CARTESIAN_POINT('Ctrl Pts',(0.0671831774557089,0.171143144838974,
2.27773815830046));
#9037=CARTESIAN_POINT('Ctrl Pts',(-0.104422007378309,0.149622226504381,
2.28866555068102));
#9038=CARTESIAN_POINT('Ctrl Pts',(-0.155590274657669,0.0488564759453739,
2.29588803876766));
#9039=CARTESIAN_POINT('Ctrl Pts',(-0.155787028866801,-4.73927552151962E-5,
2.29940562256037));
#9040=CARTESIAN_POINT('Origin',(0.,0.,-0.129405622560373));
#9041=CARTESIAN_POINT('',(-0.155793317189999,3.87877782857977E-5,2.14559437743963));
#9042=CARTESIAN_POINT('',(-0.155381207486893,0.000109800399387149,2.15940562256037));
#9043=CARTESIAN_POINT('',(-0.15555,4.36677073508985E-14,-0.129405622560373));
#9044=CARTESIAN_POINT('Ctrl Pts',(-0.155793317189999,3.87877782858049E-5,
2.14559437743963));
#9045=CARTESIAN_POINT('Ctrl Pts',(-0.155627927476026,-0.0493566447310424,
2.14914768464794));
#9046=CARTESIAN_POINT('Ctrl Pts',(-0.103538872562762,-0.150555101055555,
2.15640589615019));
#9047=CARTESIAN_POINT('Ctrl Pts',(0.0688260039060977,-0.170488812072594,
2.16736901194635));
#9048=CARTESIAN_POINT('Ctrl Pts',(0.180567516503863,-0.0346240655854127,
2.17848372482813));
#9049=CARTESIAN_POINT('Ctrl Pts',(0.127008372351303,0.132937304665343,2.18959843770991));
#9050=CARTESIAN_POINT('Ctrl Pts',(-0.0428206707452402,0.178801130147604,
2.20071315059168));
#9051=CARTESIAN_POINT('Ctrl Pts',(-0.144662237131258,0.0869458188293342,
2.20937846383492));
#9052=CARTESIAN_POINT('Ctrl Pts',(-0.155521614312629,0.017685095175004,
2.21433887278424));
#9053=CARTESIAN_POINT('Ctrl Pts',(-0.155398292298436,0.000117410475919153,
2.21559437743963));
#9054=CARTESIAN_POINT('Ctrl Pts',(-0.155381207486893,0.000109800399387143,
2.15940562256037));
#9055=CARTESIAN_POINT('Ctrl Pts',(-0.15516275883098,-0.0334134755001949,
2.16180075820114));
#9056=CARTESIAN_POINT('Ctrl Pts',(-0.128056153355666,-0.119114078918986,
2.16790079813585));
#9057=CARTESIAN_POINT('Ctrl Pts',(0.013193011805229,-0.183383204120377,
2.17770574236448));
#9058=CARTESIAN_POINT('Ctrl Pts',(0.161233041383799,-0.0883592771818423,
2.18882045524625));
#9059=CARTESIAN_POINT('Ctrl Pts',(0.161672166186531,0.08755320703735,2.19993516812803));
#9060=CARTESIAN_POINT('Ctrl Pts',(0.0141084106240242,0.183315054230848,
2.2110498810098));
#9061=CARTESIAN_POINT('Ctrl Pts',(-0.127727581106385,0.119631725398659,
2.22087336582059));
#9062=CARTESIAN_POINT('Ctrl Pts',(-0.155160817099938,0.0336671668534186,
2.22699194633744));
#9063=CARTESIAN_POINT('Ctrl Pts',(-0.155386896504006,-0.000112495826188891,
2.22940562256037));
#9064=CARTESIAN_POINT('Origin',(0.,0.,-0.129405622560373));
#9065=CARTESIAN_POINT('',(-0.155512395363828,-0.000141626737826867,2.07559437743963));
#9066=CARTESIAN_POINT('',(-0.155783925033264,5.20139628275244E-5,2.08940562256037));
#9067=CARTESIAN_POINT('',(-0.15555,4.36677073508985E-14,-0.129405622560373));
#9068=CARTESIAN_POINT('Ctrl Pts',(-0.155512395363828,-0.000141626737826864,
2.07559437743963));
#9069=CARTESIAN_POINT('Ctrl Pts',(-0.155631529586225,-0.0134421217799902,
2.0765466879238));
#9070=CARTESIAN_POINT('Ctrl Pts',(-0.147981681918013,-0.0783523864199532,
2.0812039027019));
#9071=CARTESIAN_POINT('Ctrl Pts',(-0.0572598509893232,-0.174713374727145,
2.08956602177392));
#9072=CARTESIAN_POINT('Ctrl Pts',(0.115743835073967,-0.142852436054201,
2.10068073465569));
#9073=CARTESIAN_POINT('Ctrl Pts',(0.182789748630034,0.0197828623436046,
2.11179544753748));
#9074=CARTESIAN_POINT('Ctrl Pts',(0.0825006624943804,0.164307925944582,
2.12291016041925));
#9075=CARTESIAN_POINT('Ctrl Pts',(-0.0933137111781269,0.15841718704366,
2.13402487330103));
#9076=CARTESIAN_POINT('Ctrl Pts',(-0.154806754983662,0.0557495847898722,
2.14158627897448));
#9077=CARTESIAN_POINT('Ctrl Pts',(-0.155800373320291,0.00214617764686899,
2.14544278035402));
#9078=CARTESIAN_POINT('Ctrl Pts',(-0.155793317189999,3.87877782858049E-5,
2.14559437743963));
#9079=CARTESIAN_POINT('Ctrl Pts',(-0.155783925033264,5.201396282752E-5,
2.08940562256037));
#9080=CARTESIAN_POINT('Ctrl Pts',(-0.155572294092276,-0.0485969103211591,
2.09290466577093));
#9081=CARTESIAN_POINT('Ctrl Pts',(-0.104876060672191,-0.149137277709018,
2.10010861327541));
#9082=CARTESIAN_POINT('Ctrl Pts',(0.0663275338242693,-0.17147627599867,
2.11101746507382));
#9083=CARTESIAN_POINT('Ctrl Pts',(0.180042327710072,-0.0372587603217594,
2.1221321779556));
#9084=CARTESIAN_POINT('Ctrl Pts',(0.128937250118005,0.131067312760423,2.13324689083737));
#9085=CARTESIAN_POINT('Ctrl Pts',(-0.0402035204677608,0.179407725381376,
2.14436160371915));
#9086=CARTESIAN_POINT('Ctrl Pts',(-0.144022462459615,0.0884844566890199,
2.15308118096014));
#9087=CARTESIAN_POINT('Ctrl Pts',(-0.155500665106314,0.0184418460574962,
2.15809585390722));
#9088=CARTESIAN_POINT('Ctrl Pts',(-0.155381207486893,0.000109800399387143,
2.15940562256037));
#9089=CARTESIAN_POINT('Origin',(0.,0.,-0.129405622560373));
#9090=CARTESIAN_POINT('',(-0.155307392249976,4.6077661301668E-5,2.00559437743963));
#9091=CARTESIAN_POINT('',(-0.155535029491756,-0.000142310086639022,2.01940562256037));
#9092=CARTESIAN_POINT('',(-0.15555,4.36677073508985E-14,-0.129405622560373));
#9093=CARTESIAN_POINT('Ctrl Pts',(-0.155307392249976,4.60776613016665E-5,
2.00559437743963));
#9094=CARTESIAN_POINT('Ctrl Pts',(-0.155230909498638,-0.0287678470951232,
2.00765059549358));
#9095=CARTESIAN_POINT('Ctrl Pts',(-0.133719279780215,-0.109604980011744,
2.01341171784146));
#9096=CARTESIAN_POINT('Ctrl Pts',(-0.00357486400063734,-0.183822398504055,
2.02287774448326));
#9097=CARTESIAN_POINT('Ctrl Pts',(0.152509256593582,-0.102685833967865,
2.03399245736504));
#9098=CARTESIAN_POINT('Ctrl Pts',(0.168978674541131,0.072454547095341,2.04510717024682));
#9099=CARTESIAN_POINT('Ctrl Pts',(0.0307564499829109,0.181266363754544,
2.05622188312859));
#9100=CARTESIAN_POINT('Ctrl Pts',(-0.121366472017063,0.129032552536754,
2.0663842855262));
#9101=CARTESIAN_POINT('Ctrl Pts',(-0.155168045355556,0.0383026211499949,
2.07284178362987));
#9102=CARTESIAN_POINT('Ctrl Pts',(-0.155512395363828,-0.000141626737826864,
2.07559437743963));
#9103=CARTESIAN_POINT('Ctrl Pts',(-0.155535029491756,-0.000142310086639015,
2.01940562256037));
#9104=CARTESIAN_POINT('Ctrl Pts',(-0.155649341554365,-0.0126802716132022,
2.02030366904678));
#9105=CARTESIAN_POINT('Ctrl Pts',(-0.148531226312109,-0.0768156130876391,
2.02490661982712));
#9106=CARTESIAN_POINT('Ctrl Pts',(-0.0598065907447483,-0.173858064744653,
2.03321447490139));
#9107=CARTESIAN_POINT('Ctrl Pts',(0.113644170098336,-0.144528397126456,
2.04432918778316));
#9108=CARTESIAN_POINT('Ctrl Pts',(0.183059298154547,0.0171098899136208,
2.05544390066494));
#9109=CARTESIAN_POINT('Ctrl Pts',(0.0848926672411447,0.163084916597067,
2.06655861354672));
#9110=CARTESIAN_POINT('Ctrl Pts',(-0.0909890136144577,0.159763745495145,
2.07767332642849));
#9111=CARTESIAN_POINT('Ctrl Pts',(-0.154427657211485,0.0572753556709789,
2.08528899609971));
#9112=CARTESIAN_POINT('Ctrl Pts',(-0.155796376029769,0.00291420218260239,
2.089199761477));
#9113=CARTESIAN_POINT('Ctrl Pts',(-0.155783925033264,5.201396282752E-5,
2.08940562256037));
#9114=CARTESIAN_POINT('Origin',(0.,0.,-0.129405622560373));
#9115=CARTESIAN_POINT('',(-0.155681301642334,0.000117756784957254,1.93559437743963));
#9116=CARTESIAN_POINT('',(-0.155301544039396,3.40835545433876E-5,1.94940562256037));
#9117=CARTESIAN_POINT('',(-0.15555,4.36677073508985E-14,-0.129405622560373));
#9118=CARTESIAN_POINT('Ctrl Pts',(-0.155681301642334,0.000117756784957245,
1.93559437743963));
#9119=CARTESIAN_POINT('Ctrl Pts',(-0.15531096153354,-0.0438952136125864,
1.93875450306336));
#9120=CARTESIAN_POINT('Ctrl Pts',(-0.112797922286424,-0.14013444255714,
1.94561953298102));
#9121=CARTESIAN_POINT('Ctrl Pts',(0.050423690301781,-0.176807537454614,
1.95618946719261));
#9122=CARTESIAN_POINT('Ctrl Pts',(0.175897409028035,-0.0535121980639788,
1.96730418007439));
#9123=CARTESIAN_POINT('Ctrl Pts',(0.140345725058553,0.118770919429821,1.97841889295616));
#9124=CARTESIAN_POINT('Ctrl Pts',(-0.0236855483435345,0.18232511797358,
1.98953360583794));
#9125=CARTESIAN_POINT('Ctrl Pts',(-0.139699479868363,0.0980903868046811,
1.99859210066576));
#9126=CARTESIAN_POINT('Ctrl Pts',(-0.155368716514435,0.0231492311299511,
2.00394569119965));
#9127=CARTESIAN_POINT('Ctrl Pts',(-0.155307392249976,4.60776613016665E-5,
2.00559437743963));
#9128=CARTESIAN_POINT('Ctrl Pts',(-0.155301544039396,3.40835545433651E-5,
1.94940562256037));
#9129=CARTESIAN_POINT('Ctrl Pts',(-0.15524657988075,-0.0280220748157516,
1.95140757661656));
#9130=CARTESIAN_POINT('Ctrl Pts',(-0.134566760203235,-0.108075727829195,
1.95711443496668));
#9131=CARTESIAN_POINT('Ctrl Pts',(-0.0062604319656806,-0.183750542760931,
1.96652619761073));
#9132=CARTESIAN_POINT('Ctrl Pts',(0.150992567850975,-0.10490328606436,1.9776409104925));
#9133=CARTESIAN_POINT('Ctrl Pts',(0.170019318761453,0.0699777551885857,
1.98875562337428));
#9134=CARTESIAN_POINT('Ctrl Pts',(0.0334017687074566,0.180797612872902,
1.99987033625606));
#9135=CARTESIAN_POINT('Ctrl Pts',(-0.120284414958466,0.1305251314669,2.01008700265142));
#9136=CARTESIAN_POINT('Ctrl Pts',(-0.155177745419853,0.0390452773417597,
2.01659876475286));
#9137=CARTESIAN_POINT('Ctrl Pts',(-0.155535029491756,-0.000142310086639015,
2.01940562256037));
#9138=CARTESIAN_POINT('Origin',(0.,0.,-0.129405622560373));
#9139=CARTESIAN_POINT('',(-0.155675768969518,-0.000119712528699469,1.86559437743963));
#9140=CARTESIAN_POINT('',(-0.15566006707393,0.000124743603163675,1.87940562256037));
#9141=CARTESIAN_POINT('',(-0.15555,4.36677073508985E-14,-0.129405622560373));
#9142=CARTESIAN_POINT('Ctrl Pts',(-0.155675768969518,-0.000119712528699489,
1.86559437743963));
#9143=CARTESIAN_POINT('Ctrl Pts',(-0.155742030728685,-0.00790775711175682,
1.86615350633922));
#9144=CARTESIAN_POINT('Ctrl Pts',(-0.151670179225866,-0.0672314883108279,
1.87041753953273));
#9145=CARTESIAN_POINT('Ctrl Pts',(-0.0754025780794165,-0.16768394396421,
1.87838647702017));
#9146=CARTESIAN_POINT('Ctrl Pts',(0.0999993571785868,-0.154284096420481,
1.88950118990195));
#9147=CARTESIAN_POINT('Ctrl Pts',(0.183856812913126,0.000355232096483363,
1.90061590278373));
#9148=CARTESIAN_POINT('Ctrl Pts',(0.0994024242533403,0.154669363149183,
1.9117306156655));
#9149=CARTESIAN_POINT('Ctrl Pts',(-0.0760499812776094,0.167391320539895,
1.92284532854728));
#9150=CARTESIAN_POINT('Ctrl Pts',(-0.151792203072743,0.0668263219655577,
1.93079991580532));
#9151=CARTESIAN_POINT('Ctrl Pts',(-0.155745145114401,0.00770521701255957,
1.93504959876944));
#9152=CARTESIAN_POINT('Ctrl Pts',(-0.155681301642334,0.000117756784957245,
1.93559437743963));
#9153=CARTESIAN_POINT('Ctrl Pts',(-0.15566006707393,0.000124743603163675,
1.87940562256037));
#9154=CARTESIAN_POINT('Ctrl Pts',(-0.155281954023804,-0.0431477977495249,
1.88251148418635));
#9155=CARTESIAN_POINT('Ctrl Pts',(-0.113998370735902,-0.138671816632529,
1.88932225010624));
#9156=CARTESIAN_POINT('Ctrl Pts',(0.0478348573047686,-0.177525438740387,
1.89983792032007));
#9157=CARTESIAN_POINT('Ctrl Pts',(0.175096732074868,-0.0560766385408066,
1.91095263320185));
#9158=CARTESIAN_POINT('Ctrl Pts',(0.142066184410422,0.116707558540133,1.92206734608362));
#9159=CARTESIAN_POINT('Ctrl Pts',(-0.0210189483701118,0.182651741800479,
1.9331820589654));
#9160=CARTESIAN_POINT('Ctrl Pts',(-0.138953574109165,0.099626766247391,
1.94229481779098));
#9161=CARTESIAN_POINT('Ctrl Pts',(-0.15534829897203,0.0238998867774751,
1.94770267232264));
#9162=CARTESIAN_POINT('Ctrl Pts',(-0.155301544039396,3.40835545433651E-5,
1.94940562256037));
#9163=CARTESIAN_POINT('Origin',(0.,0.,-0.129405622560373));
#9164=CARTESIAN_POINT('',(-0.155305673965381,-4.29356672906584E-5,1.79559437743963));
#9165=CARTESIAN_POINT('',(-0.155696332526243,-0.000111918222169591,1.80940562256037));
#9166=CARTESIAN_POINT('',(-0.15555,4.36677073508985E-14,-0.129405622560373));
#9167=CARTESIAN_POINT('Ctrl Pts',(-0.155305673965381,-4.29356672906715E-5,
1.79559437743963));
#9168=CARTESIAN_POINT('Ctrl Pts',(-0.15536327786609,-0.0233478236154843,
1.797257413909));
#9169=CARTESIAN_POINT('Ctrl Pts',(-0.139503695394343,-0.0984967514743806,
1.80262535467229));
#9170=CARTESIAN_POINT('Ctrl Pts',(-0.0229808287568944,-0.182415282676811,
1.81169819972952));
#9171=CARTESIAN_POINT('Ctrl Pts',(0.140803633131985,-0.118227707163963,
1.82281291261129));
#9172=CARTESIAN_POINT('Ctrl Pts',(0.175689313331093,0.0541915032607811,
1.83392762549307));
#9173=CARTESIAN_POINT('Ctrl Pts',(0.0497400921817236,0.177001065178062,
1.84504233837485));
#9174=CARTESIAN_POINT('Ctrl Pts',(-0.113117186070765,0.139748166323907,
1.85559792235703));
#9175=CARTESIAN_POINT('Ctrl Pts',(-0.155302966541089,0.0436974449055495,
1.86244860204529));
#9176=CARTESIAN_POINT('Ctrl Pts',(-0.155675768969518,-0.000119712528699489,
1.86559437743963));
#9177=CARTESIAN_POINT('Ctrl Pts',(-0.155696332526243,-0.000111918222169581,
1.80940562256037));
#9178=CARTESIAN_POINT('Ctrl Pts',(-0.155753426825624,-0.00714170684078856,
1.8099104874622));
#9179=CARTESIAN_POINT('Ctrl Pts',(-0.15212706396067,-0.0656996999979794,
1.81412025665796));
#9180=CARTESIAN_POINT('Ctrl Pts',(-0.0778446696726029,-0.16656428902048,
1.82203493014764));
#9181=CARTESIAN_POINT('Ctrl Pts',(0.0977343372718058,-0.155728784402163,
1.83314964302942));
#9182=CARTESIAN_POINT('Ctrl Pts',(0.183842378706508,-0.00233125821546848,
1.84426435591119));
#9183=CARTESIAN_POINT('Ctrl Pts',(0.101651789551148,0.15320041988971,1.85537906879297));
#9184=CARTESIAN_POINT('Ctrl Pts',(-0.0735959994667044,0.168484669438591,
1.86649378167474));
#9185=CARTESIAN_POINT('Ctrl Pts',(-0.151326219056215,0.0683587206479964,
1.87450263293055));
#9186=CARTESIAN_POINT('Ctrl Pts',(-0.155732995580608,0.00847092953884112,
1.87880657989242));
#9187=CARTESIAN_POINT('Ctrl Pts',(-0.15566006707393,0.000124743603163675,
1.87940562256037));
#9188=CARTESIAN_POINT('Origin',(0.,0.,-0.129405622560373));
#9189=CARTESIAN_POINT('',(-0.155518343429684,0.000141921497343934,1.72559437743963));
#9190=CARTESIAN_POINT('',(-0.155312812859558,-5.46847567449715E-5,1.73940562256037));
#9191=CARTESIAN_POINT('',(-0.15555,4.36677073508985E-14,-0.129405622560373));
#9192=CARTESIAN_POINT('Ctrl Pts',(-0.155518343429684,0.00014192149734394,
1.72559437743963));
#9193=CARTESIAN_POINT('Ctrl Pts',(-0.155170356887597,-0.0384989847489488,
1.72836132147878));
#9194=CARTESIAN_POINT('Ctrl Pts',(-0.121082051571819,-0.12942764660935,
1.73483316981186));
#9195=CARTESIAN_POINT('Ctrl Pts',(0.0314566718510104,-0.181146160987399,
1.74500992243886));
#9196=CARTESIAN_POINT('Ctrl Pts',(0.169257392597246,-0.071801036869925,
1.75612463532064));
#9197=CARTESIAN_POINT('Ctrl Pts',(0.15211131820417,0.103274395271066,1.76723934820241));
#9198=CARTESIAN_POINT('Ctrl Pts',(-0.00428516586664415,0.18380721203998,
1.77835406108419));
#9199=CARTESIAN_POINT('Ctrl Pts',(-0.133944959179947,0.109200715226807,
1.78780573749659));
#9200=CARTESIAN_POINT('Ctrl Pts',(-0.155234948185403,0.0285706887075647,
1.79355250961507));
#9201=CARTESIAN_POINT('Ctrl Pts',(-0.155305673965381,-4.29356672906715E-5,
1.79559437743963));
#9202=CARTESIAN_POINT('Ctrl Pts',(-0.155312812859558,-5.46847567449889E-5,
1.73940562256037));
#9203=CARTESIAN_POINT('Ctrl Pts',(-0.155383971417563,-0.0225965602306028,
1.74101439503198));
#9204=CARTESIAN_POINT('Ctrl Pts',(-0.140238499174836,-0.0969598979476685,
1.74632807179752));
#9205=CARTESIAN_POINT('Ctrl Pts',(-0.025643765052489,-0.182060023858252,
1.75534665285698));
#9206=CARTESIAN_POINT('Ctrl Pts',(0.139061101343075,-0.120272461796479,
1.76646136573876));
#9207=CARTESIAN_POINT('Ctrl Pts',(0.176462387959855,0.0516186071958565,
1.77757607862053));
#9208=CARTESIAN_POINT('Ctrl Pts',(0.0523210615336027,0.176255387132795,
1.78869079150231));
#9209=CARTESIAN_POINT('Ctrl Pts',(-0.111903083287874,0.141206823406311,
1.79930063948226));
#9210=CARTESIAN_POINT('Ctrl Pts',(-0.155334445600806,0.0444457454539616,
1.80620558316828));
#9211=CARTESIAN_POINT('Ctrl Pts',(-0.155696332526243,-0.000111918222169581,
1.80940562256037));
#9212=CARTESIAN_POINT('Origin',(0.,0.,-0.129405622560373));
#9213=CARTESIAN_POINT('',(-0.155791073984785,-4.23332785624109E-5,1.65559437743963));
#9214=CARTESIAN_POINT('',(-0.15549602743488,0.000140380679560979,1.66940562256037));
#9215=CARTESIAN_POINT('',(-0.15555,4.36677073508985E-14,-0.129405622560373));
#9216=CARTESIAN_POINT('Ctrl Pts',(-0.155791073984785,-4.23332785623931E-5,
1.65559437743963));
#9217=CARTESIAN_POINT('Ctrl Pts',(-0.155799432443742,-0.00234929814144918,
1.65576032475464));
#9218=CARTESIAN_POINT('Ctrl Pts',(-0.154707626121287,-0.056152981769663,
1.65963117636357));
#9219=CARTESIAN_POINT('Ctrl Pts',(-0.0927008570553628,-0.158776588153342,
1.66720693226643));
#9220=CARTESIAN_POINT('Ctrl Pts',(0.0831349670626055,-0.163987899236237,
1.6783216451482));
#9221=CARTESIAN_POINT('Ctrl Pts',(0.182864829055688,-0.0190763764601355,
1.68943635802998));
#9222=CARTESIAN_POINT('Ctrl Pts',(0.115190958951233,0.143298628117334,1.70055107091176));
#9223=CARTESIAN_POINT('Ctrl Pts',(-0.0579345528489473,0.174490806149227,
1.71166578379353));
#9224=CARTESIAN_POINT('Ctrl Pts',(-0.148128299703662,0.0779459344043742,
1.72001355263616));
#9225=CARTESIAN_POINT('Ctrl Pts',(-0.15563630661978,0.0132407170474581,
1.72465641718486));
#9226=CARTESIAN_POINT('Ctrl Pts',(-0.155518343429684,0.00014192149734394,
1.72559437743963));
#9227=CARTESIAN_POINT('Ctrl Pts',(-0.15549602743488,0.000140380679560978,
1.66940562256037));
#9228=CARTESIAN_POINT('Ctrl Pts',(-0.155162551505327,-0.0377565590374548,
1.67211830260176));
#9229=CARTESIAN_POINT('Ctrl Pts',(-0.122151036079771,-0.127932248494189,
1.67853588693708));
#9230=CARTESIAN_POINT('Ctrl Pts',(0.0288064689070301,-0.181586459634089,
1.68865837556633));
#9231=CARTESIAN_POINT('Ctrl Pts',(0.168190194183902,-0.0742665035780993,
1.6997730884481));
#9232=CARTESIAN_POINT('Ctrl Pts',(0.153604091834597,0.101040773675795,1.71088780132988));
#9233=CARTESIAN_POINT('Ctrl Pts',(-0.00159898082742857,0.183850205965748,
1.72200251421165));
#9234=CARTESIAN_POINT('Ctrl Pts',(-0.133085641205322,0.110728808415752,
1.73150845462182));
#9235=CARTESIAN_POINT('Ctrl Pts',(-0.155220097624497,0.0293159959014319,
1.73730949073806));
#9236=CARTESIAN_POINT('Ctrl Pts',(-0.155312812859558,-5.46847567449889E-5,
1.73940562256037));
#9237=CARTESIAN_POINT('Origin',(0.,0.,-0.129405622560373));
#9238=CARTESIAN_POINT('',(-0.155393652545721,-0.000115483920557439,1.58559437743963));
#9239=CARTESIAN_POINT('',(-0.155798596181036,-2.87742873198993E-5,1.59940562256037));
#9240=CARTESIAN_POINT('',(-0.15555,4.36677073508985E-14,-0.129405622560373));
#9241=CARTESIAN_POINT('Ctrl Pts',(-0.155393652545721,-0.000115483920557415,
1.58559437743963));
#9242=CARTESIAN_POINT('Ctrl Pts',(-0.15551609710512,-0.0178853001538728,
1.58686423232442));
#9243=CARTESIAN_POINT('Ctrl Pts',(-0.144494420494594,-0.0873527113820494,
1.59183899150313));
#9244=CARTESIAN_POINT('Ctrl Pts',(-0.042129426749787,-0.178965262680077,
1.60051865497577));
#9245=CARTESIAN_POINT('Ctrl Pts',(0.127521122443655,-0.132445525311824,
1.61163336785754));
#9246=CARTESIAN_POINT('Ctrl Pts',(0.180432373388368,0.0353215582591597,
1.62274808073932));
#9247=CARTESIAN_POINT('Ctrl Pts',(0.0681666854301347,0.170753497304986,
1.6338627936211));
#9248=CARTESIAN_POINT('Ctrl Pts',(-0.103894360880775,0.150180844959855,
1.64481155918787));
#9249=CARTESIAN_POINT('Ctrl Pts',(-0.155612823275166,0.0491555064169759,
1.65205542046071));
#9250=CARTESIAN_POINT('Ctrl Pts',(-0.155791073984785,-4.23332785623931E-5,
1.65559437743963));
#9251=CARTESIAN_POINT('Ctrl Pts',(-0.155798596181035,-2.8774287319909E-5,
1.59940562256037));
#9252=CARTESIAN_POINT('Ctrl Pts',(-0.155802548454758,-0.00158117186309398,
1.59951730587762));
#9253=CARTESIAN_POINT('Ctrl Pts',(-0.155078243731589,-0.0546279421812704,
1.60333389348879));
#9254=CARTESIAN_POINT('Ctrl Pts',(-0.0950109510297781,-0.157405127482403,
1.61085538539389));
#9255=CARTESIAN_POINT('Ctrl Pts',(0.08072995862503,-0.165185134784385,1.62197009827567));
#9256=CARTESIAN_POINT('Ctrl Pts',(0.18256657276441,-0.0217462981307606,
1.63308481115744));
#9257=CARTESIAN_POINT('Ctrl Pts',(0.117272493730902,0.141600201933013,1.64419952403922));
#9258=CARTESIAN_POINT('Ctrl Pts',(-0.0553787694277143,0.175318700856487,
1.65531423692099));
#9259=CARTESIAN_POINT('Ctrl Pts',(-0.147568974074888,0.0794830657980112,
1.66371626976138));
#9260=CARTESIAN_POINT('Ctrl Pts',(-0.155618003819817,0.0140020459368744,
1.66841339830784));
#9261=CARTESIAN_POINT('Ctrl Pts',(-0.15549602743488,0.000140380679560978,
1.66940562256037));
#9262=CARTESIAN_POINT('Origin',(0.,0.,-0.129405622560373));
#9263=CARTESIAN_POINT('',(-0.155374827277607,0.000106566912644677,1.51559437743963));
#9264=CARTESIAN_POINT('',(-0.155411636004792,-0.000122429372152177,1.52940562256037));
#9265=CARTESIAN_POINT('',(-0.15555,4.36677073508985E-14,-0.129405622560373));
#9266=CARTESIAN_POINT('Ctrl Pts',(-0.155374827277607,0.000106566912644665,
1.51559437743963));
#9267=CARTESIAN_POINT('Ctrl Pts',(-0.15516525123262,-0.0331209874429721,
1.5179681398942));
#9268=CARTESIAN_POINT('Ctrl Pts',(-0.128432482276088,-0.118516965374693,
1.52404680664269));
#9269=CARTESIAN_POINT('Ctrl Pts',(0.0121373640243727,-0.183456093490935,
1.53383037768511));
#9270=CARTESIAN_POINT('Ctrl Pts',(0.160721829762796,-0.0892857619226799,
1.54494509056689));
#9271=CARTESIAN_POINT('Ctrl Pts',(0.162173387162441,0.0866212811073344,
1.55605980344866));
#9272=CARTESIAN_POINT('Ctrl Pts',(0.0151632070148183,0.183230813449705,
1.56717451633044));
#9273=CARTESIAN_POINT('Ctrl Pts',(-0.127346320131558,0.120228081953846,
1.57701937432743));
#9274=CARTESIAN_POINT('Ctrl Pts',(-0.155158855203452,0.0339595753935086,
1.58315932803049));
#9275=CARTESIAN_POINT('Ctrl Pts',(-0.155393652545721,-0.000115483920557415,
1.58559437743963));
#9276=CARTESIAN_POINT('Ctrl Pts',(-0.155411636004792,-0.000122429372152195,
1.52940562256037));
#9277=CARTESIAN_POINT('Ctrl Pts',(-0.155536856521019,-0.017127942381014,
1.5306212134474));
#9278=CARTESIAN_POINT('Ctrl Pts',(-0.145123830999224,-0.0858141230320717,
1.53554170862835));
#9279=CARTESIAN_POINT('Ctrl Pts',(-0.0447399086353324,-0.178330579398589,
1.54416710810323));
#9280=CARTESIAN_POINT('Ctrl Pts',(0.125572262560343,-0.134294682876169,
1.55528182098501));
#9281=CARTESIAN_POINT('Ctrl Pts',(0.180929220612589,0.0326813723985916,
1.56639653386679));
#9282=CARTESIAN_POINT('Ctrl Pts',(0.0706544006326465,0.16973924308944,1.57751124674856));
#9283=CARTESIAN_POINT('Ctrl Pts',(-0.102543043975465,0.151593392893447,
1.58851427631309));
#9284=CARTESIAN_POINT('Ctrl Pts',(-0.155671438489139,0.0499169801086266,
1.59581240158369));
#9285=CARTESIAN_POINT('Ctrl Pts',(-0.155798596181035,-2.8774287319909E-5,
1.59940562256037));
#9286=CARTESIAN_POINT('Origin',(0.,0.,-0.129405622560373));
#9287=CARTESIAN_POINT('',(-0.155779565525168,5.70752760268494E-5,1.44559437743963));
#9288=CARTESIAN_POINT('',(-0.155359588126868,9.7796359098748E-5,1.45940562256037));
#9289=CARTESIAN_POINT('',(-0.15555,4.36677073508985E-14,-0.129405622560373));
#9290=CARTESIAN_POINT('Ctrl Pts',(-0.155779565525168,5.707527602684E-5,
1.44559437743963));
#9291=CARTESIAN_POINT('Ctrl Pts',(-0.155551472791767,-0.0482982854834191,
1.44907204746398));
#9292=CARTESIAN_POINT('Ctrl Pts',(-0.105397482190625,-0.148576906771086,
1.45625462178225));
#9293=CARTESIAN_POINT('Ctrl Pts',(0.0653395323085358,-0.171855169727642,
1.46714210039446));
#9294=CARTESIAN_POINT('Ctrl Pts',(0.179824906471596,-0.0382943449728064,
1.47825681327623));
#9295=CARTESIAN_POINT('Ctrl Pts',(0.129689447733715,0.130323063925534,1.48937152615801));
#9296=CARTESIAN_POINT('Ctrl Pts',(-0.0391703041140288,0.179636135340385,
1.50048623903978));
#9297=CARTESIAN_POINT('Ctrl Pts',(-0.143766574204452,0.0890904857756365,
1.50922718946699));
#9298=CARTESIAN_POINT('Ctrl Pts',(-0.155492351860353,0.0187396815013074,
1.51426323560027));
#9299=CARTESIAN_POINT('Ctrl Pts',(-0.155374827277607,0.000106566912644665,
1.51559437743963));
#9300=CARTESIAN_POINT('Ctrl Pts',(-0.155359588126868,9.77963590987375E-5,
1.45940562256037));
#9301=CARTESIAN_POINT('Ctrl Pts',(-0.155172803939685,-0.0323781756248701,
1.46172512101718));
#9302=CARTESIAN_POINT('Ctrl Pts',(-0.129376186277849,-0.116999238532853,
1.46774952376792));
#9303=CARTESIAN_POINT('Ctrl Pts',(0.00945547127077659,-0.183613858508507,
1.47747883081258));
#9304=CARTESIAN_POINT('Ctrl Pts',(0.159400061651521,-0.0916246436218211,
1.48859354369435));
#9305=CARTESIAN_POINT('Ctrl Pts',(0.163421757209686,0.0842424135684204,
1.49970825657613));
#9306=CARTESIAN_POINT('Ctrl Pts',(0.0178388940120074,0.182989695977022,
1.51082296945791));
#9307=CARTESIAN_POINT('Ctrl Pts',(-0.126366486331398,0.121740238415378,
1.52072209145265));
#9308=CARTESIAN_POINT('Ctrl Pts',(-0.155155206713338,0.0347018293285349,
1.52691630915347));
#9309=CARTESIAN_POINT('Ctrl Pts',(-0.155411636004792,-0.000122429372152195,
1.52940562256037));
#9310=CARTESIAN_POINT('Origin',(0.,0.,-0.129405622560373));
#9311=CARTESIAN_POINT('',(-0.155544028068607,-0.000142255349246604,1.37559437743963));
#9312=CARTESIAN_POINT('',(-0.155766970030976,6.94820370851796E-5,1.38940562256037));
#9313=CARTESIAN_POINT('',(-0.15555,4.36677073508985E-14,-0.129405622560373));
#9314=CARTESIAN_POINT('Ctrl Pts',(-0.155544028068607,-0.000142255349246624,
1.37559437743963));
#9315=CARTESIAN_POINT('Ctrl Pts',(-0.155656157486624,-0.0123800086342895,
1.37647105073983));
#9316=CARTESIAN_POINT('Ctrl Pts',(-0.14874404615406,-0.0762104595352229,
1.38105262833397));
#9317=CARTESIAN_POINT('Ctrl Pts',(-0.0608062091124237,-0.173510975957692,
1.38933911022202));
#9318=CARTESIAN_POINT('Ctrl Pts',(0.112810477944863,-0.145180060305354,
1.4004538231038));
#9319=CARTESIAN_POINT('Ctrl Pts',(0.183154736262308,0.0160560402683587,
1.41156853598558));
#9320=CARTESIAN_POINT('Ctrl Pts',(0.0858298667327937,0.162593627861136,
1.42268324886735));
#9321=CARTESIAN_POINT('Ctrl Pts',(-0.0900680126570708,0.160284768273284,
1.43379796174913));
#9322=CARTESIAN_POINT('Ctrl Pts',(-0.154275150059787,0.0578765860113586,
1.44143500460655));
#9323=CARTESIAN_POINT('Ctrl Pts',(-0.155794469321476,0.00321666057460228,
1.44536714317005));
#9324=CARTESIAN_POINT('Ctrl Pts',(-0.155779565525168,5.707527602684E-5,
1.44559437743963));
#9325=CARTESIAN_POINT('Ctrl Pts',(-0.155766970030976,6.94820370851787E-5,
1.38940562256037));
#9326=CARTESIAN_POINT('Ctrl Pts',(-0.155501349034121,-0.047541582630428,
1.39282902858696));
#9327=CARTESIAN_POINT('Ctrl Pts',(-0.106708006897432,-0.147149458313824,
1.39995733890748));
#9328=CARTESIAN_POINT('Ctrl Pts',(0.062821469496632,-0.172791544768887,
1.41079055352192));
#9329=CARTESIAN_POINT('Ctrl Pts',(0.179246168325776,-0.0409177970309031,
1.4219052664037));
#9330=CARTESIAN_POINT('Ctrl Pts',(0.131579840483081,0.12841417582098,1.43301997928547));
#9331=CARTESIAN_POINT('Ctrl Pts',(-0.0365413417972516,0.180189304102632,
1.44413469216725));
#9332=CARTESIAN_POINT('Ctrl Pts',(-0.143106948997553,0.090629082605181,
1.45292990659221));
#9333=CARTESIAN_POINT('Ctrl Pts',(-0.155471151858434,0.0194952661097169,
1.45802021672326));
#9334=CARTESIAN_POINT('Ctrl Pts',(-0.155359588126868,9.77963590987375E-5,
1.45940562256037));
#9335=CARTESIAN_POINT('Origin',(0.,0.,-0.129405622560373));
#9336=CARTESIAN_POINT('',(-0.155299722974107,2.92844383266709E-5,1.30559437743963));
#9337=CARTESIAN_POINT('',(-0.155567011638057,-0.00014128583726751,1.31940562256037));
#9338=CARTESIAN_POINT('',(-0.15555,4.36677073508985E-14,-0.129405622560373));
#9339=CARTESIAN_POINT('Ctrl Pts',(-0.155299722974107,2.92844383266832E-5,
1.30559437743963));
#9340=CARTESIAN_POINT('Ctrl Pts',(-0.155253032879804,-0.0277281524137369,
1.30757495830962));
#9341=CARTESIAN_POINT('Ctrl Pts',(-0.1348961631779,-0.107472984602923,1.31326044347353));
#9342=CARTESIAN_POINT('Ctrl Pts',(-0.00731787249863105,-0.183711465582603,
1.32265083293137));
#9343=CARTESIAN_POINT('Ctrl Pts',(0.150386311950183,-0.10577055839144,1.33376554581314));
#9344=CARTESIAN_POINT('Ctrl Pts',(0.170419244869387,0.0689980783976093,
1.34488025869492));
#9345=CARTESIAN_POINT('Ctrl Pts',(0.0344417641967487,0.180602377402486,
1.35599497157669));
#9346=CARTESIAN_POINT('Ctrl Pts',(-0.119853316330062,0.131111926080083,
1.36623301115827));
#9347=CARTESIAN_POINT('Ctrl Pts',(-0.155182287959412,0.0393378943554936,
1.37276614644591));
#9348=CARTESIAN_POINT('Ctrl Pts',(-0.155544028068607,-0.000142255349246624,
1.37559437743963));
#9349=CARTESIAN_POINT('Ctrl Pts',(-0.155567011638057,-0.000141285837267533,
1.31940562256037));
#9350=CARTESIAN_POINT('Ctrl Pts',(-0.155672941482856,-0.011617212227624,
1.32022803186282));
#9351=CARTESIAN_POINT('Ctrl Pts',(-0.149275241288209,-0.074674446500909,
1.32475534545919));
#9352=CARTESIAN_POINT('Ctrl Pts',(-0.0633350012944175,-0.172603976154579,
1.33298756334949));
#9353=CARTESIAN_POINT('Ctrl Pts',(0.110677115627384,-0.146812911726923,
1.34410227623126));
#9354=CARTESIAN_POINT('Ctrl Pts',(0.183369791793454,0.0133781325662369,
1.35521698911304));
#9355=CARTESIAN_POINT('Ctrl Pts',(0.0881964673803512,0.161322156305205,
1.36633170199482));
#9356=CARTESIAN_POINT('Ctrl Pts',(-0.087716373065073,0.161583702363956,
1.37744641487659));
#9357=CARTESIAN_POINT('Ctrl Pts',(-0.153879808881157,0.0594037195771841,
1.38513772173178));
#9358=CARTESIAN_POINT('Ctrl Pts',(-0.155788811393,0.0039844229192785,1.38912412429304));
#9359=CARTESIAN_POINT('Ctrl Pts',(-0.155766970030976,6.94820370851787E-5,
1.38940562256037));
#9360=CARTESIAN_POINT('Origin',(0.,0.,-0.129405622560373));
#9361=CARTESIAN_POINT('',(-0.155651485174645,0.000127186369725584,1.23559437743963));
#9362=CARTESIAN_POINT('',(-0.155296357294745,1.69605947035745E-5,1.24940562256037));
#9363=CARTESIAN_POINT('',(-0.15555,4.36677073508985E-14,-0.129405622560373));
#9364=CARTESIAN_POINT('Ctrl Pts',(-0.155651485174645,0.00012718636972558,
1.23559437743963));
#9365=CARTESIAN_POINT('Ctrl Pts',(-0.155271426560331,-0.0428537130042785,
1.2386788658794));
#9366=CARTESIAN_POINT('Ctrl Pts',(-0.114466114921002,-0.13809428189611,
1.24546825861309));
#9367=CARTESIAN_POINT('Ctrl Pts',(0.0468123474454561,-0.177797800804905,
1.25596255564071));
#9368=CARTESIAN_POINT('Ctrl Pts',(0.174771089844121,-0.0570834476806803,
1.26707726852248));
#9369=CARTESIAN_POINT('Ctrl Pts',(0.142735519209796,0.115887986436578,1.27819198140426));
#9370=CARTESIAN_POINT('Ctrl Pts',(-0.0199673795378149,0.182769684572709,
1.28930669428604));
#9371=CARTESIAN_POINT('Ctrl Pts',(-0.138655607475008,0.100231705012538,
1.29844082629783));
#9372=CARTESIAN_POINT('Ctrl Pts',(-0.155340372070791,0.0241953254608532,
1.30387005401569));
#9373=CARTESIAN_POINT('Ctrl Pts',(-0.155299722974107,2.92844383266832E-5,
1.30559437743963));
#9374=CARTESIAN_POINT('Ctrl Pts',(-0.155296357294745,1.6960594703571E-5,
1.24940562256037));
#9375=CARTESIAN_POINT('Ctrl Pts',(-0.155270088652903,-0.0269814387089377,
1.2513319394326));
#9376=CARTESIAN_POINT('Ctrl Pts',(-0.135721405315835,-0.105941739255518,
1.25696316059875));
#9377=CARTESIAN_POINT('Ctrl Pts',(-0.0100014200241654,-0.183584930129994,
1.26629928605883));
#9378=CARTESIAN_POINT('Ctrl Pts',(0.148824776878697,-0.107956661491269,
1.2774139989406));
#9379=CARTESIAN_POINT('Ctrl Pts',(0.171409230594902,0.0665006063145147,
1.28852871182238));
#9380=CARTESIAN_POINT('Ctrl Pts',(0.0370769876137034,0.180079848852746,
1.29964342470416));
#9381=CARTESIAN_POINT('Ctrl Pts',(-0.118746306416021,0.132598853125113,
1.30993572828349));
#9382=CARTESIAN_POINT('Ctrl Pts',(-0.155195733922481,0.040081143851182,
1.31652312756889));
#9383=CARTESIAN_POINT('Ctrl Pts',(-0.155567011638057,-0.000141285837267533,
1.31940562256037));
#9384=CARTESIAN_POINT('Origin',(0.,0.,-0.129405622560373));
#9385=CARTESIAN_POINT('',(-0.155704137558009,-0.000108555906714621,1.16559437743963));
#9386=CARTESIAN_POINT('',(-0.155629273963861,0.000132584196566119,1.17940562256037));
#9387=CARTESIAN_POINT('',(-0.15555,4.36677073508985E-14,-0.129405622560373));
#9388=CARTESIAN_POINT('Ctrl Pts',(-0.155704137558009,-0.000108555906714635,
1.16559437743963));
#9389=CARTESIAN_POINT('Ctrl Pts',(-0.155757622145014,-0.00683986061081713,
1.16607786915525));
#9390=CARTESIAN_POINT('Ctrl Pts',(-0.152303640106945,-0.0650965997331611,
1.1702662651648));
#9391=CARTESIAN_POINT('Ctrl Pts',(-0.0788020109327346,-0.166113506125697,
1.17815956546827));
#9392=CARTESIAN_POINT('Ctrl Pts',(0.0968364469996555,-0.156288695614551,
1.18927427835005));
#9393=CARTESIAN_POINT('Ctrl Pts',(0.183825913682498,-0.00338929243493567,
1.20038899123183));
#9394=CARTESIAN_POINT('Ctrl Pts',(0.102531822692703,0.152612840808782,1.2115037041136));
#9395=CARTESIAN_POINT('Ctrl Pts',(-0.0726250950973966,0.168905445165361,
1.22261841699538));
#9396=CARTESIAN_POINT('Ctrl Pts',(-0.151139256233472,0.0689625117337061,
1.23064864143739));
#9397=CARTESIAN_POINT('Ctrl Pts',(-0.155727930392202,0.00877239024010237,
1.23497396158547));
#9398=CARTESIAN_POINT('Ctrl Pts',(-0.155651485174645,0.00012718636972558,
1.23559437743963));
#9399=CARTESIAN_POINT('Ctrl Pts',(-0.155629273963861,0.000132584196566117,
1.17940562256037));
#9400=CARTESIAN_POINT('Ctrl Pts',(-0.155246937989768,-0.0421077654193814,
1.18243584700238));
#9401=CARTESIAN_POINT('Ctrl Pts',(-0.115640831727419,-0.136624465004964,
1.18917097573831));
#9402=CARTESIAN_POINT('Ctrl Pts',(0.0442094305335735,-0.178462828693349,
1.19961100876817));
#9403=CARTESIAN_POINT('Ctrl Pts',(0.173918351244622,-0.0596310495772682,
1.21072572164995));
#9404=CARTESIAN_POINT('Ctrl Pts',(0.144413599053411,0.113790014420313,1.22184043453173));
#9405=CARTESIAN_POINT('Ctrl Pts',(-0.0172946805849302,0.183041932345569,
1.2329551474135));
#9406=CARTESIAN_POINT('Ctrl Pts',(-0.137888448107413,0.101767008220966,
1.24214354342305));
#9407=CARTESIAN_POINT('Ctrl Pts',(-0.155320611391586,0.0249448497181091,
1.24762703513867));
#9408=CARTESIAN_POINT('Ctrl Pts',(-0.155296357294745,1.6960594703571E-5,
1.24940562256037));
#9409=CARTESIAN_POINT('Origin',(0.,0.,-0.129405622560373));
#9410=CARTESIAN_POINT('',(-0.155316093427556,-5.92046854689235E-5,1.09559437743963));
#9411=CARTESIAN_POINT('',(-0.155723105325903,-9.93094234179315E-5,1.10940562256037));
#9412=CARTESIAN_POINT('',(-0.15555,4.36677073508985E-14,-0.129405622560373));
#9413=CARTESIAN_POINT('Ctrl Pts',(-0.155316093427556,-5.92046854689179E-5,
1.09559437743963));
#9414=CARTESIAN_POINT('Ctrl Pts',(-0.155392202162635,-0.0223004273098781,
1.09718177672503));
#9415=CARTESIAN_POINT('Ctrl Pts',(-0.140523796570003,-0.0963544111096822,
1.10247408030436));
#9416=CARTESIAN_POINT('Ctrl Pts',(-0.0266911547466422,-0.181909417300769,
1.11147128817762));
#9417=CARTESIAN_POINT('Ctrl Pts',(0.138366588630194,-0.121070809839768,
1.12258600105939));
#9418=CARTESIAN_POINT('Ctrl Pts',(0.176756544363487,0.0506021528108583,
1.13370071394117));
#9419=CARTESIAN_POINT('Ctrl Pts',(0.053334601374032,0.175951340263971,1.14481542682295));
#9420=CARTESIAN_POINT('Ctrl Pts',(-0.11141976168757,0.141779822134275,1.1554466479891));
#9421=CARTESIAN_POINT('Ctrl Pts',(-0.155347780011936,0.0447408364230817,
1.16237296486133));
#9422=CARTESIAN_POINT('Ctrl Pts',(-0.155704137558009,-0.000108555906714635,
1.16559437743963));
#9423=CARTESIAN_POINT('Ctrl Pts',(-0.155723105325903,-9.93094234179323E-5,
1.10940562256037));
#9424=CARTESIAN_POINT('Ctrl Pts',(-0.155767528832372,-0.00607323109599136,
1.10983485027824));
#9425=CARTESIAN_POINT('Ctrl Pts',(-0.152743452599297,-0.0635660122040492,
1.11396898229003));
#9426=CARTESIAN_POINT('Ctrl Pts',(-0.0812207929765285,-0.164944347467861,
1.12180801859574));
#9427=CARTESIAN_POINT('Ctrl Pts',(0.0945424741868258,-0.15768695427323,
1.13292273147752));
#9428=CARTESIAN_POINT('Ctrl Pts',(0.183756769071919,-0.00607493157030043,
1.14403744435929));
#9429=CARTESIAN_POINT('Ctrl Pts',(0.104750804765144,0.151098391369297,1.15515215724107));
#9430=CARTESIAN_POINT('Ctrl Pts',(-0.0701493549889435,0.169948589190878,
1.16626687012284));
#9431=CARTESIAN_POINT('Ctrl Pts',(-0.150655835862288,0.0704960085261505,
1.17435135856261));
#9432=CARTESIAN_POINT('Ctrl Pts',(-0.155714401116427,0.00953740333429069,
1.17873094270845));
#9433=CARTESIAN_POINT('Ctrl Pts',(-0.155629273963861,0.000132584196566117,
1.17940562256037));
#9434=CARTESIAN_POINT('Origin',(0.,0.,-0.129405622560373));
#9435=CARTESIAN_POINT('',(-0.155487379626493,0.000139458551422749,1.02559437743963));
#9436=CARTESIAN_POINT('',(-0.155325604028858,-7.03580820835548E-5,1.03940562256037));
#9437=CARTESIAN_POINT('',(-0.15555,4.36677073508985E-14,-0.129405622560373));
#9438=CARTESIAN_POINT('Ctrl Pts',(-0.155487379626493,0.000139458551422741,
1.02559437743963));
#9439=CARTESIAN_POINT('Ctrl Pts',(-0.15516015826044,-0.0374642026468413,
1.02828568429481));
#9440=CARTESIAN_POINT('Ctrl Pts',(-0.122567220013461,-0.127342229539981,
1.03468189544392));
#9441=CARTESIAN_POINT('Ctrl Pts',(0.0277609020139879,-0.181749239788739,
1.04478301088696));
#9442=CARTESIAN_POINT('Ctrl Pts',(0.167759977846949,-0.0752332617743367,
1.05589772376874));
#9443=CARTESIAN_POINT('Ctrl Pts',(0.154183067891921,0.10015505688606,1.06701243665051));
#9444=CARTESIAN_POINT('Ctrl Pts',(-0.000540836401177662,0.183856360619919,
1.07812714953229));
#9445=CARTESIAN_POINT('Ctrl Pts',(-0.132742730727165,0.111330221780279,
1.08765446312866));
#9446=CARTESIAN_POINT('Ctrl Pts',(-0.155214568480931,0.0296093864093298,
1.09347687243111));
#9447=CARTESIAN_POINT('Ctrl Pts',(-0.155316093427556,-5.92046854689179E-5,
1.09559437743963));
#9448=CARTESIAN_POINT('Ctrl Pts',(-0.155325604028858,-7.03580820835287E-5,
1.03940562256037));
#9449=CARTESIAN_POINT('Ctrl Pts',(-0.155413268812163,-0.0215479955240541,
1.04093875784802));
#9450=CARTESIAN_POINT('Ctrl Pts',(-0.141237759605696,-0.0948168172565819,
1.04617679742959));
#9451=CARTESIAN_POINT('Ctrl Pts',(-0.0293463034743252,-0.181499998473078,
1.05511974130508));
#9452=CARTESIAN_POINT('Ctrl Pts',(0.136582774532958,-0.123079651747206,
1.06623445418686));
#9453=CARTESIAN_POINT('Ctrl Pts',(0.177477058724911,0.048014045858363,1.07734916706863));
#9454=CARTESIAN_POINT('Ctrl Pts',(0.0558998488320383,0.175153252535857,
1.08846387995041));
#9455=CARTESIAN_POINT('Ctrl Pts',(-0.110179630765451,0.143230603341919,
1.09914936511432));
#9456=CARTESIAN_POINT('Ctrl Pts',(-0.155384084723293,0.0454910252069913,
1.10612994598431));
#9457=CARTESIAN_POINT('Ctrl Pts',(-0.155723105325903,-9.93094234179323E-5,
1.10940562256037));
#9458=CARTESIAN_POINT('Origin',(0.,0.,-0.129405622560373));
#9459=CARTESIAN_POINT('',(-0.155800812044169,-2.33349500279874E-5,0.955594377439629));
#9460=CARTESIAN_POINT('',(-0.155465886400055,0.000136334869802884,0.969405622560371));
#9461=CARTESIAN_POINT('',(-0.15555,4.36677073508985E-14,-0.129405622560373));
#9462=CARTESIAN_POINT('Ctrl Pts',(-0.155800812044169,-2.33349500279754E-5,
0.955594377439629));
#9463=CARTESIAN_POINT('Ctrl Pts',(-0.155803439542059,-0.00127859733407187,
0.95568468757067));
#9464=CARTESIAN_POINT('Ctrl Pts',(-0.155221069917255,-0.0540275413746436,
0.959479901995636));
#9465=CARTESIAN_POINT('Ctrl Pts',(-0.0959152937319705,-0.156855698885072,
0.966980020714528));
#9466=CARTESIAN_POINT('Ctrl Pts',(0.0797779258821927,-0.165647023475673,
0.978094733596302));
#9467=CARTESIAN_POINT('Ctrl Pts',(0.182438389002691,-0.0227966677941671,
0.989209446478081));
#9468=CARTESIAN_POINT('Ctrl Pts',(0.118085504862125,0.140922912920049,1.00032415935986));
#9469=CARTESIAN_POINT('Ctrl Pts',(-0.0543688349964322,0.175634517181406,
1.01143887224163));
#9470=CARTESIAN_POINT('Ctrl Pts',(-0.147344990269918,0.0800886216370419,
1.01986227826822));
#9471=CARTESIAN_POINT('Ctrl Pts',(-0.15561061742745,0.0143017138157724,
1.02458078000089));
#9472=CARTESIAN_POINT('Ctrl Pts',(-0.155487379626493,0.000139458551422741,
1.02559437743963));
#9473=CARTESIAN_POINT('Ctrl Pts',(-0.155465886400055,0.000136334869802876,
0.969405622560371));
#9474=CARTESIAN_POINT('Ctrl Pts',(-0.15515576719121,-0.0367220611351339,
0.972042665417797));
#9475=CARTESIAN_POINT('Ctrl Pts',(-0.123611600275362,-0.125841774747843,
0.978384612569147));
#9476=CARTESIAN_POINT('Ctrl Pts',(0.0251022815740214,-0.182135472747933,
0.988431464014426));
#9477=CARTESIAN_POINT('Ctrl Pts',(0.166642788778922,-0.0776764824211173,
0.999546176896201));
#9478=CARTESIAN_POINT('Ctrl Pts',(0.155630041687788,0.0978914965540504,
1.01066088977798));
#9479=CARTESIAN_POINT('Ctrl Pts',(0.00214566711329121,0.183844638447722,
1.02177560265976));
#9480=CARTESIAN_POINT('Ctrl Pts',(-0.131860770774095,0.112855894150209,
1.03135718025388));
#9481=CARTESIAN_POINT('Ctrl Pts',(-0.155201422124717,0.0303538762959815,
1.03723385355409));
#9482=CARTESIAN_POINT('Ctrl Pts',(-0.155325604028858,-7.03580820835287E-5,
1.03940562256037));
#9483=CARTESIAN_POINT('Origin',(0.,0.,-0.129405622560373));
#9484=CARTESIAN_POINT('',(-0.155419028575706,-0.000124905745103449,0.885594377439629));
#9485=CARTESIAN_POINT('',(-0.155804426663874,-9.35735450183217E-6,0.899405622560371));
#9486=CARTESIAN_POINT('',(-0.15555,4.36677073508985E-14,-0.129405622560373));
#9487=CARTESIAN_POINT('Ctrl Pts',(-0.155419028575706,-0.000124905745103449,
0.885594377439629));
#9488=CARTESIAN_POINT('Ctrl Pts',(-0.155544942580047,-0.0168294139448893,
0.88678859514045));
#9489=CARTESIAN_POINT('Ctrl Pts',(-0.145367891922091,-0.0852081429960637,
0.891687717135198));
#9490=CARTESIAN_POINT('Ctrl Pts',(-0.0457655175701415,-0.178070130134034,
0.90029174342387));
#9491=CARTESIAN_POINT('Ctrl Pts',(0.124797271018106,-0.135015165780915,
0.911406456305646));
#9492=CARTESIAN_POINT('Ctrl Pts',(0.18111431299722,0.0316395238895826,0.922521169187422));
#9493=CARTESIAN_POINT('Ctrl Pts',(0.071630133994783,0.169329789902144,0.933635882069198));
#9494=CARTESIAN_POINT('Ctrl Pts',(-0.102005504702542,0.152147737220529,
0.944660284819935));
#9495=CARTESIAN_POINT('Ctrl Pts',(-0.15569564844375,0.0502175852432928,
0.951979783276744));
#9496=CARTESIAN_POINT('Ctrl Pts',(-0.155800812044169,-2.33349500279754E-5,
0.955594377439629));
#9497=CARTESIAN_POINT('Ctrl Pts',(-0.155804426663874,-9.35735450181938E-6,
0.899405622560371));
#9498=CARTESIAN_POINT('Ctrl Pts',(-0.155804862851121,-0.000510348018169845,
0.899441668693652));
#9499=CARTESIAN_POINT('Ctrl Pts',(-0.155575767654156,-0.0525038984009843,
0.90318261912086));
#9500=CARTESIAN_POINT('Ctrl Pts',(-0.0981969772278097,-0.155437475007334,
0.910628473841992));
#9501=CARTESIAN_POINT('Ctrl Pts',(0.0773490332209564,-0.16679503000125,
0.921743186723768));
#9502=CARTESIAN_POINT('Ctrl Pts',(0.182085818614306,-0.0254599613686364,
0.932857899605545));
#9503=CARTESIAN_POINT('Ctrl Pts',(0.120132017548368,0.139182446210336,0.943972612487321));
#9504=CARTESIAN_POINT('Ctrl Pts',(-0.0517967206657041,0.176410188769281,
0.955087325369096));
#9505=CARTESIAN_POINT('Ctrl Pts',(-0.146766922130325,0.0816263333357911,
0.963564995393448));
#9506=CARTESIAN_POINT('Ctrl Pts',(-0.155591468107198,0.0150620155784236,
0.968337761123872));
#9507=CARTESIAN_POINT('Ctrl Pts',(-0.155465886400055,0.000136334869802876,
0.969405622560371));
#9508=CARTESIAN_POINT('Origin',(0.,0.,-0.129405622560373));
#9509=CARTESIAN_POINT('',(-0.155353971596541,9.41326338506563E-5,0.815594377439629));
#9510=CARTESIAN_POINT('',(-0.15543853527939,-0.000130502868957535,0.829405622560371));
#9511=CARTESIAN_POINT('',(-0.15555,4.36677073508985E-14,-0.129405622560373));
#9512=CARTESIAN_POINT('Ctrl Pts',(-0.155353971596541,9.41326338506562E-5,
0.815594377439629));
#9513=CARTESIAN_POINT('Ctrl Pts',(-0.155176235752476,-0.0320855025530675,
0.817892502710232));
#9514=CARTESIAN_POINT('Ctrl Pts',(-0.129743274287226,-0.116400787456992,
0.823895532274761));
#9515=CARTESIAN_POINT('Ctrl Pts',(0.00839855685065273,-0.18366523374673,
0.833603466133212));
#9516=CARTESIAN_POINT('Ctrl Pts',(0.158870089284654,-0.0925405239616719,
0.844718179014991));
#9517=CARTESIAN_POINT('Ctrl Pts',(0.163903890459678,0.0833004714068091,
0.855832891896764));
#9518=CARTESIAN_POINT('Ctrl Pts',(0.0188917636673275,0.182883993585968,
0.866947604778543));
#9519=CARTESIAN_POINT('Ctrl Pts',(-0.125975846208109,0.122335050954643,
0.876868099959496));
#9520=CARTESIAN_POINT('Ctrl Pts',(-0.15515431084261,0.0349941389255136,
0.883083690846525));
#9521=CARTESIAN_POINT('Ctrl Pts',(-0.155419028575706,-0.000124905745103449,
0.885594377439629));
#9522=CARTESIAN_POINT('Ctrl Pts',(-0.15543853527939,-0.000130502868957542,
0.82940562256037));
#9523=CARTESIAN_POINT('Ctrl Pts',(-0.155565218715822,-0.0160709251164858,
0.830545576263433));
#9524=CARTESIAN_POINT('Ctrl Pts',(-0.145977858350589,-0.0836697618712271,
0.835390434260421));
#9525=CARTESIAN_POINT('Ctrl Pts',(-0.0483625319738309,-0.177382413092208,
0.843940196551336));
#9526=CARTESIAN_POINT('Ctrl Pts',(0.122811155175551,-0.136824249085392,
0.855054909433111));
#9527=CARTESIAN_POINT('Ctrl Pts',(0.18155728681432,0.0289897667799704,0.866169622314888));
#9528=CARTESIAN_POINT('Ctrl Pts',(0.0740966767894734,0.168265080935085,
0.877284335196663));
#9529=CARTESIAN_POINT('Ctrl Pts',(-0.100627295271696,0.153549890455044,
0.888363001945158));
#9530=CARTESIAN_POINT('Ctrl Pts',(-0.155760030525013,0.0509826220191848,
0.895736764399727));
#9531=CARTESIAN_POINT('Ctrl Pts',(-0.155804426663874,-9.35735450181938E-6,
0.899405622560371));
#9532=CARTESIAN_POINT('Origin',(0.,0.,-0.129405622560373));
#9533=CARTESIAN_POINT('',(-0.155761438252094,7.41758372851551E-5,0.74559437743963));
#9534=CARTESIAN_POINT('',(-0.155340757131295,8.43414871359027E-5,0.759405622560371));
#9535=CARTESIAN_POINT('',(-0.15555,4.36677073508985E-14,-0.129405622560373));
#9536=CARTESIAN_POINT('Ctrl Pts',(-0.155761438252094,7.41758372851484E-5,
0.74559437743963));
#9537=CARTESIAN_POINT('Ctrl Pts',(-0.155482663215916,-0.0472440860383338,
0.748996410280013));
#9538=CARTESIAN_POINT('Ctrl Pts',(-0.107218957683579,-0.146585393585093,
0.756103347414322));
#9539=CARTESIAN_POINT('Ctrl Pts',(0.0618259562826469,-0.173150238157939,
0.766915188842555));
#9540=CARTESIAN_POINT('Ctrl Pts',(0.179007701381185,-0.0419487388444433,
0.778029901724333));
#9541=CARTESIAN_POINT('Ctrl Pts',(0.132316724534454,0.127654761967143,0.789144614606108));
#9542=CARTESIAN_POINT('Ctrl Pts',(-0.0355036877557856,0.180396624137356,
0.800259327487885));
#9543=CARTESIAN_POINT('Ctrl Pts',(-0.142843189124192,0.0912350616645566,
0.809075915099058));
#9544=CARTESIAN_POINT('Ctrl Pts',(-0.155462771173448,0.0197926392114622,
0.814187598416307));
#9545=CARTESIAN_POINT('Ctrl Pts',(-0.155353971596541,9.41326338506562E-5,
0.815594377439629));
#9546=CARTESIAN_POINT('Ctrl Pts',(-0.155340757131295,8.43414871358941E-5,
0.759405622560371));
#9547=CARTESIAN_POINT('Ctrl Pts',(-0.155186065178493,-0.0313421581146853,
0.761649483833214));
#9548=CARTESIAN_POINT('Ctrl Pts',(-0.130663644838326,-0.114879826414827,
0.767598249399983));
#9549=CARTESIAN_POINT('Ctrl Pts',(0.0057140072891202,-0.183768346278771,
0.777251919260679));
#9550=CARTESIAN_POINT('Ctrl Pts',(0.157500961365389,-0.0948520012562343,
0.788366632142453));
#9551=CARTESIAN_POINT('Ctrl Pts',(0.165103553267307,0.080896672810716,0.799481345024232));
#9552=CARTESIAN_POINT('Ctrl Pts',(0.0215619850688987,0.182588432747595,
0.810596057906006));
#9553=CARTESIAN_POINT('Ctrl Pts',(-0.124972046377392,0.123843126491084,
0.820570817084721));
#9554=CARTESIAN_POINT('Ctrl Pts',(-0.155153491462033,0.0357362129042795,
0.826840671969508));
#9555=CARTESIAN_POINT('Ctrl Pts',(-0.15543853527939,-0.000130502868957542,
0.82940562256037));
#9556=CARTESIAN_POINT('Origin',(0.,0.,-0.129405622560373));
#9557=CARTESIAN_POINT('',(-0.155576082774588,-0.000140575406353809,0.675594377439629));
#9558=CARTESIAN_POINT('',(-0.155746091141148,8.55458678441536E-5,0.689405622560371));
#9559=CARTESIAN_POINT('',(-0.15555,4.36677073508985E-14,-0.129405622560373));
#9560=CARTESIAN_POINT('Ctrl Pts',(-0.155576082774588,-0.000140575406353826,
0.675594377439629));
#9561=CARTESIAN_POINT('Ctrl Pts',(-0.15567933078646,-0.0113165881608609,
0.676395413555869));
#9562=CARTESIAN_POINT('Ctrl Pts',(-0.149480883924574,-0.0740696137198915,
0.680901353966033));
#9563=CARTESIAN_POINT('Ctrl Pts',(-0.0643273434762849,-0.172236601004835,
0.689112198670122));
#9564=CARTESIAN_POINT('Ctrl Pts',(0.10983032453655,-0.147447460665183,0.7002269115519));
#9565=CARTESIAN_POINT('Ctrl Pts',(0.183443747273531,0.0123225577969614,
0.711341624433675));
#9566=CARTESIAN_POINT('Ctrl Pts',(0.0891234668368183,0.160811882345183,
0.722456337315452));
#9567=CARTESIAN_POINT('Ctrl Pts',(-0.0867849519149494,0.162085859856851,
0.733571050197227));
#9568=CARTESIAN_POINT('Ctrl Pts',(-0.153720861082027,0.0600054806471056,
0.74128373023862));
#9569=CARTESIAN_POINT('Ctrl Pts',(-0.155786256648735,0.00428676032007601,
0.745291505986088));
#9570=CARTESIAN_POINT('Ctrl Pts',(-0.155761438252094,7.41758372851484E-5,
0.74559437743963));
#9571=CARTESIAN_POINT('Ctrl Pts',(-0.155746091141148,8.5545867844157E-5,
0.689405622560371));
#9572=CARTESIAN_POINT('Ctrl Pts',(-0.155437871285066,-0.0464900844783075,
0.692753391402996));
#9573=CARTESIAN_POINT('Ctrl Pts',(-0.108502980662635,-0.145148810790092,
0.699806064539545));
#9574=CARTESIAN_POINT('Ctrl Pts',(0.0592893454135225,-0.174035135802431,
0.710563641970021));
#9575=CARTESIAN_POINT('Ctrl Pts',(0.17837565371923,-0.0445598601161589,
0.721678354851797));
#9576=CARTESIAN_POINT('Ctrl Pts',(0.134167848541566,0.125707769811822,0.732793067733573));
#9577=CARTESIAN_POINT('Ctrl Pts',(-0.0328640048105861,0.18089613639087,
0.743907780615349));
#9578=CARTESIAN_POINT('Ctrl Pts',(-0.142163443840071,0.0927734423224093,
0.752778632224282));
#9579=CARTESIAN_POINT('Ctrl Pts',(-0.15544148153917,0.0205470449866602,
0.757944579539289));
#9580=CARTESIAN_POINT('Ctrl Pts',(-0.155340757131295,8.43414871358941E-5,
0.759405622560371));
#9581=CARTESIAN_POINT('Origin',(0.,0.,-0.129405622560373));
#9582=CARTESIAN_POINT('',(-0.155295522970368,1.20667024935662E-5,0.605594377439629));
#9583=CARTESIAN_POINT('',(-0.155599079595997,-0.000137936170561209,0.61940562256037));
#9584=CARTESIAN_POINT('',(-0.15555,4.36677073508985E-14,-0.129405622560373));
#9585=CARTESIAN_POINT('Ctrl Pts',(-0.155295522970368,1.20667024935545E-5,
0.605594377439629));
#9586=CARTESIAN_POINT('Ctrl Pts',(-0.155277046884744,-0.0266871317790742,
0.607499321125649));
#9587=CARTESIAN_POINT('Ctrl Pts',(-0.136042101589265,-0.105338263915341,
0.613109169105595));
#9588=CARTESIAN_POINT('Ctrl Pts',(-0.0110578453815636,-0.183524325090524,
0.622423921379466));
#9589=CARTESIAN_POINT('Ctrl Pts',(0.148200983745356,-0.108811406852975,
0.633538634261242));
#9590=CARTESIAN_POINT('Ctrl Pts',(0.171789121533681,0.0655129877741882,
0.644653347143018));
#9591=CARTESIAN_POINT('Ctrl Pts',(0.0381127912063918,0.179863473198069,
0.655768060024794));
#9592=CARTESIAN_POINT('Ctrl Pts',(-0.118305335710584,0.133183342609015,
0.666081736790332));
#9593=CARTESIAN_POINT('Ctrl Pts',(-0.155201794262491,0.0403740370228492,
0.672690509261943));
#9594=CARTESIAN_POINT('Ctrl Pts',(-0.155576082774588,-0.000140575406353826,
0.675594377439629));
#9595=CARTESIAN_POINT('Ctrl Pts',(-0.155599079595997,-0.000137936170561192,
0.61940562256037));
#9596=CARTESIAN_POINT('Ctrl Pts',(-0.155694978954011,-0.0105529059502578,
0.620152394678851));
#9597=CARTESIAN_POINT('Ctrl Pts',(-0.149993983311601,-0.0725344660767061,
0.624604071091256));
#9598=CARTESIAN_POINT('Ctrl Pts',(-0.0668371390874247,-0.171278287625556,
0.632760651797588));
#9599=CARTESIAN_POINT('Ctrl Pts',(0.107664149845629,-0.14903652509151,0.643875364679364));
#9600=CARTESIAN_POINT('Ctrl Pts',(0.183604219596519,0.00964082567459112,
0.654990077561139));
#9601=CARTESIAN_POINT('Ctrl Pts',(0.0914636816765205,0.159492476021631,
0.666104790442917));
#9602=CARTESIAN_POINT('Ctrl Pts',(-0.084407345824762,0.163336630748138,
0.677219503324691));
#9603=CARTESIAN_POINT('Ctrl Pts',(-0.153309057596064,0.0615339443022911,
0.684986447363844));
#9604=CARTESIAN_POINT('Ctrl Pts',(-0.155778971618438,0.00505417110609329,
0.68904848710907));
#9605=CARTESIAN_POINT('Ctrl Pts',(-0.155746091141148,8.5545867844157E-5,
0.689405622560371));
#9606=CARTESIAN_POINT('Origin',(0.,0.,-0.129405622560373));
#9607=CARTESIAN_POINT('',(-0.155620384233268,0.000134389116543367,0.535594377439629));
#9608=CARTESIAN_POINT('',(-0.155294662735063,-4.07947690456786E-7,0.549405622560371));
#9609=CARTESIAN_POINT('',(-0.15555,4.36677073508985E-14,-0.129405622560373));
#9610=CARTESIAN_POINT('Ctrl Pts',(-0.155620384233268,0.000134389116543364,
0.535594377439629));
#9611=CARTESIAN_POINT('Ctrl Pts',(-0.155238150029612,-0.0418142075950562,
0.538603228695431));
#9612=CARTESIAN_POINT('Ctrl Pts',(-0.11609848048108,-0.136044184148923,
0.545316984245157));
#9613=CARTESIAN_POINT('Ctrl Pts',(0.0431815857942205,-0.178714309703255,
0.555735644088809));
#9614=CARTESIAN_POINT('Ctrl Pts',(0.173572271754774,-0.0606310178233981,
0.566850356970585));
#9615=CARTESIAN_POINT('Ctrl Pts',(0.145066103517367,0.112956980548805,0.577965069852361));
#9616=CARTESIAN_POINT('Ctrl Pts',(-0.0162409278223676,0.183138434272774,
0.589079782734138));
#9617=CARTESIAN_POINT('Ctrl Pts',(-0.137582057103126,0.102371477526338,
0.598289551929893));
#9618=CARTESIAN_POINT('Ctrl Pts',(-0.155312980823089,0.0252398494879608,
0.603794416831724));
#9619=CARTESIAN_POINT('Ctrl Pts',(-0.155295522970368,1.20667024935545E-5,
0.605594377439629));
#9620=CARTESIAN_POINT('Ctrl Pts',(-0.155294677199358,-4.07924581107E-7,
0.549405622560371));
#9621=CARTESIAN_POINT('Ctrl Pts',(-0.155295283821613,-0.025939410100839,
0.551256302248632));
#9622=CARTESIAN_POINT('Ctrl Pts',(-0.136845372042004,-0.103805290649511,
0.556811886230819));
#9623=CARTESIAN_POINT('Ctrl Pts',(-0.0137382592728754,-0.183343162418143,
0.56607237450693));
#9624=CARTESIAN_POINT('Ctrl Pts',(0.146595250104258,-0.110965254112288,
0.577187087388706));
#9625=CARTESIAN_POINT('Ctrl Pts',(0.172728038096355,0.0629958715212238,
0.588301800270483));
#9626=CARTESIAN_POINT('Ctrl Pts',(0.0407368261671239,0.179287383736737,
0.599416513152259));
#9627=CARTESIAN_POINT('Ctrl Pts',(-0.117173152128599,0.134664213612,0.609784453915555));
#9628=CARTESIAN_POINT('Ctrl Pts',(-0.155219200688461,0.0411180995720497,
0.616447490384925));
#9629=CARTESIAN_POINT('Ctrl Pts',(-0.155599079595997,-0.000137936170561192,
0.61940562256037));
#9630=CARTESIAN_POINT('Origin',(0.,0.,-0.129405622560373));
#9631=CARTESIAN_POINT('',(-0.155730199251335,-9.53986324873634E-5,0.465594377439629));
#9632=CARTESIAN_POINT('',(-0.155597581791774,0.000138145146615302,0.47940562256037));
#9633=CARTESIAN_POINT('',(-0.15555,4.36677073508985E-14,-0.129405622560373));
#9634=CARTESIAN_POINT('Ctrl Pts',(-0.155730199251335,-9.53986324873637E-5,
0.465594377439629));
#9635=CARTESIAN_POINT('Ctrl Pts',(-0.155771125211943,-0.00577117291295923,
0.466002231971286));
#9636=CARTESIAN_POINT('Ctrl Pts',(-0.15291335048013,-0.0629633964300589,
0.470114990796868));
#9637=CARTESIAN_POINT('Ctrl Pts',(-0.0821687549726806,-0.164474160738562,
0.477932653916376));
#9638=CARTESIAN_POINT('Ctrl Pts',(0.093633366925239,-0.158228462808239,
0.489047366798152));
#9639=CARTESIAN_POINT('Ctrl Pts',(0.183718759405662,-0.00713241101304534,
0.500162079679928));
#9640=CARTESIAN_POINT('Ctrl Pts',(0.105618688669037,0.150493011293707,0.511276792561704));
#9641=CARTESIAN_POINT('Ctrl Pts',(-0.0691700824248357,0.170349504084268,
0.52239150544348));
#9642=CARTESIAN_POINT('Ctrl Pts',(-0.150461957560835,0.0711002170416349,
0.530497367069456));
#9643=CARTESIAN_POINT('Ctrl Pts',(-0.15570880843776,0.00983857377168744,
0.534898324401505));
#9644=CARTESIAN_POINT('Ctrl Pts',(-0.155620384233268,0.000134389116543364,
0.535594377439629));
#9645=CARTESIAN_POINT('Ctrl Pts',(-0.155597581791774,0.000138145146615299,
0.47940562256037));
#9646=CARTESIAN_POINT('Ctrl Pts',(-0.155217974184216,-0.0410694712136483,
0.482360209818413));
#9647=CARTESIAN_POINT('Ctrl Pts',(-0.117247668926727,-0.134567610636498,
0.489019701370381));
#9648=CARTESIAN_POINT('Ctrl Pts',(0.0405656647148524,-0.179326188326124,
0.499384097216273));
#9649=CARTESIAN_POINT('Ctrl Pts',(0.172667825243738,-0.0631607243382489,
0.51049881009805));
#9650=CARTESIAN_POINT('Ctrl Pts',(0.146701107748166,0.110825267691061,0.521613522979825));
#9651=CARTESIAN_POINT('Ctrl Pts',(-0.0135632385845353,0.183356193057212,
0.532728235861603));
#9652=CARTESIAN_POINT('Ctrl Pts',(-0.136793374447236,0.103905470129892,
0.541992269055116));
#9653=CARTESIAN_POINT('Ctrl Pts',(-0.155294069415139,0.0259882795758376,
0.547551397954706));
#9654=CARTESIAN_POINT('Ctrl Pts',(-0.155294677199358,-4.07924581107E-7,
0.549405622560371));
#9655=CARTESIAN_POINT('Origin',(0.,0.,-0.129405622560373));
#9656=CARTESIAN_POINT('',(-0.155329799149561,-7.46101974259461E-5,0.395594377439629));
#9657=CARTESIAN_POINT('',(-0.155747148273957,-8.48283479504552E-5,0.40940562256037));
#9658=CARTESIAN_POINT('',(-0.15555,4.36677073508985E-14,-0.129405622560373));
#9659=CARTESIAN_POINT('Ctrl Pts',(-0.155329799149561,-7.46101974259585E-5,
0.395594377439629));
#9660=CARTESIAN_POINT('Ctrl Pts',(-0.155421611019211,-0.0212513995734132,
0.397106139541067));
#9661=CARTESIAN_POINT('Ctrl Pts',(-0.141514901582445,-0.0942110799989907,
0.40232280593643));
#9662=CARTESIAN_POINT('Ctrl Pts',(-0.030390408656302,-0.18132809188354,
0.411244376625719));
#9663=CARTESIAN_POINT('Ctrl Pts',(0.135872146613563,-0.123863689671489,
0.422359089507495));
#9664=CARTESIAN_POINT('Ctrl Pts',(0.177750452880091,0.0469918114711103,
0.433473802389271));
#9665=CARTESIAN_POINT('Ctrl Pts',(0.0569069861965436,0.174828626850531,
0.444588515271047));
#9666=CARTESIAN_POINT('Ctrl Pts',(-0.109686020656632,0.143800409504297,
0.455295373621167));
#9667=CARTESIAN_POINT('Ctrl Pts',(-0.15539935842889,0.045786916726629,0.46229732767736));
#9668=CARTESIAN_POINT('Ctrl Pts',(-0.155730199251335,-9.53986324873637E-5,
0.465594377439629));
#9669=CARTESIAN_POINT('Ctrl Pts',(-0.155747148273957,-8.48283479504535E-5,
0.40940562256037));
#9670=CARTESIAN_POINT('Ctrl Pts',(-0.155779482799656,-0.00500404714443213,
0.409759213094268));
#9671=CARTESIAN_POINT('Ctrl Pts',(-0.153336323268121,-0.0614340654297066,
0.413817707922091));
#9672=CARTESIAN_POINT('Ctrl Pts',(-0.0845632241029054,-0.163255983359439,
0.42158110704384));
#9673=CARTESIAN_POINT('Ctrl Pts',(0.0913113927969153,-0.159579712115361,
0.432695819925616));
#9674=CARTESIAN_POINT('Ctrl Pts',(0.183594933073833,-0.00981608490943425,
0.443810532807392));
#9675=CARTESIAN_POINT('Ctrl Pts',(0.107806367033371,0.148933683901261,0.454925245689169));
#9676=CARTESIAN_POINT('Ctrl Pts',(-0.0666736110104746,0.171342010517439,
0.466039958570945));
#9677=CARTESIAN_POINT('Ctrl Pts',(-0.149960857132942,0.0726347328707636,
0.474200084194679));
#9678=CARTESIAN_POINT('Ctrl Pts',(-0.155693983092541,0.0106028137662625,
0.478655305524487));
#9679=CARTESIAN_POINT('Ctrl Pts',(-0.155597581791774,0.000138145146615299,
0.47940562256037));
#9680=CARTESIAN_POINT('Origin',(0.,0.,-0.129405622560373));
#9681=CARTESIAN_POINT('',(-0.155457619458094,0.000134802415058048,0.325594377439629));
#9682=CARTESIAN_POINT('',(-0.155341574103549,-8.50015047459685E-5,0.33940562256037));
#9683=CARTESIAN_POINT('',(-0.15555,4.36677073508985E-14,-0.129405622560373));
#9684=CARTESIAN_POINT('Ctrl Pts',(-0.155457619458094,0.000134802415058059,
0.325594377439629));
#9685=CARTESIAN_POINT('Ctrl Pts',(-0.155154675739571,-0.0364297795001245,
0.328210047110848));
#9686=CARTESIAN_POINT('Ctrl Pts',(-0.124018139179925,-0.125249838662379,
0.334530621075992));
#9687=CARTESIAN_POINT('Ctrl Pts',(0.0240536163419306,-0.182276924995041,
0.344556099335061));
#9688=CARTESIAN_POINT('Ctrl Pts',(0.166192972555312,-0.078634278260764,
0.355670812216838));
#9689=CARTESIAN_POINT('Ctrl Pts',(0.156190859040095,0.0969941719726652,
0.366785525098613));
#9690=CARTESIAN_POINT('Ctrl Pts',(0.00320371741518769,0.183829241523736,
0.37790023798039));
#9691=CARTESIAN_POINT('Ctrl Pts',(-0.131508890630062,0.113456296578242,
0.387503188760728));
#9692=CARTESIAN_POINT('Ctrl Pts',(-0.15519660591439,0.0306469631491546,
0.393401235247141));
#9693=CARTESIAN_POINT('Ctrl Pts',(-0.155329799149561,-7.46101974259585E-5,
0.395594377439629));
#9694=CARTESIAN_POINT('Ctrl Pts',(-0.155341574103549,-8.50015047459546E-5,
0.33940562256037));
#9695=CARTESIAN_POINT('Ctrl Pts',(-0.15544287226748,-0.0204977876623303,
0.340863120664049));
#9696=CARTESIAN_POINT('Ctrl Pts',(-0.142208294129094,-0.0926729514204939,
0.346025523061653));
#9697=CARTESIAN_POINT('Ctrl Pts',(-0.0330366684018241,-0.180864682882801,
0.354892829753183));
#9698=CARTESIAN_POINT('Ctrl Pts',(0.134047790173482,-0.125835785541829,
0.366007542634959));
#9699=CARTESIAN_POINT('Ctrl Pts',(0.178418108088907,0.0443895672348972,
0.377122255516735));
#9700=CARTESIAN_POINT('Ctrl Pts',(0.0594554476394192,0.173978460503991,
0.388236968398511));
#9701=CARTESIAN_POINT('Ctrl Pts',(-0.108419677339067,0.145242852620103,
0.39899809074639));
#9702=CARTESIAN_POINT('Ctrl Pts',(-0.155440683223253,0.0465392864424033,
0.406054308800343));
#9703=CARTESIAN_POINT('Ctrl Pts',(-0.155747148273957,-8.48283479504535E-5,
0.40940562256037));
#9704=CARTESIAN_POINT('Origin',(0.,0.,-0.129405622560373));
#9705=CARTESIAN_POINT('',(-0.15580501159203,-3.81191605503711E-6,0.255594377439629));
#9706=CARTESIAN_POINT('',(-0.155437230887358,0.000130168175253818,0.26940562256037));
#9707=CARTESIAN_POINT('',(-0.15555,4.36677073508985E-14,-0.129405622560373));
#9708=CARTESIAN_POINT('Ctrl Pts',(-0.15580501159203,-3.81191605504483E-6,
0.255594377439629));
#9709=CARTESIAN_POINT('Ctrl Pts',(-0.155805085024067,-0.000207743207977253,
0.255609050386703));
#9710=CARTESIAN_POINT('Ctrl Pts',(-0.15571236399541,-0.05190405066865,0.259328627627703));
#9711=CARTESIAN_POINT('Ctrl Pts',(-0.0990899426121504,-0.154869742320406,
0.266753109162628));
#9712=CARTESIAN_POINT('Ctrl Pts',(0.0763877910491314,-0.167237433721381,
0.277867822044404));
#9713=CARTESIAN_POINT('Ctrl Pts',(0.181936269483671,-0.0265075025422269,
0.288982534926181));
#9714=CARTESIAN_POINT('Ctrl Pts',(0.120931066297065,0.138488739775033,0.300097247807957));
#9715=CARTESIAN_POINT('Ctrl Pts',(-0.0507805637499992,0.17670537114635,
0.311211960689733));
#9716=CARTESIAN_POINT('Ctrl Pts',(-0.146535504929177,0.0822320925013407,
0.31971100390029));
#9717=CARTESIAN_POINT('Ctrl Pts',(-0.155583773303352,0.0153612696655085,
0.324505142816922));
#9718=CARTESIAN_POINT('Ctrl Pts',(-0.155457619458094,0.000134802415058059,
0.325594377439629));
#9719=CARTESIAN_POINT('Ctrl Pts',(-0.155437230887358,0.00013016817525382,
0.26940562256037));
#9720=CARTESIAN_POINT('Ctrl Pts',(-0.155153480292112,-0.0356877371401405,
0.27196702823383));
#9721=CARTESIAN_POINT('Ctrl Pts',(-0.125038150141719,-0.1237447022416,0.278233338201215));
#9722=CARTESIAN_POINT('Ctrl Pts',(0.0213876812582842,-0.182608932054395,
0.288204552462526));
#9723=CARTESIAN_POINT('Ctrl Pts',(0.1650262562684,-0.0810542393413567,0.299319265344302));
#9724=CARTESIAN_POINT('Ctrl Pts',(0.157591432764151,0.0947016118771478,
0.310433978226078));
#9725=CARTESIAN_POINT('Ctrl Pts',(0.00588942498427058,0.183762808117002,
0.321548691107855));
#9726=CARTESIAN_POINT('Ctrl Pts',(-0.130604027396502,0.114979253369884,
0.331205905885952));
#9727=CARTESIAN_POINT('Ctrl Pts',(-0.155185376218898,0.031390732051916,
0.337158216370124));
#9728=CARTESIAN_POINT('Ctrl Pts',(-0.155341574103549,-8.50015047459546E-5,
0.33940562256037));
#9729=CARTESIAN_POINT('Origin',(0.,0.,-0.129405622560373));
#9730=CARTESIAN_POINT('',(-0.155446481294809,-0.000132426206499563,0.185594377439629));
#9731=CARTESIAN_POINT('',(-0.155804282564045,1.0275387755743E-5,0.19940562256037));
#9732=CARTESIAN_POINT('',(-0.15555,4.36677073508985E-14,-0.129405622560373));
#9733=CARTESIAN_POINT('Ctrl Pts',(-0.155446481294809,-0.000132426206499552,
0.185594377439629));
#9734=CARTESIAN_POINT('Ctrl Pts',(-0.15557308597482,-0.0157719577277014,
0.186712957956484));
#9735=CARTESIAN_POINT('Ctrl Pts',(-0.14621431385393,-0.0830638986146384,
0.191536442767265));
#9736=CARTESIAN_POINT('Ctrl Pts',(-0.0493826231024586,-0.177101125876806,
0.200064831871971));
#9737=CARTESIAN_POINT('Ctrl Pts',(0.122021650540482,-0.137528801235027,
0.211179544753747));
#9738=CARTESIAN_POINT('Ctrl Pts',(0.181721122596515,0.027944365932959,0.222294257635524));
#9739=CARTESIAN_POINT('Ctrl Pts',(0.0750638686912215,0.167835840141849,
0.2334089705173));
#9740=CARTESIAN_POINT('Ctrl Pts',(-0.10007913601891,0.154100039675233,0.244509010452001));
#9741=CARTESIAN_POINT('Ctrl Pts',(-0.155786543508857,0.0512847017165995,
0.251904146092778));
#9742=CARTESIAN_POINT('Ctrl Pts',(-0.15580501159203,-3.81191605504483E-6,
0.255594377439629));
#9743=CARTESIAN_POINT('Ctrl Pts',(-0.155804282564045,1.02753877557394E-5,
0.19940562256037));
#9744=CARTESIAN_POINT('Ctrl Pts',(-0.155755696547123,-0.0509325620518932,
0.203070935803611));
#9745=CARTESIAN_POINT('Ctrl Pts',(-0.100717920681623,-0.153458525692979,
0.210441153340777));
#9746=CARTESIAN_POINT('Ctrl Pts',(0.0739360216217259,-0.168335735272026,
0.221516275171869));
#9747=CARTESIAN_POINT('Ctrl Pts',(0.181529531305135,-0.0291630630877277,
0.232630988053645));
#9748=CARTESIAN_POINT('Ctrl Pts',(0.122941707923409,0.13670695445041,0.243745700935421));
#9749=CARTESIAN_POINT('Ctrl Pts',(-0.0481931854649256,0.177428497887793,
0.254860413817197));
#9750=CARTESIAN_POINT('Ctrl Pts',(-0.145938433460327,0.0837702536114789,
0.263413721025514));
#9751=CARTESIAN_POINT('Ctrl Pts',(-0.155563906805031,0.0161204994767368,
0.268262123939905));
#9752=CARTESIAN_POINT('Ctrl Pts',(-0.155437230887358,0.00013016817525382,
0.26940562256037));
#9753=CARTESIAN_POINT('Origin',(0.,0.,-0.129405622560373));
#9754=CARTESIAN_POINT('',(-0.15533593717049,8.0492722526641E-5,0.115594377439629));
#9755=CARTESIAN_POINT('',(-0.155467267562279,-0.000136569073934972,0.12940562256037));
#9756=CARTESIAN_POINT('',(-0.15555,4.36677073508985E-14,-0.129405622560373));
#9757=CARTESIAN_POINT('Ctrl Pts',(-0.15533593717049,8.04927225266511E-5,
0.115594377439629));
#9758=CARTESIAN_POINT('Ctrl Pts',(-0.155190332415358,-0.0310491436783933,
0.117816865526265));
#9759=CARTESIAN_POINT('Ctrl Pts',(-0.131021645937763,-0.114280472202705,
0.123744257906827));
#9760=CARTESIAN_POINT('Ctrl Pts',(0.00465630089802304,-0.183797982260963,
0.133376554581314));
#9761=CARTESIAN_POINT('Ctrl Pts',(0.156952427521129,-0.0957570050449602,
0.14449126746309));
#9762=CARTESIAN_POINT('Ctrl Pts',(0.165566412512777,0.0799451630251659,
0.155605980344867));
#9763=CARTESIAN_POINT('Ctrl Pts',(0.0226124784964766,0.182461279865869,
0.166720693226643));
#9764=CARTESIAN_POINT('Ctrl Pts',(-0.124571916682485,0.124436273223993,
0.176716825591564));
#9765=CARTESIAN_POINT('Ctrl Pts',(-0.155153752528961,0.036028486330431,
0.183008053662559));
#9766=CARTESIAN_POINT('Ctrl Pts',(-0.155446481294809,-0.000132426206499552,
0.185594377439629));
#9767=CARTESIAN_POINT('Ctrl Pts',(-0.155467267562279,-0.000136569073934965,
0.12940562256037));
#9768=CARTESIAN_POINT('Ctrl Pts',(-0.155592737404977,-0.0150123740177689,
0.130469939079467));
#9769=CARTESIAN_POINT('Ctrl Pts',(-0.146805111767969,-0.0815259022509084,
0.135239159892488));
#9770=CARTESIAN_POINT('Ctrl Pts',(-0.0519650836355626,-0.176360636356525,
0.143713284999436));
#9771=CARTESIAN_POINT('Ctrl Pts',(0.119999097845339,-0.139297072446483,
0.154827997881212));
#9772=CARTESIAN_POINT('Ctrl Pts',(0.182110041762725,0.0252861433827556,
0.165942710762988));
#9773=CARTESIAN_POINT('Ctrl Pts',(0.0775082145815245,0.166721114602665,
0.177057423644764));
#9774=CARTESIAN_POINT('Ctrl Pts',(-0.0980485553243366,0.155531142530291,
0.18817213652654));
#9775=CARTESIAN_POINT('Ctrl Pts',(-0.15555294238022,0.0526034030257051,
0.195621536165076));
#9776=CARTESIAN_POINT('Ctrl Pts',(-0.155804807368156,0.000560536804787789,
0.199366031509686));
#9777=CARTESIAN_POINT('Ctrl Pts',(-0.155804282564045,1.02753877557394E-5,
0.19940562256037));
#9778=CARTESIAN_POINT('Origin',(0.,0.,-0.129405622560373));
#9779=CARTESIAN_POINT('',(-0.155737693224454,0.000100603112028587,0.045594377439629));
#9780=CARTESIAN_POINT('',(-0.155324515707295,7.08434145518383E-5,0.0594056225603703));
#9781=CARTESIAN_POINT('',(-0.15555,4.36677073508985E-14,-0.129405622560373));
#9782=CARTESIAN_POINT('Ctrl Pts',(-0.155737693224454,0.000100603112028588,
0.045594377439629));
#9783=CARTESIAN_POINT('Ctrl Pts',(-0.155418890749049,-0.0461799127824949,
0.0489207730960463));
#9784=CARTESIAN_POINT('Ctrl Pts',(-0.109006528319361,-0.14459862692607,
0.055952073046389));
#9785=CARTESIAN_POINT('Ctrl Pts',(0.0582883981674798,-0.17436384297299,
0.0666882772906571));
#9786=CARTESIAN_POINT('Ctrl Pts',(0.178115364857574,-0.0455907972452466,
0.0778029901724332));
#9787=CARTESIAN_POINT('Ctrl Pts',(0.134889573452136,0.124936168947966,0.0889177030542095));
#9788=CARTESIAN_POINT('Ctrl Pts',(-0.0318225855039178,0.181080880580275,
0.100032415935985));
#9789=CARTESIAN_POINT('Ctrl Pts',(-0.141891652849943,0.0933796088184345,
0.108924640731125));
#9790=CARTESIAN_POINT('Ctrl Pts',(-0.155433056633206,0.0208441934619002,
0.11411196123234));
#9791=CARTESIAN_POINT('Ctrl Pts',(-0.15533593717049,8.04927225266511E-5,
0.115594377439629));
#9792=CARTESIAN_POINT('Ctrl Pts',(-0.155324515707295,7.08434145518418E-5,
0.0594056225603703));
#9793=CARTESIAN_POINT('Ctrl Pts',(-0.155202011031474,-0.0303045958272501,
0.0615738466492476));
#9794=CARTESIAN_POINT('Ctrl Pts',(-0.131919585929676,-0.112758296333805,
0.0674469750320503));
#9795=CARTESIAN_POINT('Ctrl Pts',(0.00197063906297734,-0.183845261801054,
0.0770250077087785));
#9796=CARTESIAN_POINT('Ctrl Pts',(0.155536281225319,-0.0980407171232175,
0.0881397205905545));
#9797=CARTESIAN_POINT('Ctrl Pts',(0.166716989499632,0.0775177448756012,
0.0992544334723309));
#9798=CARTESIAN_POINT('Ctrl Pts',(0.0252760640494928,0.182111233028749,
0.110369146354107));
#9799=CARTESIAN_POINT('Ctrl Pts',(-0.12354388404776,0.125939975141946,0.120419542716787));
#9800=CARTESIAN_POINT('Ctrl Pts',(-0.15515597470269,0.0367705614371862,
0.126765034785541));
#9801=CARTESIAN_POINT('Ctrl Pts',(-0.155467267562279,-0.000136569073934965,
0.12940562256037));
#9802=CARTESIAN_POINT('Ctrl Pts',(-0.0685825729128552,0.139614588036684,
-0.0230074082272072));
#9803=CARTESIAN_POINT('Ctrl Pts',(-0.115011604060829,0.116807355219849,
-0.0193025039332818));
#9804=CARTESIAN_POINT('Ctrl Pts',(-0.18252632432761,0.0216311623708125,
-0.011892695345431));
#9805=CARTESIAN_POINT('Ctrl Pts',(-0.117028832316993,-0.141960369302502,
-0.00077798246365487));
#9806=CARTESIAN_POINT('Ctrl Pts',(0.0557547713450657,-0.175142639980632,
0.0103367304181214));
#9807=CARTESIAN_POINT('Ctrl Pts',(0.177419525591119,-0.0482168938798953,
0.0214514432998975));
#9808=CARTESIAN_POINT('Ctrl Pts',(0.13670630608002,0.122966787890628,0.0325661561816737));
#9809=CARTESIAN_POINT('Ctrl Pts',(-0.0291762440449378,0.181518694867924,
0.0436808690634499));
#9810=CARTESIAN_POINT('Ctrl Pts',(-0.168338109470647,0.0739316281669151,
0.0547955819452261));
#9811=CARTESIAN_POINT('Ctrl Pts',(-0.153400663029731,-0.101353247263981,
0.0659102948270022));
#9812=CARTESIAN_POINT('Ctrl Pts',(0.00197063906297734,-0.183845261801054,
0.0770250077087785));
#9813=CARTESIAN_POINT('Ctrl Pts',(0.155536281225319,-0.0980407171232175,
0.0881397205905545));
#9814=CARTESIAN_POINT('Ctrl Pts',(0.166716989499632,0.0775177448756012,
0.0992544334723309));
#9815=CARTESIAN_POINT('Ctrl Pts',(0.0252760640494928,0.182111233028749,
0.110369146354107));
#9816=CARTESIAN_POINT('Ctrl Pts',(-0.13930361365595,0.119991553257876,0.121483859235883));
#9817=CARTESIAN_POINT('Ctrl Pts',(-0.176357828501591,-0.0519748351675156,
0.132598572117659));
#9818=CARTESIAN_POINT('Ctrl Pts',(-0.0519650836355626,-0.176360636356525,
0.143713284999436));
#9819=CARTESIAN_POINT('Ctrl Pts',(0.119999097845339,-0.139297072446483,
0.154827997881212));
#9820=CARTESIAN_POINT('Ctrl Pts',(0.182110041762725,0.0252861433827556,
0.165942710762988));
#9821=CARTESIAN_POINT('Ctrl Pts',(0.0775082145815245,0.166721114602665,
0.177057423644764));
#9822=CARTESIAN_POINT('Ctrl Pts',(-0.0980485553243366,0.155531142530291,
0.18817213652654));
#9823=CARTESIAN_POINT('Ctrl Pts',(-0.183846711227048,0.00196007268919948,
0.199286849408317));
#9824=CARTESIAN_POINT('Ctrl Pts',(-0.101342268945007,-0.15340534304023,
0.210401562290092));
#9825=CARTESIAN_POINT('Ctrl Pts',(0.0739360216217259,-0.168335735272026,
0.221516275171869));
#9826=CARTESIAN_POINT('Ctrl Pts',(0.181529531305135,-0.0291630630877277,
0.232630988053645));
#9827=CARTESIAN_POINT('Ctrl Pts',(0.122941707923409,0.13670695445041,0.243745700935421));
#9828=CARTESIAN_POINT('Ctrl Pts',(-0.0481931854649256,0.177428497887793,
0.254860413817197));
#9829=CARTESIAN_POINT('Ctrl Pts',(-0.175209594506165,0.055723002131679,
0.265975126698974));
#9830=CARTESIAN_POINT('Ctrl Pts',(-0.141830261094154,-0.116994153730485,
0.27708983958075));
#9831=CARTESIAN_POINT('Ctrl Pts',(0.0213876812582842,-0.182608932054395,
0.288204552462526));
#9832=CARTESIAN_POINT('Ctrl Pts',(0.1650262562684,-0.0810542393413567,0.299319265344302));
#9833=CARTESIAN_POINT('Ctrl Pts',(0.157591432764151,0.0947016118771478,
0.310433978226078));
#9834=CARTESIAN_POINT('Ctrl Pts',(0.00588942498427058,0.183762808117002,
0.321548691107855));
#9835=CARTESIAN_POINT('Ctrl Pts',(-0.151204060903134,0.104598216713686,
0.332663403989631));
#9836=CARTESIAN_POINT('Ctrl Pts',(-0.169877686425305,-0.0703208832997102,
0.343778116871407));
#9837=CARTESIAN_POINT('Ctrl Pts',(-0.0330366684018241,-0.180864682882801,
0.354892829753183));
#9838=CARTESIAN_POINT('Ctrl Pts',(0.134047790173482,-0.125835785541829,
0.366007542634959));
#9839=CARTESIAN_POINT('Ctrl Pts',(0.178418108088907,0.0443895672348972,
0.377122255516735));
#9840=CARTESIAN_POINT('Ctrl Pts',(0.0594554476394192,0.173978460503991,
0.388236968398511));
#9841=CARTESIAN_POINT('Ctrl Pts',(-0.11393574277819,0.144298653808392,0.399351681280288));
#9842=CARTESIAN_POINT('Ctrl Pts',(-0.183024379999154,-0.0174794536315888,
0.410466394162064));
#9843=CARTESIAN_POINT('Ctrl Pts',(-0.0845632241029054,-0.163255983359439,
0.42158110704384));
#9844=CARTESIAN_POINT('Ctrl Pts',(0.0913113927969153,-0.159579712115361,
0.432695819925616));
#9845=CARTESIAN_POINT('Ctrl Pts',(0.183594933073833,-0.00981608490943425,
0.443810532807392));
#9846=CARTESIAN_POINT('Ctrl Pts',(0.107806367033371,0.148933683901261,0.454925245689169));
#9847=CARTESIAN_POINT('Ctrl Pts',(-0.0666736110104746,0.171342010517439,
0.466039958570945));
#9848=CARTESIAN_POINT('Ctrl Pts',(-0.180117186520217,0.0368951771018348,
0.477154671452721));
#9849=CARTESIAN_POINT('Ctrl Pts',(-0.128672361159773,-0.131327371278433,
0.488269384334498));
#9850=CARTESIAN_POINT('Ctrl Pts',(0.0405656647148524,-0.179326188326124,
0.499384097216273));
#9851=CARTESIAN_POINT('Ctrl Pts',(0.172667825243738,-0.0631607243382489,
0.51049881009805));
#9852=CARTESIAN_POINT('Ctrl Pts',(0.146701107748166,0.110825267691061,0.521613522979825));
#9853=CARTESIAN_POINT('Ctrl Pts',(-0.0135632385845353,0.183356193057212,
0.532728235861603));
#9854=CARTESIAN_POINT('Ctrl Pts',(-0.161411108932732,0.0880335668165284,
0.543842948743377));
#9855=CARTESIAN_POINT('Ctrl Pts',(-0.161495069857358,-0.0878794480245611,
0.554957661625155));
#9856=CARTESIAN_POINT('Ctrl Pts',(-0.0137382592728754,-0.183343162418143,
0.56607237450693));
#9857=CARTESIAN_POINT('Ctrl Pts',(0.146595250104258,-0.110965254112288,
0.577187087388706));
#9858=CARTESIAN_POINT('Ctrl Pts',(0.172728038096355,0.0629958715212238,
0.588301800270483));
#9859=CARTESIAN_POINT('Ctrl Pts',(0.0407368261671239,0.179287383736737,
0.599416513152259));
#9860=CARTESIAN_POINT('Ctrl Pts',(-0.12854694097571,0.131450138604423,0.610531226034035));
#9861=CARTESIAN_POINT('Ctrl Pts',(-0.180152323597142,-0.0367232252925209,
0.621645938915811));
#9862=CARTESIAN_POINT('Ctrl Pts',(-0.0668371390874247,-0.171278287625556,
0.632760651797588));
#9863=CARTESIAN_POINT('Ctrl Pts',(0.107664149845629,-0.14903652509151,0.643875364679364));
#9864=CARTESIAN_POINT('Ctrl Pts',(0.183604219596519,0.00964082567459112,
0.654990077561139));
#9865=CARTESIAN_POINT('Ctrl Pts',(0.0914636816765205,0.159492476021631,
0.666104790442917));
#9866=CARTESIAN_POINT('Ctrl Pts',(-0.084407345824762,0.163336630748138,
0.677219503324691));
#9867=CARTESIAN_POINT('Ctrl Pts',(-0.183007611198191,0.0176541557959064,
0.688334216206469));
#9868=CARTESIAN_POINT('Ctrl Pts',(-0.114073434464645,-0.144189828083589,
0.699448929088244));
#9869=CARTESIAN_POINT('Ctrl Pts',(0.0592893454135225,-0.174035135802431,
0.710563641970021));
#9870=CARTESIAN_POINT('Ctrl Pts',(0.17837565371923,-0.0445598601161589,
0.721678354851797));
#9871=CARTESIAN_POINT('Ctrl Pts',(0.134167848541566,0.125707769811822,0.732793067733573));
#9872=CARTESIAN_POINT('Ctrl Pts',(-0.0328640048105861,0.18089613639087,
0.743907780615349));
#9873=CARTESIAN_POINT('Ctrl Pts',(-0.169810482613085,0.0704830119109969,
0.755022493497126));
#9874=CARTESIAN_POINT('Ctrl Pts',(-0.151303838645199,-0.104453833747555,
0.766137206378901));
#9875=CARTESIAN_POINT('Ctrl Pts',(0.0057140072891202,-0.183768346278771,
0.777251919260679));
#9876=CARTESIAN_POINT('Ctrl Pts',(0.157500961365389,-0.0948520012562343,
0.788366632142453));
#9877=CARTESIAN_POINT('Ctrl Pts',(0.165103553267307,0.080896672810716,0.799481345024232));
#9878=CARTESIAN_POINT('Ctrl Pts',(0.0215619850688987,0.182588432747595,
0.810596057906006));
#9879=CARTESIAN_POINT('Ctrl Pts',(-0.141718517021854,0.117129487775116,
0.821710770787783));
#9880=CARTESIAN_POINT('Ctrl Pts',(-0.17526270634378,-0.0555557264230108,
0.832825483669558));
#9881=CARTESIAN_POINT('Ctrl Pts',(-0.0483625319738309,-0.177382413092208,
0.843940196551336));
#9882=CARTESIAN_POINT('Ctrl Pts',(0.122811155175551,-0.136824249085392,
0.855054909433111));
#9883=CARTESIAN_POINT('Ctrl Pts',(0.18155728681432,0.0289897667799704,0.866169622314888));
#9884=CARTESIAN_POINT('Ctrl Pts',(0.0740966767894734,0.168265080935085,
0.877284335196663));
#9885=CARTESIAN_POINT('Ctrl Pts',(-0.101195786384157,0.153502012336733,
0.88839904807844));
#9886=CARTESIAN_POINT('Ctrl Pts',(-0.183848498104576,-0.00178457782861093,
0.899513760960216));
#9887=CARTESIAN_POINT('Ctrl Pts',(-0.0981969772278097,-0.155437475007334,
0.910628473841992));
#9888=CARTESIAN_POINT('Ctrl Pts',(0.0773490332209564,-0.16679503000125,
0.921743186723768));
#9889=CARTESIAN_POINT('Ctrl Pts',(0.182085818614306,-0.0254599613686364,
0.932857899605545));
#9890=CARTESIAN_POINT('Ctrl Pts',(0.120132017548368,0.139182446210336,0.943972612487321));
#9891=CARTESIAN_POINT('Ctrl Pts',(-0.0517967206657041,0.176410188769281,
0.955087325369096));
#9892=CARTESIAN_POINT('Ctrl Pts',(-0.1763081157273,0.0521431040696983,0.966202038250874));
#9893=CARTESIAN_POINT('Ctrl Pts',(-0.139418126366054,-0.11985842070507,
0.977316751132648));
#9894=CARTESIAN_POINT('Ctrl Pts',(0.0251022815740214,-0.182135472747933,
0.988431464014426));
#9895=CARTESIAN_POINT('Ctrl Pts',(0.166642788778922,-0.0776764824211173,
0.999546176896201));
#9896=CARTESIAN_POINT('Ctrl Pts',(0.155630041687788,0.0978914965540504,
1.01066088977798));
#9897=CARTESIAN_POINT('Ctrl Pts',(0.00214566711329121,0.183844638447722,
1.02177560265976));
#9898=CARTESIAN_POINT('Ctrl Pts',(-0.153302959879009,0.1014970810697,1.03289031554153));
#9899=CARTESIAN_POINT('Ctrl Pts',(-0.168410288012087,-0.073766048186277,
1.04400502842331));
#9900=CARTESIAN_POINT('Ctrl Pts',(-0.0293463034743252,-0.181499998473078,
1.05511974130508));
#9901=CARTESIAN_POINT('Ctrl Pts',(0.136582774532958,-0.123079651747206,
1.06623445418686));
#9902=CARTESIAN_POINT('Ctrl Pts',(0.177477058724911,0.048014045858363,1.07734916706863));
#9903=CARTESIAN_POINT('Ctrl Pts',(0.0558998488320383,0.175153252535857,
1.08846387995041));
#9904=CARTESIAN_POINT('Ctrl Pts',(-0.116850915683094,0.141948295084362,
1.09957859283219));
#9905=CARTESIAN_POINT('Ctrl Pts',(-0.182630429983634,-0.0212033256195195,
1.11069330571396));
#9906=CARTESIAN_POINT('Ctrl Pts',(-0.0812207929765285,-0.164944347467861,
1.12180801859574));
#9907=CARTESIAN_POINT('Ctrl Pts',(0.0945424741868258,-0.15768695427323,
1.13292273147752));
#9908=CARTESIAN_POINT('Ctrl Pts',(0.183756769071919,-0.00607493157030043,
1.14403744435929));
#9909=CARTESIAN_POINT('Ctrl Pts',(0.104750804765144,0.151098391369297,1.15515215724107));
#9910=CARTESIAN_POINT('Ctrl Pts',(-0.0701493549889435,0.169948589190878,
1.16626687012284));
#9911=CARTESIAN_POINT('Ctrl Pts',(-0.180831240020515,0.033219235481529,
1.17738158300462));
#9912=CARTESIAN_POINT('Ctrl Pts',(-0.125971043419533,-0.133920689936726,
1.1884962958864));
#9913=CARTESIAN_POINT('Ctrl Pts',(0.0442094305335735,-0.178462828693349,
1.19961100876817));
#9914=CARTESIAN_POINT('Ctrl Pts',(0.173918351244622,-0.0596310495772682,
1.21072572164995));
#9915=CARTESIAN_POINT('Ctrl Pts',(0.144413599053411,0.113790014420313,1.22184043453173));
#9916=CARTESIAN_POINT('Ctrl Pts',(-0.0172946805849302,0.183041932345569,
1.2329551474135));
#9917=CARTESIAN_POINT('Ctrl Pts',(-0.16317053312232,0.0847279888461446,
1.24406986029528));
#9918=CARTESIAN_POINT('Ctrl Pts',(-0.159671810165464,-0.0911502496530778,
1.25518457317705));
#9919=CARTESIAN_POINT('Ctrl Pts',(-0.0100014200241654,-0.183584930129994,
1.26629928605883));
#9920=CARTESIAN_POINT('Ctrl Pts',(0.148824776878697,-0.107956661491269,
1.2774139989406));
#9921=CARTESIAN_POINT('Ctrl Pts',(0.171409230594902,0.0665006063145147,
1.28852871182238));
#9922=CARTESIAN_POINT('Ctrl Pts',(0.0370769876137034,0.180079848852746,
1.29964342470416));
#9923=CARTESIAN_POINT('Ctrl Pts',(-0.13119740888887,0.128804871313864,1.31075813758594));
#9924=CARTESIAN_POINT('Ctrl Pts',(-0.17936704821676,-0.0403846132498615,
1.32187285046771));
#9925=CARTESIAN_POINT('Ctrl Pts',(-0.0633350012944175,-0.172603976154579,
1.33298756334949));
#9926=CARTESIAN_POINT('Ctrl Pts',(0.110677115627384,-0.146812911726923,
1.34410227623126));
#9927=CARTESIAN_POINT('Ctrl Pts',(0.183369791793454,0.0133781325662369,
1.35521698911304));
#9928=CARTESIAN_POINT('Ctrl Pts',(0.0881964673803512,0.161322156305205,
1.36633170199482));
#9929=CARTESIAN_POINT('Ctrl Pts',(-0.087716373065073,0.161583702363956,
1.37744641487659));
#9930=CARTESIAN_POINT('Ctrl Pts',(-0.183329200145536,0.013923338225167,
1.38856112775837));
#9931=CARTESIAN_POINT('Ctrl Pts',(-0.111113186298513,-0.146483155358991,
1.39967584064014));
#9932=CARTESIAN_POINT('Ctrl Pts',(0.062821469496632,-0.172791544768887,
1.41079055352192));
#9933=CARTESIAN_POINT('Ctrl Pts',(0.179246168325776,-0.0409177970309031,
1.4219052664037));
#9934=CARTESIAN_POINT('Ctrl Pts',(0.131579840483081,0.12841417582098,1.43301997928547));
#9935=CARTESIAN_POINT('Ctrl Pts',(-0.0365413417972516,0.180189304102632,
1.44413469216725));
#9936=CARTESIAN_POINT('Ctrl Pts',(-0.171210727883091,0.0670100114242395,
1.45524940504903));
#9937=CARTESIAN_POINT('Ctrl Pts',(-0.149145136714026,-0.107513641775772,
1.4663641179308));
#9938=CARTESIAN_POINT('Ctrl Pts',(0.00945547127077659,-0.183613858508507,
1.47747883081258));
#9939=CARTESIAN_POINT('Ctrl Pts',(0.159400061651521,-0.0916246436218211,
1.48859354369435));
#9940=CARTESIAN_POINT('Ctrl Pts',(0.163421757209686,0.0842424135684204,
1.49970825657613));
#9941=CARTESIAN_POINT('Ctrl Pts',(0.0178388940120074,0.182989695977022,
1.51082296945791));
#9942=CARTESIAN_POINT('Ctrl Pts',(-0.144074596838477,0.114218936780048,
1.52193768233968));
#9943=CARTESIAN_POINT('Ctrl Pts',(-0.174094900049997,-0.059113625755116,
1.53305239522146));
#9944=CARTESIAN_POINT('Ctrl Pts',(-0.0447399086353324,-0.178330579398589,
1.54416710810323));
#9945=CARTESIAN_POINT('Ctrl Pts',(0.125572262560343,-0.134294682876169,
1.55528182098501));
#9946=CARTESIAN_POINT('Ctrl Pts',(0.180929220612589,0.0326813723985916,
1.56639653386679));
#9947=CARTESIAN_POINT('Ctrl Pts',(0.0706544006326465,0.16973924308944,1.57751124674856));
#9948=CARTESIAN_POINT('Ctrl Pts',(-0.104301038447746,0.151409208280264,
1.58862595963034));
#9949=CARTESIAN_POINT('Ctrl Pts',(-0.183774020961904,-0.0055284891994118,
1.59974067251211));
#9950=CARTESIAN_POINT('Ctrl Pts',(-0.0950109510297781,-0.157405127482403,
1.61085538539389));
#9951=CARTESIAN_POINT('Ctrl Pts',(0.08072995862503,-0.165185134784385,1.62197009827567));
#9952=CARTESIAN_POINT('Ctrl Pts',(0.18256657276441,-0.0217462981307606,
1.63308481115744));
#9953=CARTESIAN_POINT('Ctrl Pts',(0.117272493730902,0.141600201933013,1.64419952403922));
#9954=CARTESIAN_POINT('Ctrl Pts',(-0.0553787694277143,0.175318700856487,
1.65531423692099));
#9955=CARTESIAN_POINT('Ctrl Pts',(-0.177333500459066,0.0485415758733555,
1.66642894980278));
#9956=CARTESIAN_POINT('Ctrl Pts',(-0.136948157917673,-0.12267296774877,
1.67754366268455));
#9957=CARTESIAN_POINT('Ctrl Pts',(0.0288064689070301,-0.181586459634089,
1.68865837556633));
#9958=CARTESIAN_POINT('Ctrl Pts',(0.168190194183902,-0.0742665035780993,
1.6997730884481));
#9959=CARTESIAN_POINT('Ctrl Pts',(0.153604091834597,0.101040773675795,1.71088780132988));
#9960=CARTESIAN_POINT('Ctrl Pts',(-0.00159898082742857,0.183850205965748,
1.72200251421165));
#9961=CARTESIAN_POINT('Ctrl Pts',(-0.155338265403761,0.098353842195845,
1.73311722709343));
#9962=CARTESIAN_POINT('Ctrl Pts',(-0.166873029294335,-0.0771806132877065,
1.74423193997521));
#9963=CARTESIAN_POINT('Ctrl Pts',(-0.025643765052489,-0.182060023858252,
1.75534665285698));
#9964=CARTESIAN_POINT('Ctrl Pts',(0.139061101343075,-0.120272461796479,
1.76646136573876));
#9965=CARTESIAN_POINT('Ctrl Pts',(0.176462387959855,0.0516186071958565,
1.77757607862053));
#9966=CARTESIAN_POINT('Ctrl Pts',(0.0523210615336027,0.176255387132795,
1.78869079150231));
#9967=CARTESIAN_POINT('Ctrl Pts',(-0.119717616249168,0.139539053074583,
1.79980550438409));
#9968=CARTESIAN_POINT('Ctrl Pts',(-0.182160720834928,-0.0249184020000041,
1.81092021726586));
#9969=CARTESIAN_POINT('Ctrl Pts',(-0.0778446696726029,-0.16656428902048,
1.82203493014764));
#9970=CARTESIAN_POINT('Ctrl Pts',(0.0977343372718058,-0.155728784402163,
1.83314964302942));
#9971=CARTESIAN_POINT('Ctrl Pts',(0.183842378706508,-0.00233125821546848,
1.84426435591119));
#9972=CARTESIAN_POINT('Ctrl Pts',(0.101651789551148,0.15320041988971,1.85537906879297));
#9973=CARTESIAN_POINT('Ctrl Pts',(-0.0735959994667044,0.168484669438591,
1.86649378167474));
#9974=CARTESIAN_POINT('Ctrl Pts',(-0.181470280731337,0.0295295137891618,
1.87760849455652));
#9975=CARTESIAN_POINT('Ctrl Pts',(-0.12321747011018,-0.136458455337079,
1.88872320743829));
#9976=CARTESIAN_POINT('Ctrl Pts',(0.0478348573047686,-0.177525438740387,
1.89983792032007));
#9977=CARTESIAN_POINT('Ctrl Pts',(0.175096732074868,-0.0560766385408066,
1.91095263320185));
#9978=CARTESIAN_POINT('Ctrl Pts',(0.142066184410422,0.116707558540133,1.92206734608362));
#9979=CARTESIAN_POINT('Ctrl Pts',(-0.0210189483701118,0.182651741800479,
1.9331820589654));
#9980=CARTESIAN_POINT('Ctrl Pts',(-0.16486227057344,0.0813872638359589,
1.94429677184718));
#9981=CARTESIAN_POINT('Ctrl Pts',(-0.157782315082607,-0.0943832401462696,
1.95541148472895));
#9982=CARTESIAN_POINT('Ctrl Pts',(-0.0062604319656806,-0.183750542760931,
1.96652619761073));
#9983=CARTESIAN_POINT('Ctrl Pts',(0.150992567850975,-0.10490328606436,1.9776409104925));
#9984=CARTESIAN_POINT('Ctrl Pts',(0.170019318761453,0.0699777551885857,
1.98875562337428));
#9985=CARTESIAN_POINT('Ctrl Pts',(0.0334017687074566,0.180797612872902,
1.99987033625606));
#9986=CARTESIAN_POINT('Ctrl Pts',(-0.133793453221103,0.126106172919867,
2.01098504913783));
#9987=CARTESIAN_POINT('Ctrl Pts',(-0.178507367426113,-0.0440292487783591,
2.02209976201961));
#9988=CARTESIAN_POINT('Ctrl Pts',(-0.0598065907447483,-0.173858064744653,
2.03321447490139));
#9989=CARTESIAN_POINT('Ctrl Pts',(0.113644170098336,-0.144528397126456,
2.04432918778316));
#9990=CARTESIAN_POINT('Ctrl Pts',(0.183059298154547,0.0171098899136208,
2.05544390066494));
#9991=CARTESIAN_POINT('Ctrl Pts',(0.0848926672411447,0.163084916597067,
2.06655861354672));
#9992=CARTESIAN_POINT('Ctrl Pts',(-0.0909890136144577,0.159763745495145,
2.07767332642849));
#9993=CARTESIAN_POINT('Ctrl Pts',(-0.183574740100876,0.0101867449437282,
2.08878803931027));
#9994=CARTESIAN_POINT('Ctrl Pts',(-0.108106845918033,-0.148715718183394,
2.09990275219204));
#9995=CARTESIAN_POINT('Ctrl Pts',(0.0663275338242693,-0.17147627599867,
2.11101746507382));
#9996=CARTESIAN_POINT('Ctrl Pts',(0.180042327710072,-0.0372587603217594,
2.1221321779556));
#9997=CARTESIAN_POINT('Ctrl Pts',(0.128937250118005,0.131067312760423,2.13324689083737));
#9998=CARTESIAN_POINT('Ctrl Pts',(-0.0402035204677608,0.179407725381376,
2.14436160371915));
#9999=CARTESIAN_POINT('Ctrl Pts',(-0.172539951470817,0.0635092135777934,
2.15547631660092));
#10000=CARTESIAN_POINT('Ctrl Pts',(-0.146924565505413,-0.110528850528984,
2.1665910294827));
#10001=CARTESIAN_POINT('Ctrl Pts',(0.013193011805229,-0.183383204120377,
2.17770574236448));
#10002=CARTESIAN_POINT('Ctrl Pts',(0.161233041383799,-0.0883592771818423,
2.18882045524625));
#10003=CARTESIAN_POINT('Ctrl Pts',(0.161672166186531,0.08755320703735,2.19993516812803));
#10004=CARTESIAN_POINT('Ctrl Pts',(0.0141084106240242,0.183315054230848,
2.2110498810098));
#10005=CARTESIAN_POINT('Ctrl Pts',(-0.146370925859051,0.111260999182195,
2.22216459389158));
#10006=CARTESIAN_POINT('Ctrl Pts',(-0.172854847713642,-0.0626469919088142,
2.23327930677336));
#10007=CARTESIAN_POINT('Ctrl Pts',(-0.0410987787696598,-0.179204792201909,
2.24439401965513));
#10008=CARTESIAN_POINT('Ctrl Pts',(0.128281379817428,-0.13170936649677,
2.25550873253691));
#10009=CARTESIAN_POINT('Ctrl Pts',(0.18022591070051,0.0363593415954858,
2.26662344541869));
#10010=CARTESIAN_POINT('Ctrl Pts',(0.0671831774557089,0.171143144838974,
2.27773815830046));
#10011=CARTESIAN_POINT('Ctrl Pts',(-0.107363712783848,0.149253308736201,
2.28885287118224));
#10012=CARTESIAN_POINT('Ctrl Pts',(-0.18362200020929,-0.0092695600841741,
2.29996758406402));
#10013=CARTESIAN_POINT('Ctrl Pts',(-0.0917880045327959,-0.15930852573796,
2.31108229694579));
#10014=CARTESIAN_POINT('Ctrl Pts',(0.0840821369721223,-0.163504736890904,
2.32219700982757));
#10015=CARTESIAN_POINT('Ctrl Pts',(0.182962573561233,-0.0180273813676558,
2.33331172270934));
#10016=CARTESIAN_POINT('Ctrl Pts',(0.114381487141248,0.143966386512752,
2.34442643559112));
#10017=CARTESIAN_POINT('Ctrl Pts',(-0.0589705282315283,0.174140844480832,
2.35554114847289));
#10018=CARTESIAN_POINT('Ctrl Pts',(-0.178222903013509,0.0449459198210797,
2.36665586135467));
#10019=CARTESIAN_POINT('Ctrl Pts',(-0.134542235007309,-0.125486577151581,
2.37777057423645));
#10020=CARTESIAN_POINT('Ctrl Pts',(0.0327466243405011,-0.180863000230457,
2.38888528711822));
#10021=CARTESIAN_POINT('Ctrl Pts',(0.123618421332056,-0.107657388085867,
2.39629509570608));
#10022=CARTESIAN_POINT('Ctrl Pts',(0.143545299885864,-0.0599211930845618,
2.4));
#10023=CARTESIAN_POINT('Ctrl Pts',(-0.0744392439309176,0.151537102412042,
-0.0153382721514717));
#10024=CARTESIAN_POINT('Ctrl Pts',(-0.124833124304749,0.126782225262728,
-0.0116333678575463));
#10025=CARTESIAN_POINT('Ctrl Pts',(-0.198113325344336,0.023478375100856,
-0.0042235592696955));
#10026=CARTESIAN_POINT('Ctrl Pts',(-0.127022615597461,-0.154083203796675,
0.00689115361208068));
#10027=CARTESIAN_POINT('Ctrl Pts',(0.0605160006134741,-0.190099104575569,
0.0180058664938568));
#10028=CARTESIAN_POINT('Ctrl Pts',(0.192570426897894,-0.0523344192653271,
0.0291205793756331));
#10029=CARTESIAN_POINT('Ctrl Pts',(0.148380465079886,0.133467648273019,
0.0402352922574092));
#10030=CARTESIAN_POINT('Ctrl Pts',(-0.0316677758679159,0.197019648453023,
0.0513500051391854));
#10031=CARTESIAN_POINT('Ctrl Pts',(-0.182713495011001,0.0802450866099659,
0.0624647180209616));
#10032=CARTESIAN_POINT('Ctrl Pts',(-0.166500451783044,-0.110008399741151,
0.0735794309027378));
#10033=CARTESIAN_POINT('Ctrl Pts',(0.00213892357312778,-0.199544894679597,
0.0846941437845138));
#10034=CARTESIAN_POINT('Ctrl Pts',(0.168818443031448,-0.106412993084556,
0.0958088566662903));
#10035=CARTESIAN_POINT('Ctrl Pts',(0.180953938029707,0.0841374430075943,
0.106923569548066));
#10036=CARTESIAN_POINT('Ctrl Pts',(0.0274345364643011,0.197662786947523,
0.118038282429843));
#10037=CARTESIAN_POINT('Ctrl Pts',(-0.151199572092017,0.130238340780269,
0.129152995311619));
#10038=CARTESIAN_POINT('Ctrl Pts',(-0.191418065222447,-0.0564132733576527,
0.140267708193395));
#10039=CARTESIAN_POINT('Ctrl Pts',(-0.0564026890847757,-0.191421112856703,
0.151382421075171));
#10040=CARTESIAN_POINT('Ctrl Pts',(0.130246529644629,-0.151192472290029,
0.162497133956947));
#10041=CARTESIAN_POINT('Ctrl Pts',(0.197661493952255,0.0274454765313785,
0.173611846838723));
#10042=CARTESIAN_POINT('Ctrl Pts',(0.0841270988654031,0.180958415399658,
0.1847265597205));
#10043=CARTESIAN_POINT('Ctrl Pts',(-0.106421500635976,0.168812865512893,
0.195841272602275));
#10044=CARTESIAN_POINT('Ctrl Pts',(-0.199546467880638,0.00212745487426852,
0.206955985484052));
#10045=CARTESIAN_POINT('Ctrl Pts',(-0.109996483918663,-0.16650553144729,
0.218070698365828));
#10046=CARTESIAN_POINT('Ctrl Pts',(0.0802498552478435,-0.182710918065531,
0.229185411247605));
#10047=CARTESIAN_POINT('Ctrl Pts',(0.19703141027762,-0.0316534693109011,
0.24030012412938));
#10048=CARTESIAN_POINT('Ctrl Pts',(0.133440426579246,0.14838116881846,0.251414837011157));
#10049=CARTESIAN_POINT('Ctrl Pts',(-0.0523086862487663,0.192580165391978,
0.262529549892933));
#10050=CARTESIAN_POINT('Ctrl Pts',(-0.190171776743541,0.0604815184392873,
0.273644262774709));
#10051=CARTESIAN_POINT('Ctrl Pts',(-0.153941984879862,-0.126984975601611,
0.284758975656486));
#10052=CARTESIAN_POINT('Ctrl Pts',(0.0232141016978955,-0.198202987432875,
0.295873688538261));
#10053=CARTESIAN_POINT('Ctrl Pts',(0.179118823100709,-0.0879759396258336,
0.306988401420038));
#10054=CARTESIAN_POINT('Ctrl Pts',(0.17104909609995,0.102788741917448,0.318103114301814));
#10055=CARTESIAN_POINT('Ctrl Pts',(0.00639235777248694,0.199455399788411,
0.32921782718359));
#10056=CARTESIAN_POINT('Ctrl Pts',(-0.164116268825541,0.113530476300182,
0.340332540065366));
#10057=CARTESIAN_POINT('Ctrl Pts',(-0.18438454553609,-0.0763259989099004,
0.351447252947142));
#10058=CARTESIAN_POINT('Ctrl Pts',(-0.0358578646641422,-0.196309786521245,
0.362561965828918));
#10059=CARTESIAN_POINT('Ctrl Pts',(0.14549492279625,-0.136581646580809,
0.373676678710695));
#10060=CARTESIAN_POINT('Ctrl Pts',(0.193654284253789,0.0481802545901155,
0.384791391592471));
#10061=CARTESIAN_POINT('Ctrl Pts',(0.0645326995164768,0.188835508936616,
0.395906104474247));
#10062=CARTESIAN_POINT('Ctrl Pts',(-0.123665388872078,0.156621168228757,
0.407020817356023));
#10063=CARTESIAN_POINT('Ctrl Pts',(-0.198653912931686,-0.0189721274282693,
0.418135530237799));
#10064=CARTESIAN_POINT('Ctrl Pts',(-0.0917845773237327,-0.177197376131055,
0.429250243119575));
#10065=CARTESIAN_POINT('Ctrl Pts',(0.0991090120039419,-0.173207166369719,
0.440364956001352));
#10066=CARTESIAN_POINT('Ctrl Pts',(0.199273188903667,-0.0106543383834273,
0.451479668883127));
#10067=CARTESIAN_POINT('Ctrl Pts',(0.117012589526199,0.161652010920368,
0.462594381764904));
#10068=CARTESIAN_POINT('Ctrl Pts',(-0.0723672644954619,0.185973916912209,
0.473709094646681));
#10069=CARTESIAN_POINT('Ctrl Pts',(-0.195498457028802,0.0400458742142447,
0.484823807528456));
#10070=CARTESIAN_POINT('Ctrl Pts',(-0.139660454146413,-0.142542191262248,
0.495938520410233));
#10071=CARTESIAN_POINT('Ctrl Pts',(0.0440298064461046,-0.19463991082649,
0.507053233292008));
#10072=CARTESIAN_POINT('Ctrl Pts',(0.187412950789573,-0.0685543916796767,
0.518167946173786));
#10073=CARTESIAN_POINT('Ctrl Pts',(0.159228781901736,0.120289291943693,
0.529282659055561));
#10074=CARTESIAN_POINT('Ctrl Pts',(-0.0147214836452785,0.19901406146679,
0.540397371937338));
#10075=CARTESIAN_POINT('Ctrl Pts',(-0.175194956979385,0.0955512731009747,
0.551512084819113));
#10076=CARTESIAN_POINT('Ctrl Pts',(-0.175286087823317,-0.0953839931949897,
0.56262679770089));
#10077=CARTESIAN_POINT('Ctrl Pts',(-0.0149114503840338,-0.19899991806448,
0.573741510582666));
#10078=CARTESIAN_POINT('Ctrl Pts',(0.159113884448319,-0.12044123263232,
0.584856223464442));
#10079=CARTESIAN_POINT('Ctrl Pts',(0.187478305573349,0.068375461106829,
0.595970936346218));
#10080=CARTESIAN_POINT('Ctrl Pts',(0.0442155843858271,0.194597792483998,
0.607085649227995));
#10081=CARTESIAN_POINT('Ctrl Pts',(-0.139524323591982,0.142675442415383,
0.618200362109771));
#10082=CARTESIAN_POINT('Ctrl Pts',(-0.195536594668278,-0.0398592384242233,
0.629315074991547));
#10083=CARTESIAN_POINT('Ctrl Pts',(-0.0725447572008543,-0.18590475234618,
0.640429787873323));
#10084=CARTESIAN_POINT('Ctrl Pts',(0.116858227572727,-0.16176363432733,
0.651544500755099));
#10085=CARTESIAN_POINT('Ctrl Pts',(0.19928326845738,0.010464112727274,0.662659213636875));
#10086=CARTESIAN_POINT('Ctrl Pts',(0.0992743057305387,0.173112480670647,
0.673773926518652));
#10087=CARTESIAN_POINT('Ctrl Pts',(-0.0916153876786538,0.177284910476655,
0.684888639400427));
#10088=CARTESIAN_POINT('Ctrl Pts',(-0.198635712143757,0.0191617484423541,
0.696003352282205));
#10089=CARTESIAN_POINT('Ctrl Pts',(-0.123814838864976,-0.156503049232485,
0.707118065163979));
#10090=CARTESIAN_POINT('Ctrl Pts',(0.0643524128403538,-0.188897024073568,
0.718232778045757));
#10091=CARTESIAN_POINT('Ctrl Pts',(0.193608204454711,-0.0483650897864192,
0.729347490927532));
#10092=CARTESIAN_POINT('Ctrl Pts',(0.145625233657563,0.136442698831435,
0.74046220380931));
#10093=CARTESIAN_POINT('Ctrl Pts',(-0.0356704563089337,0.196343926030162,
0.751576916691083));
#10094=CARTESIAN_POINT('Ctrl Pts',(-0.184311602793374,0.0765019726409902,
0.762691629572863));
#10095=CARTESIAN_POINT('Ctrl Pts',(-0.164224567178383,-0.113373763619712,
0.773806342454636));
#10096=CARTESIAN_POINT('Ctrl Pts',(0.00620196012416494,-0.199461410886526,
0.784921055336414));
#10097=CARTESIAN_POINT('Ctrl Pts',(0.170950898814037,-0.102951973933957,
0.796035768218188));
#10098=CARTESIAN_POINT('Ctrl Pts',(0.179202720946941,0.0878049175584046,
0.807150481099967));
#10099=CARTESIAN_POINT('Ctrl Pts',(0.0234032903405015,0.198180737569178,
0.818265193981741));
#10100=CARTESIAN_POINT('Ctrl Pts',(-0.153820698321162,0.127131866619725,
0.829379906863519));
#10101=CARTESIAN_POINT('Ctrl Pts',(-0.190229424114698,-0.0602999580697674,
0.840494619745293));
#10102=CARTESIAN_POINT('Ctrl Pts',(-0.0524924942563878,-0.192530145143477,
0.851609332627072));
#10103=CARTESIAN_POINT('Ctrl Pts',(0.13329872516108,-0.148508479935175,
0.862724045508846));
#10104=CARTESIAN_POINT('Ctrl Pts',(0.197061535993685,0.0314653742077725,
0.873838758390623));
#10105=CARTESIAN_POINT('Ctrl Pts',(0.0804242297093462,0.182634230137408,
0.884953471272399));
#10106=CARTESIAN_POINT('Ctrl Pts',(-0.109837492346678,0.166610455906041,
0.896068184154175));
#10107=CARTESIAN_POINT('Ctrl Pts',(-0.199548407350193,-0.00193697347089583,
0.907182897035951));
#10108=CARTESIAN_POINT('Ctrl Pts',(-0.106582597162507,-0.168711199166861,
0.918297609917728));
#10109=CARTESIAN_POINT('Ctrl Pts',(0.0839543240681803,-0.181038642870743,
0.929412322799503));
#10110=CARTESIAN_POINT('Ctrl Pts',(0.197635202246108,-0.027634137861807,
0.94052703568128));
#10111=CARTESIAN_POINT('Ctrl Pts',(0.130390800146249,0.151068057442487,
0.951641748563056));
#10112=CARTESIAN_POINT('Ctrl Pts',(-0.0562199486064098,0.191474896842688,
0.962756461444832));
#10113=CARTESIAN_POINT('Ctrl Pts',(-0.19136410718071,0.0565959117353481,
0.973871174326609));
#10114=CARTESIAN_POINT('Ctrl Pts',(-0.151323863718857,-0.130093839252372,
0.984985887208385));
#10115=CARTESIAN_POINT('Ctrl Pts',(0.0272459136767254,-0.197689096639511,
0.996100600090161));
#10116=CARTESIAN_POINT('Ctrl Pts',(0.180873400871156,-0.084309736089776,
1.00721531297194));
#10117=CARTESIAN_POINT('Ctrl Pts',(0.168920210253646,0.106251029689549,
1.01833002585371));
#10118=CARTESIAN_POINT('Ctrl Pts',(0.00232889830253915,0.199544218094441,
1.02944473873549));
#10119=CARTESIAN_POINT('Ctrl Pts',(-0.166394405183155,0.110164516365158,
1.04055945161727));
#10120=CARTESIAN_POINT('Ctrl Pts',(-0.18279183730445,-0.0800653667767086,
1.05167416449904));
#10121=CARTESIAN_POINT('Ctrl Pts',(-0.0318523576765106,-0.196999355462583,
1.06278887738082));
#10122=CARTESIAN_POINT('Ctrl Pts',(0.148246384444326,-0.133590150240991,
1.07390359026259));
#10123=CARTESIAN_POINT('Ctrl Pts',(0.192632873125826,0.0521142488530221,
1.08501830314437));
#10124=CARTESIAN_POINT('Ctrl Pts',(0.0606734671240232,0.190110623399576,
1.09613301602615));
#10125=CARTESIAN_POINT('Ctrl Pts',(-0.126829505611247,0.15407009848972,
1.10724772890792));
#10126=CARTESIAN_POINT('Ctrl Pts',(-0.198226321197279,-0.0230140028421487,
1.1183624417897));
#10127=CARTESIAN_POINT('Ctrl Pts',(-0.0881567162597448,-0.179029919623856,
1.12947715467147));
#10128=CARTESIAN_POINT('Ctrl Pts',(0.102616014519724,-0.171152774754934,
1.14059186755325));
#10129=CARTESIAN_POINT('Ctrl Pts',(0.199448845033595,-0.00659370586168438,
1.15170658043503));
#10130=CARTESIAN_POINT('Ctrl Pts',(0.113696094746692,0.164001575546019,
1.1628212933168));
#10131=CARTESIAN_POINT('Ctrl Pts',(-0.0761398227834604,0.184461503107637,
1.17393600619858));
#10132=CARTESIAN_POINT('Ctrl Pts',(-0.196273487775402,0.0360560222252062,
1.18505071908035));
#10133=CARTESIAN_POINT('Ctrl Pts',(-0.136728454927659,-0.145356968719496,
1.19616543196213));
#10134=CARTESIAN_POINT('Ctrl Pts',(0.0479847349517988,-0.193702823814809,
1.20728014484391));
#10135=CARTESIAN_POINT('Ctrl Pts',(0.188770266592525,-0.0647232971410789,
1.21839485772568));
#10136=CARTESIAN_POINT('Ctrl Pts',(0.156745929327229,0.123507215908905,
1.22950957060746));
#10137=CARTESIAN_POINT('Ctrl Pts',(-0.0187715755197026,0.198672964176643,
1.24062428348924));
#10138=CARTESIAN_POINT('Ctrl Pts',(-0.177104628793434,0.0919634123016617,
1.25173899637101));
#10139=CARTESIAN_POINT('Ctrl Pts',(-0.173307129216344,-0.09893410789518,
1.26285370925279));
#10140=CARTESIAN_POINT('Ctrl Pts',(-0.0108555003583793,-0.199262331749367,
1.27396842213457));
#10141=CARTESIAN_POINT('Ctrl Pts',(0.161533803683835,-0.117175718515645,
1.28508313501634));
#10142=CARTESIAN_POINT('Ctrl Pts',(0.186046877309155,0.0721794859065759,
1.29619784789812));
#10143=CARTESIAN_POINT('Ctrl Pts',(0.0402432105996758,0.195457930877352,
1.3073125607799));
#10144=CARTESIAN_POINT('Ctrl Pts',(-0.142401130616552,0.139804280125299,
1.31842727366167));
#10145=CARTESIAN_POINT('Ctrl Pts',(-0.194684259984547,-0.0438332939270479,
1.32954198654345));
#10146=CARTESIAN_POINT('Ctrl Pts',(-0.0687435511745859,-0.187343649249534,
1.34065669942522));
#10147=CARTESIAN_POINT('Ctrl Pts',(0.120128488300164,-0.159350133482664,
1.351771412307));
#10148=CARTESIAN_POINT('Ctrl Pts',(0.199028821479448,0.0145205703306567,
1.36288612518877));
#10149=CARTESIAN_POINT('Ctrl Pts',(0.0957280847061954,0.175098408161551,
1.37400083807055));
#10150=CARTESIAN_POINT('Ctrl Pts',(-0.0952069923014279,0.175382289183205,
1.38511555095233));
#10151=CARTESIAN_POINT('Ctrl Pts',(-0.19898476347094,0.0151123343213224,
1.3962302638341));
#10152=CARTESIAN_POINT('Ctrl Pts',(-0.120601797621762,-0.158992217270611,
1.40734497671588));
#10153=CARTESIAN_POINT('Ctrl Pts',(0.0681861658631651,-0.187547235455782,
1.41845968959766));
#10154=CARTESIAN_POINT('Ctrl Pts',(0.194553057445636,-0.0444120094206586,
1.42957440247943));
#10155=CARTESIAN_POINT('Ctrl Pts',(0.142816220303608,0.139380220836447,
1.44068911536121));
#10156=CARTESIAN_POINT('Ctrl Pts',(-0.0396618228229078,0.195576733157576,
1.45180382824298));
#10157=CARTESIAN_POINT('Ctrl Pts',(-0.18583142327823,0.0727323921276658,
1.46291854112476));
#10158=CARTESIAN_POINT('Ctrl Pts',(-0.161881520937861,-0.116694866729734,
1.47403325400654));
#10159=CARTESIAN_POINT('Ctrl Pts',(0.0102629298160299,-0.199293730493,1.48514796688831));
#10160=CARTESIAN_POINT('Ctrl Pts',(0.173012174491582,-0.09944901316715,
1.49626267977009));
#10161=CARTESIAN_POINT('Ctrl Pts',(0.177377306389596,0.0914363708826889,
1.50737739265186));
#10162=CARTESIAN_POINT('Ctrl Pts',(0.0193622625459762,0.198616267036026,
1.51849210553364));
#10163=CARTESIAN_POINT('Ctrl Pts',(-0.156377977710683,0.123972766482573,
1.52960681841542));
#10164=CARTESIAN_POINT('Ctrl Pts',(-0.188961891943262,-0.0641616874423405,
1.54072153129719));
#10165=CARTESIAN_POINT('Ctrl Pts',(-0.0485605137121908,-0.193559280971576,
1.55183624417897));
#10166=CARTESIAN_POINT('Ctrl Pts',(0.136295619815311,-0.145762899125208,
1.56295095706075));
#10167=CARTESIAN_POINT('Ctrl Pts',(0.196379835509003,0.0354722278364698,
1.57406566994252));
#10168=CARTESIAN_POINT('Ctrl Pts',(0.0766879972579736,0.184234279705994,
1.5851803828243));
#10169=CARTESIAN_POINT('Ctrl Pts',(-0.11320792022669,0.164338934949004,
1.59629509570607));
#10170=CARTESIAN_POINT('Ctrl Pts',(-0.199467570164373,-0.00600059954892135,
1.60740980858785));
#10171=CARTESIAN_POINT('Ctrl Pts',(-0.103124497367579,-0.170846881109693,
1.61852452146962));
#10172=CARTESIAN_POINT('Ctrl Pts',(0.0876239666636226,-0.179291269191664,
1.6296392343514));
#10173=CARTESIAN_POINT('Ctrl Pts',(0.198157010832902,-0.0236033429834524,
1.64075394723318));
#10174=CARTESIAN_POINT('Ctrl Pts',(0.127287084698812,0.153692279607998,
1.65186866011496));
#10175=CARTESIAN_POINT('Ctrl Pts',(-0.060107889671358,0.190290200329605,
1.66298337299673));
#10176=CARTESIAN_POINT('Ctrl Pts',(-0.192477055571666,0.0526868277721045,
1.67409808587851));
#10177=CARTESIAN_POINT('Ctrl Pts',(-0.148642970074574,-0.133148737093653,
1.68521279876028));
#10178=CARTESIAN_POINT('Ctrl Pts',(0.0312664234467219,-0.197093200052857,
1.69632751164206));
#10179=CARTESIAN_POINT('Ctrl Pts',(0.182552948364186,-0.0806085590106191,
1.70744222452384));
#10180=CARTESIAN_POINT('Ctrl Pts',(0.166721252575211,0.10966924218749,1.71855693740561));
#10181=CARTESIAN_POINT('Ctrl Pts',(-0.00173552724546146,0.199550261055719,
1.72967165028739));
#10182=CARTESIAN_POINT('Ctrl Pts',(-0.168603517469208,0.106752857756764,
1.74078636316916));
#10183=CARTESIAN_POINT('Ctrl Pts',(-0.181123302984206,-0.0837715217619741,
1.75190107605094));
#10184=CARTESIAN_POINT('Ctrl Pts',(-0.0278336376279517,-0.197607204723465,
1.76301578893272));
#10185=CARTESIAN_POINT('Ctrl Pts',(0.150936350220227,-0.130543237758309,
1.77413050181449));
#10186=CARTESIAN_POINT('Ctrl Pts',(0.191531553630485,0.0560266249752561,
1.78524521469627));
#10187=CARTESIAN_POINT('Ctrl Pts',(0.0567890660382895,0.191306875780052,
1.79635992757805));
#10188=CARTESIAN_POINT('Ctrl Pts',(-0.129941010672249,0.151455117073342,
1.80747464045982));
#10189=CARTESIAN_POINT('Ctrl Pts',(-0.197716500809795,-0.0270463315397067,
1.8185893533416));
#10190=CARTESIAN_POINT('Ctrl Pts',(-0.0844922858441475,-0.180788197554642,
1.82970406622337));
#10191=CARTESIAN_POINT('Ctrl Pts',(0.106080449647855,-0.169027385191674,
1.84081877910515));
#10192=CARTESIAN_POINT('Ctrl Pts',(0.199541765380578,-0.0025303381252174,
1.85193349198693));
#10193=CARTESIAN_POINT('Ctrl Pts',(0.1103324363177,0.166283108698467,1.8630482048687));
#10194=CARTESIAN_POINT('Ctrl Pts',(-0.0798807965924946,0.182872570600334,
1.87416291775048));
#10195=CARTESIAN_POINT('Ctrl Pts',(-0.196967099947332,0.0320512134023539,
1.88527763063225));
#10196=CARTESIAN_POINT('Ctrl Pts',(-0.133739737728071,-0.148111448897957,
1.89639234351403));
#10197=CARTESIAN_POINT('Ctrl Pts',(0.0519197583303703,-0.192685384596604,
1.90750705639581));
#10198=CARTESIAN_POINT('Ctrl Pts',(0.190049276322557,-0.0608653539503196,
1.91862176927758));
#10199=CARTESIAN_POINT('Ctrl Pts',(0.154198055081705,0.126673906355039,
1.92973648215936));
#10200=CARTESIAN_POINT('Ctrl Pts',(-0.0228138805302983,0.198249452956054,
1.94085119504114));
#10201=CARTESIAN_POINT('Ctrl Pts',(-0.178940833698592,0.0883374030492047,
1.95196590792291));
#10202=CARTESIAN_POINT('Ctrl Pts',(-0.17125627898712,-0.10244318254385,
1.96308062080469));
#10203=CARTESIAN_POINT('Ctrl Pts',(-0.00679504723157641,-0.199442087021132,
1.97419533368646));
#10204=CARTESIAN_POINT('Ctrl Pts',(0.163886715132369,-0.113861597324754,
1.98531004656824));
#10205=CARTESIAN_POINT('Ctrl Pts',(0.184538272694043,0.0759535690625106,
1.99642475945002));
#10206=CARTESIAN_POINT('Ctrl Pts',(0.0362541430415187,0.196236989007019,
2.00753947233179));
#10207=CARTESIAN_POINT('Ctrl Pts',(-0.145218866509139,0.136875123934236,
2.01865418521357));
#10208=CARTESIAN_POINT('Ctrl Pts',(-0.193751165973055,-0.0477891664121737,
2.02976889809535));
#10209=CARTESIAN_POINT('Ctrl Pts',(-0.0649138288057709,-0.188704831872211,
2.04088361097712));
#10210=CARTESIAN_POINT('Ctrl Pts',(0.123348917078771,-0.156870530685843,
2.0519983238589));
#10211=CARTESIAN_POINT('Ctrl Pts',(0.19869181295463,0.0185710044814121,
2.06311303674067));
#10212=CARTESIAN_POINT('Ctrl Pts',(0.0921421535575656,0.177011700967353,
2.07422774962245));
#10213=CARTESIAN_POINT('Ctrl Pts',(-0.0987591029588015,0.173406915446888,
2.08534246250422));
#10214=CARTESIAN_POINT('Ctrl Pts',(-0.19925127153347,0.0110566512675373,
2.09645717538601));
#10215=CARTESIAN_POINT('Ctrl Pts',(-0.11733872807775,-0.161415431822329,
2.10757188826778));
#10216=CARTESIAN_POINT('Ctrl Pts',(0.0719916337340498,-0.186119648115988,
2.11868660114956));
#10217=CARTESIAN_POINT('Ctrl Pts',(0.195417205582667,-0.0404405059530035,
2.12980131403133));
#10218=CARTESIAN_POINT('Ctrl Pts',(0.139947963537486,0.142259924811219,
2.14091602691311));
#10219=CARTESIAN_POINT('Ctrl Pts',(-0.043636736562569,0.194728410812529,
2.15203073979488));
#10220=CARTESIAN_POINT('Ctrl Pts',(-0.187274157119832,0.0689326404739108,
2.16314545267666));
#10221=CARTESIAN_POINT('Ctrl Pts',(-0.159471322036838,-0.11996756196921,
2.17426016555844));
#10222=CARTESIAN_POINT('Ctrl Pts',(0.0143196410143589,-0.199043379164193,
2.18537487844021));
#10223=CARTESIAN_POINT('Ctrl Pts',(0.175001683190603,-0.0959047977983527,
2.19648959132199));
#10224=CARTESIAN_POINT('Ctrl Pts',(0.175478307454146,0.0950298925627762,
2.20760430420376));
#10225=CARTESIAN_POINT('Ctrl Pts',(0.0153132111455397,0.198969409553037,
2.21871901708554));
#10226=CARTESIAN_POINT('Ctrl Pts',(-0.15887040383073,0.120762233120711,
2.22983372996731));
#10227=CARTESIAN_POINT('Ctrl Pts',(-0.18761594421292,-0.0679967886034852,
2.2409484428491));
#10228=CARTESIAN_POINT('Ctrl Pts',(-0.0446084462591464,-0.194508147970143,
2.25206315573087));
#10229=CARTESIAN_POINT('Ctrl Pts',(0.139236084597726,-0.142956807308717,
2.26317786861265));
#10230=CARTESIAN_POINT('Ctrl Pts',(0.195616465809081,0.0394642805488386,
2.27429258149442));
#10231=CARTESIAN_POINT('Ctrl Pts',(0.0729203458294538,0.185758068918763,
2.28540729437619));
#10232=CARTESIAN_POINT('Ctrl Pts',(-0.116532134415559,0.161998930407982,
2.29652200725798));
#10233=CARTESIAN_POINT('Ctrl Pts',(-0.199302567461706,-0.0100611425750267,
2.30763672013975));
#10234=CARTESIAN_POINT('Ctrl Pts',(-0.0996263244312855,-0.172912821785659,
2.31875143302153));
#10235=CARTESIAN_POINT('Ctrl Pts',(0.0912624073210796,-0.177467372195954,
2.3298661459033));
#10236=CARTESIAN_POINT('Ctrl Pts',(0.198586828476941,-0.0195668459503173,
2.34098085878508));
#10237=CARTESIAN_POINT('Ctrl Pts',(0.1241491979793,0.156260526666046,2.35209557166686));
#10238=CARTESIAN_POINT('Ctrl Pts',(-0.0640063699759371,0.189011759840439,
2.36321028454863));
#10239=CARTESIAN_POINT('Ctrl Pts',(-0.19344240946393,0.0487841174099963,
2.37432499743041));
#10240=CARTESIAN_POINT('Ctrl Pts',(-0.146031591195115,-0.136202617223352,
2.38543971031218));
#10241=CARTESIAN_POINT('Ctrl Pts',(0.0355430520271422,-0.196307960177277,
2.39655442319396));
#10242=CARTESIAN_POINT('Ctrl Pts',(0.134174928543208,-0.11685088838635,
2.40396423178181));
#10243=CARTESIAN_POINT('Ctrl Pts',(0.155803480964729,-0.0650382177163376,
2.40766913607574));
#10244=CARTESIAN_POINT('Ctrl Pts',(-0.0802959149489801,0.163459616787401,
-0.00766913607573617));
#10245=CARTESIAN_POINT('Ctrl Pts',(-0.134654644548669,0.136757095305608,
-0.00396423178181077));
#10246=CARTESIAN_POINT('Ctrl Pts',(-0.213700326361063,0.0253255878308996,
0.00344557680604003));
#10247=CARTESIAN_POINT('Ctrl Pts',(-0.13701639887793,-0.166206038290849,
0.0145602896878162));
#10248=CARTESIAN_POINT('Ctrl Pts',(0.0652772298818827,-0.205055569170507,
0.0256750025695924));
#10249=CARTESIAN_POINT('Ctrl Pts',(0.207721328204669,-0.0564519446507592,
0.0367897154513685));
#10250=CARTESIAN_POINT('Ctrl Pts',(0.160054624079751,0.143968508655411,
0.0479044283331447));
#10251=CARTESIAN_POINT('Ctrl Pts',(-0.0341593076908942,0.212520602038122,
0.059019141214921));
#10252=CARTESIAN_POINT('Ctrl Pts',(-0.197088880551355,0.0865585450530169,
0.070133854096697));
#10253=CARTESIAN_POINT('Ctrl Pts',(-0.179600240536358,-0.118663552218321,
0.0812485669784734));
#10254=CARTESIAN_POINT('Ctrl Pts',(0.00230720808327818,-0.21524452755814,
0.0923632798602493));
#10255=CARTESIAN_POINT('Ctrl Pts',(0.182100604837577,-0.114785269045894,
0.103477992742026));
#10256=CARTESIAN_POINT('Ctrl Pts',(0.195190886559782,0.0907571411395873,
0.114592705623802));
#10257=CARTESIAN_POINT('Ctrl Pts',(0.0295930088791093,0.213214340866297,
0.125707418505578));
#10258=CARTESIAN_POINT('Ctrl Pts',(-0.163095530528085,0.140485128302662,
0.136822131387354));
#10259=CARTESIAN_POINT('Ctrl Pts',(-0.206478301943304,-0.0608517115477897,
0.14793684426913));
#10260=CARTESIAN_POINT('Ctrl Pts',(-0.0608402945339887,-0.206481589356881,
0.159051557150907));
#10261=CARTESIAN_POINT('Ctrl Pts',(0.140493961443918,-0.163087872133576,
0.170166270032683));
#10262=CARTESIAN_POINT('Ctrl Pts',(0.213212946141786,0.0296048096800013,
0.181280982914459));
#10263=CARTESIAN_POINT('Ctrl Pts',(0.0907459831492815,0.195195716196652,
0.192395695796235));
#10264=CARTESIAN_POINT('Ctrl Pts',(-0.114794445947616,0.182094588495495,
0.203510408678011));
#10265=CARTESIAN_POINT('Ctrl Pts',(-0.215246224534229,0.00229483705933785,
0.214625121559788));
#10266=CARTESIAN_POINT('Ctrl Pts',(-0.11865069889232,-0.179605719854349,
0.225739834441564));
#10267=CARTESIAN_POINT('Ctrl Pts',(0.0865636888739609,-0.197086100859037,
0.23685454732334));
#10268=CARTESIAN_POINT('Ctrl Pts',(0.212533289250105,-0.0341438755340746,
0.247969260205116));
#10269=CARTESIAN_POINT('Ctrl Pts',(0.143939145235083,0.160055383186509,
0.259083973086892));
#10270=CARTESIAN_POINT('Ctrl Pts',(-0.0564241870326071,0.207731832896163,
0.270198685968668));
#10271=CARTESIAN_POINT('Ctrl Pts',(-0.205133958980916,0.0652400347468957,
0.281313398850444));
#10272=CARTESIAN_POINT('Ctrl Pts',(-0.16605370866557,-0.136975797472738,
0.292428111732221));
#10273=CARTESIAN_POINT('Ctrl Pts',(0.025040522137507,-0.213797042811354,
0.303542824613997));
#10274=CARTESIAN_POINT('Ctrl Pts',(0.193211389933017,-0.0948976399103106,
0.314657537495773));
#10275=CARTESIAN_POINT('Ctrl Pts',(0.184506759435748,0.110875871957748,
0.325772250377549));
#10276=CARTESIAN_POINT('Ctrl Pts',(0.00689529056070297,0.215147991459819,
0.336886963259325));
#10277=CARTESIAN_POINT('Ctrl Pts',(-0.177028476747947,0.122462735886679,
0.348001676141102));
#10278=CARTESIAN_POINT('Ctrl Pts',(-0.198891404646875,-0.082331114520091,
0.359116389022878));
#10279=CARTESIAN_POINT('Ctrl Pts',(-0.0386790609264599,-0.211754890159689,
0.370231101904654));
#10280=CARTESIAN_POINT('Ctrl Pts',(0.156942055419018,-0.14732750761979,
0.38134581478643));
#10281=CARTESIAN_POINT('Ctrl Pts',(0.208890460418672,0.0519709419453341,
0.392460527668207));
#10282=CARTESIAN_POINT('Ctrl Pts',(0.0696099513935343,0.203692557369242,
0.403575240549982));
#10283=CARTESIAN_POINT('Ctrl Pts',(-0.133395034965965,0.168943682649122,
0.414689953431759));
#10284=CARTESIAN_POINT('Ctrl Pts',(-0.214283445864218,-0.0204648012249496,
0.425804666313535));
#10285=CARTESIAN_POINT('Ctrl Pts',(-0.0990059305445593,-0.191138768902671,
0.436919379195311));
#10286=CARTESIAN_POINT('Ctrl Pts',(0.106906631210968,-0.186834620624077,
0.448034092077087));
#10287=CARTESIAN_POINT('Ctrl Pts',(0.214951444733503,-0.0114925918574203,
0.459148804958863));
#10288=CARTESIAN_POINT('Ctrl Pts',(0.126218812019027,0.174370337939476,
0.47026351784064));
#10289=CARTESIAN_POINT('Ctrl Pts',(-0.0780609179804491,0.200605823306979,
0.481378230722416));
#10290=CARTESIAN_POINT('Ctrl Pts',(-0.210879727537387,0.0431965713266546,
0.492492943604192));
#10291=CARTESIAN_POINT('Ctrl Pts',(-0.150648547133053,-0.153757011246062,
0.503607656485968));
#10292=CARTESIAN_POINT('Ctrl Pts',(0.0474939481773568,-0.209953633326855,
0.514722369367745));
#10293=CARTESIAN_POINT('Ctrl Pts',(0.202158076335407,-0.0739480590211045,
0.52583708224952));
#10294=CARTESIAN_POINT('Ctrl Pts',(0.171756456055305,0.129753316196324,
0.536951795131297));
#10295=CARTESIAN_POINT('Ctrl Pts',(-0.0158797287060216,0.214671929876368,
0.548066508013073));
#10296=CARTESIAN_POINT('Ctrl Pts',(-0.188978805026037,0.103068979385421,
0.55918122089485));
#10297=CARTESIAN_POINT('Ctrl Pts',(-0.189077105789276,-0.102888538365418,
0.570295933776625));
#10298=CARTESIAN_POINT('Ctrl Pts',(-0.0160846414951921,-0.214656673710818,
0.581410646658403));
#10299=CARTESIAN_POINT('Ctrl Pts',(0.171632518792379,-0.129917211152352,
0.592525359540176));
#10300=CARTESIAN_POINT('Ctrl Pts',(0.202228573050342,0.073755050692434,
0.603640072421955));
#10301=CARTESIAN_POINT('Ctrl Pts',(0.0476943426045303,0.20990820123126,
0.614754785303729));
#10302=CARTESIAN_POINT('Ctrl Pts',(-0.150501706208254,0.153900746226344,
0.625869498185507));
#10303=CARTESIAN_POINT('Ctrl Pts',(-0.210920865739414,-0.0429952515559257,
0.636984211067282));
#10304=CARTESIAN_POINT('Ctrl Pts',(-0.0782523753142842,-0.200531217066804,
0.64809892394906));
#10305=CARTESIAN_POINT('Ctrl Pts',(0.126052305299824,-0.17449074356315,
0.659213636830834));
#10306=CARTESIAN_POINT('Ctrl Pts',(0.214962317318242,0.011287399779957,
0.670328349712612));
#10307=CARTESIAN_POINT('Ctrl Pts',(0.107084929784557,0.186732485319662,
0.681443062594386));
#10308=CARTESIAN_POINT('Ctrl Pts',(-0.0988234295325455,0.191233190205171,
0.692557775476164));
#10309=CARTESIAN_POINT('Ctrl Pts',(-0.214263813089322,0.0206693410888018,
0.703672488357938));
#10310=CARTESIAN_POINT('Ctrl Pts',(-0.133556243265307,-0.168816270381381,
0.714787201239717));
#10311=CARTESIAN_POINT('Ctrl Pts',(0.069415480267185,-0.203758912344705,
0.72590191412149));
#10312=CARTESIAN_POINT('Ctrl Pts',(0.208840755190191,-0.0521703194566796,
0.73701662700327));
#10313=CARTESIAN_POINT('Ctrl Pts',(0.15708261877356,0.147177627851049,0.748131339885043));
#10314=CARTESIAN_POINT('Ctrl Pts',(-0.0384769078072813,0.211791715669455,
0.759246052766822));
#10315=CARTESIAN_POINT('Ctrl Pts',(-0.198812722973664,0.0825209333709834,
0.770360765648595));
#10316=CARTESIAN_POINT('Ctrl Pts',(-0.177145295711566,-0.122293693491868,
0.781475478530374));
#10317=CARTESIAN_POINT('Ctrl Pts',(0.0066899129592092,-0.215154475494282,
0.792590191412148));
#10318=CARTESIAN_POINT('Ctrl Pts',(0.184400836262686,-0.111051946611679,
0.803704904293927));
#10319=CARTESIAN_POINT('Ctrl Pts',(0.193301888626575,0.094713162306093,
0.8148196171757));
#10320=CARTESIAN_POINT('Ctrl Pts',(0.0252445956121046,0.213773042390762,
0.825934330057479));
#10321=CARTESIAN_POINT('Ctrl Pts',(-0.16592287962047,0.137134245464334,
0.837049042939253));
#10322=CARTESIAN_POINT('Ctrl Pts',(-0.205196141885616,-0.0650441897165239,
0.848163755821031));
#10323=CARTESIAN_POINT('Ctrl Pts',(-0.0566224565389448,-0.207677877194747,
0.859278468702805));
#10324=CARTESIAN_POINT('Ctrl Pts',(0.143786295146609,-0.160192710784959,
0.870393181584584));
#10325=CARTESIAN_POINT('Ctrl Pts',(0.212565785173049,0.0339409816355746,
0.881507894466357));
#10326=CARTESIAN_POINT('Ctrl Pts',(0.0867517826292189,0.197003379339731,
0.892622607348135));
#10327=CARTESIAN_POINT('Ctrl Pts',(-0.118479198309198,0.179718899475349,
0.903737320229911));
#10328=CARTESIAN_POINT('Ctrl Pts',(-0.21524831659581,-0.0020893691131805,
0.914852033111686));
#10329=CARTESIAN_POINT('Ctrl Pts',(-0.114968217097204,-0.181984923326388,
0.925966745993464));
#10330=CARTESIAN_POINT('Ctrl Pts',(0.0905596149154041,-0.195282255740236,
0.937081458875238));
#10331=CARTESIAN_POINT('Ctrl Pts',(0.21318458587791,-0.0298083143549778,
0.948196171757016));
#10332=CARTESIAN_POINT('Ctrl Pts',(0.140649582744129,0.162953668674638,
0.959310884638791));
#10333=CARTESIAN_POINT('Ctrl Pts',(-0.0606431765471154,0.206539604916095,
0.970425597520568));
#10334=CARTESIAN_POINT('Ctrl Pts',(-0.206420098634119,0.061048719400998,
0.981540310402345));
#10335=CARTESIAN_POINT('Ctrl Pts',(-0.163229601071661,-0.140329257799675,
0.99265502328412));
#10336=CARTESIAN_POINT('Ctrl Pts',(0.0293895457794294,-0.213242720531089,
1.0037697361659));
#10337=CARTESIAN_POINT('Ctrl Pts',(0.195104012963389,-0.0909429897584348,
1.01488444904767));
#10338=CARTESIAN_POINT('Ctrl Pts',(0.182210378819503,0.114610562825048,
1.02599916192945));
#10339=CARTESIAN_POINT('Ctrl Pts',(0.00251212949178726,0.215243797741161,
1.03711387481123));
#10340=CARTESIAN_POINT('Ctrl Pts',(-0.179485850487301,0.118831951660617,
1.048228587693));
#10341=CARTESIAN_POINT('Ctrl Pts',(-0.197173386596812,-0.0863646853671406,
1.05934330057478));
#10342=CARTESIAN_POINT('Ctrl Pts',(-0.034358411878696,-0.212498712452088,
1.07045801345655));
#10343=CARTESIAN_POINT('Ctrl Pts',(0.159909994355694,-0.144100648734776,
1.08157272633833));
#10344=CARTESIAN_POINT('Ctrl Pts',(0.207788687526742,0.0562144518476816,
1.0926874392201));
#10345=CARTESIAN_POINT('Ctrl Pts',(0.0654470854160082,0.205067994263295,
1.10380215210188));
#10346=CARTESIAN_POINT('Ctrl Pts',(-0.136808095539401,0.166191901895078,
1.11491686498366));
#10347=CARTESIAN_POINT('Ctrl Pts',(-0.213822212410925,-0.0248246800647778,
1.12603157786543));
#10348=CARTESIAN_POINT('Ctrl Pts',(-0.095092639542961,-0.193115491779851,
1.13714629074721));
#10349=CARTESIAN_POINT('Ctrl Pts',(0.110689554852622,-0.184618595236638,
1.14826100362899));
#10350=CARTESIAN_POINT('Ctrl Pts',(0.215140920995271,-0.00711248015306863,
1.15937571651076));
#10351=CARTESIAN_POINT('Ctrl Pts',(0.12264138472824,0.176904759722742,1.17049042939254));
#10352=CARTESIAN_POINT('Ctrl Pts',(-0.0821302905779772,0.198974417024396,
1.18160514227431));
#10353=CARTESIAN_POINT('Ctrl Pts',(-0.211715735530289,0.0388928089688832,
1.19271985515609));
#10354=CARTESIAN_POINT('Ctrl Pts',(-0.147485866435784,-0.156793247502267,
1.20383456803787));
#10355=CARTESIAN_POINT('Ctrl Pts',(0.0517600393700242,-0.20894281893627,
1.21494928091964));
#10356=CARTESIAN_POINT('Ctrl Pts',(0.203622181940428,-0.0698155447048894,
1.22606399380142));
#10357=CARTESIAN_POINT('Ctrl Pts',(0.169078259601047,0.133224417397496,
1.2371787066832));
#10358=CARTESIAN_POINT('Ctrl Pts',(-0.0202484704544748,0.214303996007717,
1.24829341956497));
#10359=CARTESIAN_POINT('Ctrl Pts',(-0.191038724464548,0.0991988357571789,
1.25940813244675));
#10360=CARTESIAN_POINT('Ctrl Pts',(-0.186942448267222,-0.106717966137282,
1.27052284532852));
#10361=CARTESIAN_POINT('Ctrl Pts',(-0.0117095806925935,-0.214939733368739,
1.2816375582103));
#10362=CARTESIAN_POINT('Ctrl Pts',(0.174242830488972,-0.126394775540022,
1.29275227109208));
#10363=CARTESIAN_POINT('Ctrl Pts',(0.200684524023408,0.077858365498637,
1.30386698397385));
#10364=CARTESIAN_POINT('Ctrl Pts',(0.0434094335856485,0.210836012901957,
1.31498169685563));
#10365=CARTESIAN_POINT('Ctrl Pts',(-0.153604852344235,0.150803688936734,
1.32609640973741));
#10366=CARTESIAN_POINT('Ctrl Pts',(-0.210001471752333,-0.0472819746042342,
1.33721112261918));
#10367=CARTESIAN_POINT('Ctrl Pts',(-0.0741521010547544,-0.202083322344489,
1.34832583550096));
#10368=CARTESIAN_POINT('Ctrl Pts',(0.129579860972944,-0.171887355238405,
1.35944054838274));
#10369=CARTESIAN_POINT('Ctrl Pts',(0.214687851165442,0.0156630080950769,
1.37055526126451));
#10370=CARTESIAN_POINT('Ctrl Pts',(0.10325970203204,0.188874660017895,1.38166997414629));
#10371=CARTESIAN_POINT('Ctrl Pts',(-0.102697611537783,0.189180876002454,
1.39278468702806));
#10372=CARTESIAN_POINT('Ctrl Pts',(-0.214640326796344,0.0163013304174776,
1.40389939990984));
#10373=CARTESIAN_POINT('Ctrl Pts',(-0.130090408945011,-0.17150127918223,
1.41501411279161));
#10374=CARTESIAN_POINT('Ctrl Pts',(0.0735508622296984,-0.202302926142676,
1.42612882567339));
#10375=CARTESIAN_POINT('Ctrl Pts',(0.209859946565495,-0.0479062218104144,
1.43724353855517));
#10376=CARTESIAN_POINT('Ctrl Pts',(0.154052600124136,0.150346265851913,
1.44835825143694));
#10377=CARTESIAN_POINT('Ctrl Pts',(-0.0427823038485639,0.21096416221252,
1.45947296431872));
#10378=CARTESIAN_POINT('Ctrl Pts',(-0.20045211867337,0.0784547728310926,
1.4705876772005));
#10379=CARTESIAN_POINT('Ctrl Pts',(-0.174617905161696,-0.125876091683695,
1.48170239008227));
#10380=CARTESIAN_POINT('Ctrl Pts',(0.0110703883612833,-0.214973602477494,
1.49281710296405));
#10381=CARTESIAN_POINT('Ctrl Pts',(0.186624287331642,-0.107273382712479,
1.50393181584582));
#10382=CARTESIAN_POINT('Ctrl Pts',(0.191332855569507,0.0986303281969572,
1.5150465287276));
#10383=CARTESIAN_POINT('Ctrl Pts',(0.0208856310799447,0.214242838095031,
1.52616124160938));
#10384=CARTESIAN_POINT('Ctrl Pts',(-0.168681358582888,0.133726596185098,
1.53727595449115));
#10385=CARTESIAN_POINT('Ctrl Pts',(-0.203828883836526,-0.0692097491295648,
1.54839066737293));
#10386=CARTESIAN_POINT('Ctrl Pts',(-0.0523811187890492,-0.208787982544563,
1.55950538025471));
#10387=CARTESIAN_POINT('Ctrl Pts',(0.14701897707028,-0.157231115374246,
1.57062009313648));
#10388=CARTESIAN_POINT('Ctrl Pts',(0.211830450405416,0.0382630832743479,
1.58173480601826));
#10389=CARTESIAN_POINT('Ctrl Pts',(0.082721593883301,0.198729316322549,
1.59284951890003));
#10390=CARTESIAN_POINT('Ctrl Pts',(-0.122114802005634,0.177268661617743,
1.60396423178181));
#10391=CARTESIAN_POINT('Ctrl Pts',(-0.215161119366841,-0.0064727098984307,
1.61507894466359));
#10392=CARTESIAN_POINT('Ctrl Pts',(-0.11123804370538,-0.184288634736983,
1.62619365754536));
#10393=CARTESIAN_POINT('Ctrl Pts',(0.0945179747022152,-0.193397403598943,
1.63730837042714));
#10394=CARTESIAN_POINT('Ctrl Pts',(0.213747448901395,-0.0254603878361445,
1.64842308330892));
#10395=CARTESIAN_POINT('Ctrl Pts',(0.137301675666721,0.165784357282983,
1.65953779619069));
#10396=CARTESIAN_POINT('Ctrl Pts',(-0.0648370099150017,0.205261699802723,
1.67065250907247));
#10397=CARTESIAN_POINT('Ctrl Pts',(-0.207620610684265,0.0568320796708535,
1.68176722195424));
#10398=CARTESIAN_POINT('Ctrl Pts',(-0.160337782231475,-0.143624506438537,
1.69288193483602));
#10399=CARTESIAN_POINT('Ctrl Pts',(0.0337263779864135,-0.212599940471626,
1.7039966477178));
#10400=CARTESIAN_POINT('Ctrl Pts',(0.196915702544469,-0.0869506144431389,
1.71511136059957));
#10401=CARTESIAN_POINT('Ctrl Pts',(0.179838413315825,0.118297710699184,
1.72622607348135));
#10402=CARTESIAN_POINT('Ctrl Pts',(-0.00187207366349427,0.21525031614569,
1.73734078636313));
#10403=CARTESIAN_POINT('Ctrl Pts',(-0.181868769534656,0.115151873317682,
1.7484554992449));
#10404=CARTESIAN_POINT('Ctrl Pts',(-0.195373576674077,-0.0903624302362419,
1.75957021212668));
#10405=CARTESIAN_POINT('Ctrl Pts',(-0.0300235102034143,-0.213154385588678,
1.77068492500845));
#10406=CARTESIAN_POINT('Ctrl Pts',(0.162811599097379,-0.140814013720139,
1.78179963789023));
#10407=CARTESIAN_POINT('Ctrl Pts',(0.206600719301116,0.0604346427546558,
1.792914350772));
#10408=CARTESIAN_POINT('Ctrl Pts',(0.0612570705429762,0.206358364427309,
1.80402906365378));
#10409=CARTESIAN_POINT('Ctrl Pts',(-0.140164405095331,0.163371181072101,
1.81514377653556));
#10410=CARTESIAN_POINT('Ctrl Pts',(-0.213272280784662,-0.0291742610794093,
1.82625848941733));
#10411=CARTESIAN_POINT('Ctrl Pts',(-0.0911399020156923,-0.195012106088805,
1.83737320229911));
#10412=CARTESIAN_POINT('Ctrl Pts',(0.114426562023903,-0.182325985981184,
1.84848791518088));
#10413=CARTESIAN_POINT('Ctrl Pts',(0.215241152054647,-0.00272941803496647,
1.85960262806266));
#10414=CARTESIAN_POINT('Ctrl Pts',(0.119013083084253,0.179365797507223,
1.87071734094444));
#10415=CARTESIAN_POINT('Ctrl Pts',(-0.0861655937182851,0.197260471762076,
1.88183205382621));
#10416=CARTESIAN_POINT('Ctrl Pts',(-0.212463919163327,0.034572913015546,
1.89294676670799));
#10417=CARTESIAN_POINT('Ctrl Pts',(-0.144262005345963,-0.159764442458836,
1.90406147958977));
#10418=CARTESIAN_POINT('Ctrl Pts',(0.056004659355972,-0.207845330452822,
1.91517619247154));
#10419=CARTESIAN_POINT('Ctrl Pts',(0.205001820570246,-0.0656540693598324,
1.92629090535332));
#10420=CARTESIAN_POINT('Ctrl Pts',(0.166329925752987,0.136640254169945,
1.9374056182351));
#10421=CARTESIAN_POINT('Ctrl Pts',(-0.0246088126904845,0.213847164111628,
1.94852033111687));
#10422=CARTESIAN_POINT('Ctrl Pts',(-0.193019396823745,0.0952875422624504,
1.95963504399865));
#10423=CARTESIAN_POINT('Ctrl Pts',(-0.184730242891633,-0.110503124941429,
1.97074975688042));
#10424=CARTESIAN_POINT('Ctrl Pts',(-0.0073296624974724,-0.215133631281334,
1.9818644697622));
#10425=CARTESIAN_POINT('Ctrl Pts',(0.176780862413764,-0.122819908585148,
1.99297918264398));
#10426=CARTESIAN_POINT('Ctrl Pts',(0.199057226626634,0.0819293829364356,
2.00409389552575));
#10427=CARTESIAN_POINT('Ctrl Pts',(0.0391065173755809,0.211676365141135,
2.01520860840753));
#10428=CARTESIAN_POINT('Ctrl Pts',(-0.156644279797176,0.147644074948605,
2.02632332128931));
#10429=CARTESIAN_POINT('Ctrl Pts',(-0.208994964519996,-0.0515490840459884,
2.03743803417108));
#10430=CARTESIAN_POINT('Ctrl Pts',(-0.0700210668667938,-0.20355159899977,
2.04855274705286));
#10431=CARTESIAN_POINT('Ctrl Pts',(0.133053664059207,-0.16921266424523,
2.05966745993463));
#10432=CARTESIAN_POINT('Ctrl Pts',(0.214324327754712,0.0200321190492036,
2.07078217281641));
#10433=CARTESIAN_POINT('Ctrl Pts',(0.0993916398739864,0.190938485337639,
2.08189688569819));
#10434=CARTESIAN_POINT('Ctrl Pts',(-0.106529192303145,0.18705008539863,
2.09301159857996));
#10435=CARTESIAN_POINT('Ctrl Pts',(-0.214927802966064,0.0119265575913465,
2.10412631146174));
#10436=CARTESIAN_POINT('Ctrl Pts',(-0.126570610237467,-0.174115145461265,
2.11524102434351));
#10437=CARTESIAN_POINT('Ctrl Pts',(0.0776557336438302,-0.200763020233305,
2.12635573722529));
#10438=CARTESIAN_POINT('Ctrl Pts',(0.210792083455263,-0.0436222515842479,
2.13747045010707));
#10439=CARTESIAN_POINT('Ctrl Pts',(0.150958676956968,0.153452536862016,
2.14858516298884));
#10440=CARTESIAN_POINT('Ctrl Pts',(-0.0470699526573771,0.210049096243681,
2.15969987587062));
#10441=CARTESIAN_POINT('Ctrl Pts',(-0.202008362768847,0.0743560673700281,
2.17081458875239));
#10442=CARTESIAN_POINT('Ctrl Pts',(-0.172018078568263,-0.129406273409436,
2.18192930163417));
#10443=CARTESIAN_POINT('Ctrl Pts',(0.0154462702234889,-0.214703554208009,
2.19304401451595));
#10444=CARTESIAN_POINT('Ctrl Pts',(0.188770324997408,-0.103450318414863,
2.20415872739772));
#10445=CARTESIAN_POINT('Ctrl Pts',(0.18928444872176,0.102506578088203,2.2152734402795));
#10446=CARTESIAN_POINT('Ctrl Pts',(0.0165180116670554,0.214623764875225,
2.22638815316127));
#10447=CARTESIAN_POINT('Ctrl Pts',(-0.171369881802411,0.130263467059228,
2.23750286604305));
#10448=CARTESIAN_POINT('Ctrl Pts',(-0.202377040712198,-0.073346585298156,
2.24861757892483));
#10449=CARTESIAN_POINT('Ctrl Pts',(-0.0481181137486331,-0.209811503738378,
2.2597322918066));
#10450=CARTESIAN_POINT('Ctrl Pts',(0.150190789378024,-0.154204248120663,
2.27084700468838));
#10451=CARTESIAN_POINT('Ctrl Pts',(0.211007020917653,0.0425692195021916,
2.28196171757016));
#10452=CARTESIAN_POINT('Ctrl Pts',(0.0786575142031988,0.200372992998553,
2.29307643045193));
#10453=CARTESIAN_POINT('Ctrl Pts',(-0.12570055604727,0.174744552079762,
2.30419114333371));
#10454=CARTESIAN_POINT('Ctrl Pts',(-0.214983134714123,-0.0108527250658792,
2.31530585621548));
#10455=CARTESIAN_POINT('Ctrl Pts',(-0.107464644329775,-0.186517117833358,
2.32642056909726));
#10456=CARTESIAN_POINT('Ctrl Pts',(0.0984426776700368,-0.191430007501004,
2.33753528197904));
#10457=CARTESIAN_POINT('Ctrl Pts',(0.214211083392649,-0.0211063105329791,
2.34864999486081));
#10458=CARTESIAN_POINT('Ctrl Pts',(0.133916908817353,0.168554666819339,
2.35976470774259));
#10459=CARTESIAN_POINT('Ctrl Pts',(-0.0690422117203459,0.203882675200046,
2.37087942062436));
#10460=CARTESIAN_POINT('Ctrl Pts',(-0.208661915914351,0.0526223149989132,
2.38199413350615));
#10461=CARTESIAN_POINT('Ctrl Pts',(-0.157520947382922,-0.146918657295124,
2.39310884638792));
#10462=CARTESIAN_POINT('Ctrl Pts',(0.0383394797137831,-0.211752920124096,
2.4042235592697));
#10463=CARTESIAN_POINT('Ctrl Pts',(0.144731435754359,-0.126044388686833,
2.41163336785755));
#10464=CARTESIAN_POINT('Ctrl Pts',(0.168061662043594,-0.0701552423481134,
2.41533827215147));
#10465=CARTESIAN_POINT('Ctrl Pts',(-0.0861525859670425,0.175382131162759,
-6.38378239159465E-16));
#10466=CARTESIAN_POINT('Ctrl Pts',(-0.14447616479259,0.146731965348487,
0.00370490429392476));
#10467=CARTESIAN_POINT('Ctrl Pts',(-0.22928732737779,0.0271728005609432,
0.0111147128817755));
#10468=CARTESIAN_POINT('Ctrl Pts',(-0.147010182158398,-0.178328872785022,
0.0222294257635518));
#10469=CARTESIAN_POINT('Ctrl Pts',(0.0700384591502911,-0.220012033765444,
0.0333441386453279));
#10470=CARTESIAN_POINT('Ctrl Pts',(0.222872229511445,-0.0605694700361912,
0.0444588515271041));
#10471=CARTESIAN_POINT('Ctrl Pts',(0.171728783079617,0.154469369037803,
0.0555735644088802));
#10472=CARTESIAN_POINT('Ctrl Pts',(-0.0366508395138724,0.228021555623221,
0.0666882772906566));
#10473=CARTESIAN_POINT('Ctrl Pts',(-0.211464266091708,0.0928720034960677,
0.0778029901724325));
#10474=CARTESIAN_POINT('Ctrl Pts',(-0.192700029289671,-0.127318704695491,
0.0889177030542089));
#10475=CARTESIAN_POINT('Ctrl Pts',(0.00247549259342858,-0.230944160436682,
0.100032415935985));
#10476=CARTESIAN_POINT('Ctrl Pts',(0.195382766643706,-0.123157545007232,
0.111147128817761));
#10477=CARTESIAN_POINT('Ctrl Pts',(0.209427835089857,0.0973768392715804,
0.122261841699537));
#10478=CARTESIAN_POINT('Ctrl Pts',(0.0317514812939175,0.228765894785071,
0.133376554581313));
#10479=CARTESIAN_POINT('Ctrl Pts',(-0.174991488964152,0.150731915825055,
0.14449126746309));
#10480=CARTESIAN_POINT('Ctrl Pts',(-0.221538538664161,-0.0652901497379268,
0.155605980344866));
#10481=CARTESIAN_POINT('Ctrl Pts',(-0.0652778999832015,-0.221542065857059,
0.166720693226642));
#10482=CARTESIAN_POINT('Ctrl Pts',(0.150741393243207,-0.174983271977123,
0.177835406108418));
#10483=CARTESIAN_POINT('Ctrl Pts',(0.228764398331316,0.0317641428286243,
0.188950118990194));
#10484=CARTESIAN_POINT('Ctrl Pts',(0.0973648674331599,0.209433016993645,
0.200064831871971));
#10485=CARTESIAN_POINT('Ctrl Pts',(-0.123167391259255,0.195376311478096,
0.211179544753747));
#10486=CARTESIAN_POINT('Ctrl Pts',(-0.230945981187819,0.00246221924440694,
0.222294257635523));
#10487=CARTESIAN_POINT('Ctrl Pts',(-0.127304913865976,-0.192705908261409,
0.233408970517299));
#10488=CARTESIAN_POINT('Ctrl Pts',(0.0928775225000782,-0.211461283652542,
0.244523683399076));
#10489=CARTESIAN_POINT('Ctrl Pts',(0.228035168222589,-0.0366342817572481,
0.255638396280851));
#10490=CARTESIAN_POINT('Ctrl Pts',(0.15443786389092,0.171729597554559,0.266753109162628));
#10491=CARTESIAN_POINT('Ctrl Pts',(-0.0605396878164478,0.222883500400348,
0.277867822044404));
#10492=CARTESIAN_POINT('Ctrl Pts',(-0.220096141218292,0.0699985510545042,
0.28898253492618));
#10493=CARTESIAN_POINT('Ctrl Pts',(-0.178165432451279,-0.146966619343865,
0.300097247807956));
#10494=CARTESIAN_POINT('Ctrl Pts',(0.0268669425771186,-0.229391098189834,
0.311211960689733));
#10495=CARTESIAN_POINT('Ctrl Pts',(0.207303956765325,-0.101819340194788,
0.322326673571508));
#10496=CARTESIAN_POINT('Ctrl Pts',(0.197964422771547,0.118963001998048,
0.333441386453285));
#10497=CARTESIAN_POINT('Ctrl Pts',(0.00739822334891944,0.230840583131227,
0.344556099335061));
#10498=CARTESIAN_POINT('Ctrl Pts',(-0.189940684670355,0.131394995473175,
0.355670812216837));
#10499=CARTESIAN_POINT('Ctrl Pts',(-0.213398263757659,-0.0883362301302812,
0.366785525098613));
#10500=CARTESIAN_POINT('Ctrl Pts',(-0.0415002571887781,-0.227199993798133,
0.37790023798039));
#10501=CARTESIAN_POINT('Ctrl Pts',(0.168389188041786,-0.158073368658771,
0.389014950862165));
#10502=CARTESIAN_POINT('Ctrl Pts',(0.224126636583554,0.0557616293005522,
0.400129663743942));
#10503=CARTESIAN_POINT('Ctrl Pts',(0.074687203270592,0.218549605801867,
0.411244376625718));
#10504=CARTESIAN_POINT('Ctrl Pts',(-0.143124681059852,0.181266197069486,
0.422359089507494));
#10505=CARTESIAN_POINT('Ctrl Pts',(-0.22991297879675,-0.0219574750216296,
0.433473802389271));
#10506=CARTESIAN_POINT('Ctrl Pts',(-0.106227283765387,-0.205080161674287,
0.444588515271047));
#10507=CARTESIAN_POINT('Ctrl Pts',(0.114704250417995,-0.200462074878434,
0.455703228152823));
#10508=CARTESIAN_POINT('Ctrl Pts',(0.230629700563337,-0.0123308453314138,
0.466817941034599));
#10509=CARTESIAN_POINT('Ctrl Pts',(0.135425034511855,0.187088664958583,
0.477932653916375));
#10510=CARTESIAN_POINT('Ctrl Pts',(-0.0837545714654364,0.215237729701748,
0.489047366798152));
#10511=CARTESIAN_POINT('Ctrl Pts',(-0.226260998045971,0.0463472684390648,
0.500162079679927));
#10512=CARTESIAN_POINT('Ctrl Pts',(-0.161636640119692,-0.164971831229877,
0.511276792561705));
#10513=CARTESIAN_POINT('Ctrl Pts',(0.0509580899086091,-0.225267355827221,
0.522391505443479));
#10514=CARTESIAN_POINT('Ctrl Pts',(0.216903201881242,-0.0793417263625324,
0.533506218325257));
#10515=CARTESIAN_POINT('Ctrl Pts',(0.184284130208874,0.139217340448956,
0.544620931207032));
#10516=CARTESIAN_POINT('Ctrl Pts',(-0.0170379737667647,0.230329798285947,
0.555735644088809));
#10517=CARTESIAN_POINT('Ctrl Pts',(-0.202762653072689,0.110586685669867,
0.566850356970584));
#10518=CARTESIAN_POINT('Ctrl Pts',(-0.202868123755235,-0.110393083535847,
0.577965069852361));
#10519=CARTESIAN_POINT('Ctrl Pts',(-0.0172578326063502,-0.230313429357155,
0.589079782734137));
#10520=CARTESIAN_POINT('Ctrl Pts',(0.18415115313644,-0.139393189672384,
0.600194495615913));
#10521=CARTESIAN_POINT('Ctrl Pts',(0.216978840527336,0.0791346402780395,
0.61130920849769));
#10522=CARTESIAN_POINT('Ctrl Pts',(0.0511731008232336,0.225218609978521,
0.622423921379465));
#10523=CARTESIAN_POINT('Ctrl Pts',(-0.161479088824527,0.165126050037305,
0.633538634261242));
#10524=CARTESIAN_POINT('Ctrl Pts',(-0.22630513681055,-0.0461312646876283,
0.644653347143017));
#10525=CARTESIAN_POINT('Ctrl Pts',(-0.0839599934277138,-0.215157681787428,
0.655768060024794));
#10526=CARTESIAN_POINT('Ctrl Pts',(0.135246383026922,-0.18721785279897,
0.66688277290657));
#10527=CARTESIAN_POINT('Ctrl Pts',(0.230641366179104,0.01211068683264,0.677997485788347));
#10528=CARTESIAN_POINT('Ctrl Pts',(0.114895553838575,0.200352489968677,
0.689112198670123));
#10529=CARTESIAN_POINT('Ctrl Pts',(-0.106031471386437,0.205181469933688,
0.700226911551899));
#10530=CARTESIAN_POINT('Ctrl Pts',(-0.229891914034888,0.0221769337352497,
0.711341624433676));
#10531=CARTESIAN_POINT('Ctrl Pts',(-0.143297647665638,-0.181129491530277,
0.722456337315451));
#10532=CARTESIAN_POINT('Ctrl Pts',(0.0744785476940164,-0.218620800615842,
0.733571050197228));
#10533=CARTESIAN_POINT('Ctrl Pts',(0.224073305925671,-0.0559755491269399,
0.744685763079003));
#10534=CARTESIAN_POINT('Ctrl Pts',(0.168540003889557,0.157912556870662,
0.75580047596078));
#10535=CARTESIAN_POINT('Ctrl Pts',(-0.0412833593056288,0.227239505308747,
0.766915188842556));
#10536=CARTESIAN_POINT('Ctrl Pts',(-0.213313843153954,0.0885398941009765,
0.778029901724332));
#10537=CARTESIAN_POINT('Ctrl Pts',(-0.19006602424475,-0.131213623364024,
0.789144614606108));
#10538=CARTESIAN_POINT('Ctrl Pts',(0.00717786579425366,-0.230847540102037,
0.800259327487884));
#10539=CARTESIAN_POINT('Ctrl Pts',(0.197850773711335,-0.119151919289402,
0.811374040369661));
#10540=CARTESIAN_POINT('Ctrl Pts',(0.207401056306209,0.101621407053782,
0.822488753251437));
#10541=CARTESIAN_POINT('Ctrl Pts',(0.0270859008837078,0.229365347212345,
0.833603466133214));
#10542=CARTESIAN_POINT('Ctrl Pts',(-0.178025060919778,0.147136624308943,
0.844718179014988));
#10543=CARTESIAN_POINT('Ctrl Pts',(-0.220162859656535,-0.0697884213632804,
0.855832891896766));
#10544=CARTESIAN_POINT('Ctrl Pts',(-0.0607524188215016,-0.222825609246017,
0.86694760477854));
#10545=CARTESIAN_POINT('Ctrl Pts',(0.154273865132138,-0.171876941634742,
0.878062317660319));
#10546=CARTESIAN_POINT('Ctrl Pts',(0.228070034352413,0.0364165890633767,
0.889177030542093));
#10547=CARTESIAN_POINT('Ctrl Pts',(0.0930793355490916,0.211372528542054,
0.900291743423871));
#10548=CARTESIAN_POINT('Ctrl Pts',(-0.127120904271719,0.192827343044658,
0.911406456305645));
#10549=CARTESIAN_POINT('Ctrl Pts',(-0.230948225841428,-0.00224176475546543,
0.922521169187423));
#10550=CARTESIAN_POINT('Ctrl Pts',(-0.123353837031902,-0.195258647485915,
0.933635882069198));
#10551=CARTESIAN_POINT('Ctrl Pts',(0.0971649057626279,-0.209525868609729,
0.944750594950976));
#10552=CARTESIAN_POINT('Ctrl Pts',(0.228733969509712,-0.0319824908481486,
0.95586530783275));
#10553=CARTESIAN_POINT('Ctrl Pts',(0.15090836534201,0.174839279906789,0.966980020714528));
#10554=CARTESIAN_POINT('Ctrl Pts',(-0.0650664044878212,0.221604312989502,
0.978094733596303));
#10555=CARTESIAN_POINT('Ctrl Pts',(-0.221476090087528,0.0655015270666479,
0.98920944647808));
#10556=CARTESIAN_POINT('Ctrl Pts',(-0.175135338424465,-0.150564676346977,
1.00032415935986));
#10557=CARTESIAN_POINT('Ctrl Pts',(0.0315331778821334,-0.228796344422667,
1.01143887224163));
#10558=CARTESIAN_POINT('Ctrl Pts',(0.209334625055623,-0.0975762434270938,
1.02255358512341));
#10559=CARTESIAN_POINT('Ctrl Pts',(0.19550054738536,0.122970095960548,1.03366829800518));
#10560=CARTESIAN_POINT('Ctrl Pts',(0.00269536068103519,0.230943377387881,
1.04478301088696));
#10561=CARTESIAN_POINT('Ctrl Pts',(-0.192577295791447,0.127499386956076,
1.05589772376874));
#10562=CARTESIAN_POINT('Ctrl Pts',(-0.211554935889174,-0.0926640039575724,
1.06701243665051));
#10563=CARTESIAN_POINT('Ctrl Pts',(-0.0368644660808813,-0.227998069441593,
1.07812714953229));
#10564=CARTESIAN_POINT('Ctrl Pts',(0.171573604267061,-0.154611147228561,
1.08924186241407));
#10565=CARTESIAN_POINT('Ctrl Pts',(0.222944501927657,0.0603146548423409,
1.10035657529584));
#10566=CARTESIAN_POINT('Ctrl Pts',(0.0702207037079931,0.220025365127014,
1.11147128817762));
#10567=CARTESIAN_POINT('Ctrl Pts',(-0.146786685467554,0.178313705300437,
1.12258600105939));
#10568=CARTESIAN_POINT('Ctrl Pts',(-0.22941810362457,-0.0266353572874071,
1.13370071394117));
#10569=CARTESIAN_POINT('Ctrl Pts',(-0.102028562826177,-0.207201063935846,
1.14481542682294));
#10570=CARTESIAN_POINT('Ctrl Pts',(0.11876309518552,-0.198084415718342,
1.15593013970472));
#10571=CARTESIAN_POINT('Ctrl Pts',(0.230832996956947,-0.00763125444445281,
1.1670448525865));
#10572=CARTESIAN_POINT('Ctrl Pts',(0.131586674709788,0.189807943899465,
1.17815956546828));
#10573=CARTESIAN_POINT('Ctrl Pts',(-0.0881207583724943,0.213487330941155,
1.18927427835005));
#10574=CARTESIAN_POINT('Ctrl Pts',(-0.227157983285175,0.0417295957125604,
1.20038899123183));
#10575=CARTESIAN_POINT('Ctrl Pts',(-0.15824327794391,-0.168229526285038,
1.2115037041136));
#10576=CARTESIAN_POINT('Ctrl Pts',(0.0555353437882497,-0.22418281405773,
1.22261841699538));
#10577=CARTESIAN_POINT('Ctrl Pts',(0.218474097288331,-0.0749077922687001,
1.23373312987716));
#10578=CARTESIAN_POINT('Ctrl Pts',(0.181410589874865,0.142941618886087,
1.24484784275893));
#10579=CARTESIAN_POINT('Ctrl Pts',(-0.0217253653892473,0.229935027838791,
1.25596255564071));
#10580=CARTESIAN_POINT('Ctrl Pts',(-0.204972820135662,0.106434259212696,
1.26707726852249));
#10581=CARTESIAN_POINT('Ctrl Pts',(-0.200577767318102,-0.114501824379384,
1.27819198140426));
#10582=CARTESIAN_POINT('Ctrl Pts',(-0.0125636610268072,-0.230617134988113,
1.28930669428604));
#10583=CARTESIAN_POINT('Ctrl Pts',(0.186951857294109,-0.135613832564399,
1.30042140716781));
#10584=CARTESIAN_POINT('Ctrl Pts',(0.215322170737661,0.0835372450906981,
1.31153612004959));
#10585=CARTESIAN_POINT('Ctrl Pts',(0.046575656571621,0.226214094926563,
1.32265083293136));
#10586=CARTESIAN_POINT('Ctrl Pts',(-0.164808574071917,0.161803097748168,
1.33376554581314));
#10587=CARTESIAN_POINT('Ctrl Pts',(-0.225318683520119,-0.0507306552814204,
1.34488025869492));
#10588=CARTESIAN_POINT('Ctrl Pts',(-0.0795606509349228,-0.216822995439444,
1.35599497157669));
#10589=CARTESIAN_POINT('Ctrl Pts',(0.139031233645724,-0.184424576994146,
1.36710968445847));
#10590=CARTESIAN_POINT('Ctrl Pts',(0.230346880851436,0.0168054458594967,
1.37822439734025));
#10591=CARTESIAN_POINT('Ctrl Pts',(0.110791319357884,0.202650911874241,
1.38933911022202));
#10592=CARTESIAN_POINT('Ctrl Pts',(-0.110188230774137,0.202979462821703,
1.4004538231038));
#10593=CARTESIAN_POINT('Ctrl Pts',(-0.230295890121748,0.0174903265136328,
1.41156853598557));
#10594=CARTESIAN_POINT('Ctrl Pts',(-0.139579020268259,-0.184010341093849,
1.42268324886735));
#10595=CARTESIAN_POINT('Ctrl Pts',(0.0789155585962315,-0.217058616829571,
1.43379796174913));
#10596=CARTESIAN_POINT('Ctrl Pts',(0.225166835685355,-0.05140043420017,
1.4449126746309));
#10597=CARTESIAN_POINT('Ctrl Pts',(0.165288979944664,0.16131231086738,1.45602738751268));
#10598=CARTESIAN_POINT('Ctrl Pts',(-0.0459027848742203,0.226351591267464,
1.46714210039445));
#10599=CARTESIAN_POINT('Ctrl Pts',(-0.21507281406851,0.0841771535345191,
1.47825681327623));
#10600=CARTESIAN_POINT('Ctrl Pts',(-0.187354289385532,-0.135057316637657,
1.48937152615801));
#10601=CARTESIAN_POINT('Ctrl Pts',(0.0118778469065368,-0.230653474461988,
1.50048623903978));
#10602=CARTESIAN_POINT('Ctrl Pts',(0.200236400171702,-0.115097752257808,
1.51160095192156));
#10603=CARTESIAN_POINT('Ctrl Pts',(0.205288404749417,0.105824285511226,
1.52271566480333));
#10604=CARTESIAN_POINT('Ctrl Pts',(0.0224089996139133,0.229869409154036,
1.53383037768511));
#10605=CARTESIAN_POINT('Ctrl Pts',(-0.180984739455093,0.143480425887623,
1.54494509056689));
#10606=CARTESIAN_POINT('Ctrl Pts',(-0.21869587572979,-0.0742578108167894,
1.55605980344866));
#10607=CARTESIAN_POINT('Ctrl Pts',(-0.0562017238659076,-0.22401668411755,
1.56717451633044));
#10608=CARTESIAN_POINT('Ctrl Pts',(0.157742334325249,-0.168699331623285,
1.57828922921222));
#10609=CARTESIAN_POINT('Ctrl Pts',(0.22728106530183,0.0410539387122264,
1.58940394209399));
#10610=CARTESIAN_POINT('Ctrl Pts',(0.0887551905086285,0.213224352939102,
1.60051865497577));
#10611=CARTESIAN_POINT('Ctrl Pts',(-0.131021683784578,0.190198388286483,
1.61163336785754));
#10612=CARTESIAN_POINT('Ctrl Pts',(-0.230854668569309,-0.00694482024794042,
1.62274808073932));
#10613=CARTESIAN_POINT('Ctrl Pts',(-0.119351590043181,-0.197730388364273,
1.6338627936211));
#10614=CARTESIAN_POINT('Ctrl Pts',(0.101411982740808,-0.207503538006223,
1.64497750650287));
#10615=CARTESIAN_POINT('Ctrl Pts',(0.229337886969887,-0.0273174326888366,
1.65609221938465));
#10616=CARTESIAN_POINT('Ctrl Pts',(0.14731626663463,0.177876434957968,1.66720693226643));
#10617=CARTESIAN_POINT('Ctrl Pts',(-0.0695661301586456,0.220233199275841,
1.6783216451482));
#10618=CARTESIAN_POINT('Ctrl Pts',(-0.222764165796864,0.0609773315696025,
1.68943635802998));
#10619=CARTESIAN_POINT('Ctrl Pts',(-0.172032594388376,-0.154100275783421,
1.70055107091176));
#10620=CARTESIAN_POINT('Ctrl Pts',(0.0361863325261053,-0.228106680890394,
1.71166578379353));
#10621=CARTESIAN_POINT('Ctrl Pts',(0.211278456724753,-0.0932926698756588,
1.72278049667531));
#10622=CARTESIAN_POINT('Ctrl Pts',(0.192955574056439,0.126926179210878,
1.73389520955708));
#10623=CARTESIAN_POINT('Ctrl Pts',(-0.00200862008152737,0.230950371235661,
1.74500992243886));
#10624=CARTESIAN_POINT('Ctrl Pts',(-0.195134021600103,0.123550888878601,
1.75612463532063));
#10625=CARTESIAN_POINT('Ctrl Pts',(-0.209623850363949,-0.0969533387105092,
1.76723934820241));
#10626=CARTESIAN_POINT('Ctrl Pts',(-0.0322133827788769,-0.228701566453891,
1.77835406108419));
#10627=CARTESIAN_POINT('Ctrl Pts',(0.174686847974531,-0.151084789681969,
1.78946877396597));
#10628=CARTESIAN_POINT('Ctrl Pts',(0.221669884971746,0.0648426605340554,
1.80058348684774));
#10629=CARTESIAN_POINT('Ctrl Pts',(0.0657250750476629,0.221409853074566,
1.81169819972952));
#10630=CARTESIAN_POINT('Ctrl Pts',(-0.150387799518412,0.17528724507086,
1.82281291261129));
#10631=CARTESIAN_POINT('Ctrl Pts',(-0.228828060759529,-0.0313021906191119,
1.83392762549307));
#10632=CARTESIAN_POINT('Ctrl Pts',(-0.0977875181872369,-0.209236014622967,
1.84504233837484));
#10633=CARTESIAN_POINT('Ctrl Pts',(0.122772674399952,-0.195624586770695,
1.85615705125662));
#10634=CARTESIAN_POINT('Ctrl Pts',(0.230940538728716,-0.00292849794471524,
1.8672717641384));
#10635=CARTESIAN_POINT('Ctrl Pts',(0.127693729850804,0.192448486315979,
1.87838647702018));
#10636=CARTESIAN_POINT('Ctrl Pts',(-0.0924503908440751,0.211648372923818,
1.88950118990195));
#10637=CARTESIAN_POINT('Ctrl Pts',(-0.227960738379322,0.037094612628738,
1.90061590278373));
#10638=CARTESIAN_POINT('Ctrl Pts',(-0.154784272963854,-0.171417436019714,
1.9117306156655));
#10639=CARTESIAN_POINT('Ctrl Pts',(0.0600895603815735,-0.22300527630904,
1.92284532854728));
#10640=CARTESIAN_POINT('Ctrl Pts',(0.219954364817935,-0.0704427847693452,
1.93396004142905));
#10641=CARTESIAN_POINT('Ctrl Pts',(0.17846179642427,0.146606601984851,1.94507475431083));
#10642=CARTESIAN_POINT('Ctrl Pts',(-0.0264037448506712,0.229444875267203,
1.95618946719261));
#10643=CARTESIAN_POINT('Ctrl Pts',(-0.207097959948898,0.102237681475696,
1.96730418007438));
#10644=CARTESIAN_POINT('Ctrl Pts',(-0.198204206796146,-0.118563067339009,
1.97841889295616));
#10645=CARTESIAN_POINT('Ctrl Pts',(-0.00786427776336803,-0.230825175541536,
1.98953360583794));
#10646=CARTESIAN_POINT('Ctrl Pts',(0.189675009695157,-0.131778219845543,
2.00064831871971));
#10647=CARTESIAN_POINT('Ctrl Pts',(0.213576180559224,0.0879051968103603,
2.01176303160149));
#10648=CARTESIAN_POINT('Ctrl Pts',(0.041958891709643,0.227115741275252,
2.02287774448326));
#10649=CARTESIAN_POINT('Ctrl Pts',(-0.168069693085213,0.158413025962974,
2.03399245736504));
#10650=CARTESIAN_POINT('Ctrl Pts',(-0.224238763066937,-0.0553090016798028,
2.04510717024682));
#10651=CARTESIAN_POINT('Ctrl Pts',(-0.0751283049278165,-0.218398366127328,
2.05622188312859));
#10652=CARTESIAN_POINT('Ctrl Pts',(0.142758411039642,-0.181554797804617,
2.06733659601037));
#10653=CARTESIAN_POINT('Ctrl Pts',(0.229956842554795,0.0214932336169949,
2.07845130889215));
#10654=CARTESIAN_POINT('Ctrl Pts',(0.106641126190407,0.204865269707925,
2.08956602177392));
#10655=CARTESIAN_POINT('Ctrl Pts',(-0.114299281647489,0.200693255350372,
2.1006807346557));
#10656=CARTESIAN_POINT('Ctrl Pts',(-0.230604334398658,0.0127964639151555,
2.11179544753747));
#10657=CARTESIAN_POINT('Ctrl Pts',(-0.135802492397184,-0.186814859100201,
2.12291016041925));
#10658=CARTESIAN_POINT('Ctrl Pts',(0.0833198335536108,-0.215406392350623,
2.13402487330102));
#10659=CARTESIAN_POINT('Ctrl Pts',(0.226166961327859,-0.046803997215492,
2.1451395861828));
#10660=CARTESIAN_POINT('Ctrl Pts',(0.161969390376449,0.164645148912813,
2.15625429906458));
#10661=CARTESIAN_POINT('Ctrl Pts',(-0.0505031687521857,0.225369781674834,
2.16736901194636));
#10662=CARTESIAN_POINT('Ctrl Pts',(-0.216742568417862,0.0797794942661454,
2.17848372482813));
#10663=CARTESIAN_POINT('Ctrl Pts',(-0.184564835099688,-0.138844984849663,
2.18959843770991));
#10664=CARTESIAN_POINT('Ctrl Pts',(0.0165728994326188,-0.230363729251825,
2.20071315059168));
#10665=CARTESIAN_POINT('Ctrl Pts',(0.202538966804212,-0.110995839031374,
2.21182786347346));
#10666=CARTESIAN_POINT('Ctrl Pts',(0.203090589989375,0.109983263613629,
2.22294257635523));
#10667=CARTESIAN_POINT('Ctrl Pts',(0.017722812188571,0.230278120197415,
2.23405728923701));
#10668=CARTESIAN_POINT('Ctrl Pts',(-0.18386935977409,0.139764700997745,
2.24517200211879));
#10669=CARTESIAN_POINT('Ctrl Pts',(-0.217138137211476,-0.0786963819928267,
2.25628671500057));
#10670=CARTESIAN_POINT('Ctrl Pts',(-0.0516277812381195,-0.225114859506612,
2.26740142788234));
#10671=CARTESIAN_POINT('Ctrl Pts',(0.161145494158321,-0.165451688932609,
2.27851614076412));
#10672=CARTESIAN_POINT('Ctrl Pts',(0.226397576026225,0.0456741584555444,
2.28963085364589));
#10673=CARTESIAN_POINT('Ctrl Pts',(0.0843946825769435,0.214987917078343,
2.30074556652767));
#10674=CARTESIAN_POINT('Ctrl Pts',(-0.134868977678981,0.187490173751543,
2.31186027940945));
#10675=CARTESIAN_POINT('Ctrl Pts',(-0.23066370196654,-0.0116443075567319,
2.32297499229122));
#10676=CARTESIAN_POINT('Ctrl Pts',(-0.115302964228264,-0.200121413881057,
2.334089705173));
#10677=CARTESIAN_POINT('Ctrl Pts',(0.105622948018994,-0.205392642806054,
2.34520441805477));
#10678=CARTESIAN_POINT('Ctrl Pts',(0.229835338308358,-0.0226457751156407,
2.35631913093655));
#10679=CARTESIAN_POINT('Ctrl Pts',(0.143684619655405,0.180848806972633,
2.36743384381833));
#10680=CARTESIAN_POINT('Ctrl Pts',(-0.0740780534647546,0.218753590559653,
2.3785485567001));
#10681=CARTESIAN_POINT('Ctrl Pts',(-0.223881422364772,0.0564605125878301,
2.38966326958188));
#10682=CARTESIAN_POINT('Ctrl Pts',(-0.169010303570728,-0.157634697366895,
2.40077798246365));
#10683=CARTESIAN_POINT('Ctrl Pts',(0.041135907400424,-0.227197880070916,
2.41189269534543));
#10684=CARTESIAN_POINT('Ctrl Pts',(0.15528794296551,-0.135237888987316,
2.41930250393328));
#10685=CARTESIAN_POINT('Ctrl Pts',(0.180319843122459,-0.0752722669798892,
2.42300740822721));
#10686=CARTESIAN_POINT('',(-0.152020725150953,-0.123272996449671,2.4));
#10687=CARTESIAN_POINT('Ctrl Pts',(-0.152022961461291,-0.123275749177759,
2.4));
#10688=CARTESIAN_POINT('Ctrl Pts',(-0.148843860776273,-0.126520593760054,
2.4));
#10689=CARTESIAN_POINT('Ctrl Pts',(-0.145550280466061,-0.129639743170448,
2.4));
#10690=CARTESIAN_POINT('Ctrl Pts',(-0.142144069729337,-0.132625074476751,
2.4));
#10691=CARTESIAN_POINT('Ctrl Pts',(-0.132568315892317,-0.141017625590188,
2.4));
#10692=CARTESIAN_POINT('Ctrl Pts',(-0.122103883881501,-0.148356196379371,
2.4));
#10693=CARTESIAN_POINT('Ctrl Pts',(-0.110956607971893,-0.154597350195316,
2.4));
#10694=CARTESIAN_POINT('Ctrl Pts',(-0.105501670740442,-0.15765146876149,
2.4));
#10695=CARTESIAN_POINT('Ctrl Pts',(-0.0998828881521222,-0.160442052175162,
2.4));
#10696=CARTESIAN_POINT('Ctrl Pts',(-0.0941236483875527,-0.162959592659121,
2.4));
#10697=CARTESIAN_POINT('Ctrl Pts',(-0.090759079960923,-0.164430348795582,
2.4));
#10698=CARTESIAN_POINT('Ctrl Pts',(-0.0873466982488509,-0.165807525926122,
2.4));
#10699=CARTESIAN_POINT('Ctrl Pts',(-0.0839043527287597,-0.167084756767954,
2.4));
#10700=CARTESIAN_POINT('Ctrl Pts',(-0.0722464129819429,-0.171410261023684,
2.4));
#10701=CARTESIAN_POINT('Ctrl Pts',(-0.0602078660333974,-0.174610335907723,
2.4));
#10702=CARTESIAN_POINT('Ctrl Pts',(-0.047979011447792,-0.17663071349189,
2.4));
#10703=CARTESIAN_POINT('Ctrl Pts',(-0.0395067434511661,-0.178030450501403,
2.4));
#10704=CARTESIAN_POINT('Ctrl Pts',(-0.0309428099130652,-0.178862922405498,
2.4));
#10705=CARTESIAN_POINT('Ctrl Pts',(-0.0223535667019919,-0.179095476400577,
2.4));
#10706=CARTESIAN_POINT('Ctrl Pts',(-0.0183635027663534,-0.179203507490867,
2.4));
#10707=CARTESIAN_POINT('Ctrl Pts',(-0.014376249181295,-0.179181530851919,
2.4));
#10708=CARTESIAN_POINT('Ctrl Pts',(-0.0104054136088075,-0.179027692656729,
2.4));
#10709=CARTESIAN_POINT('Ctrl Pts',(0.00121824750065017,-0.178577368533774,
2.4));
#10710=CARTESIAN_POINT('Ctrl Pts',(0.0127220893604508,-0.17700119131334,
2.4));
#10711=CARTESIAN_POINT('Ctrl Pts',(0.0239367001203737,-0.17422702409659,
2.4));
#10712=CARTESIAN_POINT('Ctrl Pts',(0.0263036255441019,-0.173641515864913,
2.4));
#10713=CARTESIAN_POINT('Ctrl Pts',(0.0286575889694474,-0.173002476522168,
2.4));
#10714=CARTESIAN_POINT('Ctrl Pts',(0.0309968484005323,-0.172308959609585,
2.4));
#10715=CARTESIAN_POINT('Ctrl Pts',(0.0349907200356912,-0.171124902172917,
2.4));
#10716=CARTESIAN_POINT('Ctrl Pts',(0.0389417632399139,-0.169782062987551,
2.4));
#10717=CARTESIAN_POINT('Ctrl Pts',(0.0428430867479635,-0.168285488070655,
2.4));
#10718=CARTESIAN_POINT('Ctrl Pts',(0.0460795423288881,-0.167043961129333,
2.4));
#10719=CARTESIAN_POINT('Ctrl Pts',(0.0492804988882749,-0.1656968372236,
2.4));
#10720=CARTESIAN_POINT('Ctrl Pts',(0.0524310205930229,-0.164252769154906,
2.4));
#10721=CARTESIAN_POINT('Ctrl Pts',(0.0632193618964415,-0.159307842361683,
2.4));
#10722=CARTESIAN_POINT('Ctrl Pts',(0.0734566084017215,-0.153215648615148,
2.4));
#10723=CARTESIAN_POINT('Ctrl Pts',(0.0829954583811563,-0.146117480833417,
2.4));
#10724=CARTESIAN_POINT('Ctrl Pts',(0.0871250594161281,-0.143044510707979,
2.4));
#10725=CARTESIAN_POINT('Ctrl Pts',(0.0911232569109863,-0.139782483459033,
2.4));
#10726=CARTESIAN_POINT('Ctrl Pts',(0.0949753370068491,-0.136341074649165,
2.4));
#10727=CARTESIAN_POINT('Ctrl Pts',(0.0986768888660373,-0.133034146220529,
2.4));
#10728=CARTESIAN_POINT('Ctrl Pts',(0.102245690547589,-0.129558617700049,
2.4));
#10729=CARTESIAN_POINT('Ctrl Pts',(0.105650031744245,-0.125942409265612,
2.4));
#10730=CARTESIAN_POINT('Ctrl Pts',(0.111001095053008,-0.120258325575831,
2.4));
#10731=CARTESIAN_POINT('Ctrl Pts',(0.115956461643762,-0.114218962093958,
2.4));
#10732=CARTESIAN_POINT('Ctrl Pts',(0.120465674061468,-0.107861150525121,
2.4));
#10733=CARTESIAN_POINT('Ctrl Pts',(0.122806690655693,-0.10456040950721,
2.4));
#10734=CARTESIAN_POINT('Ctrl Pts',(0.125027588538421,-0.101173242254719,
2.4));
#10735=CARTESIAN_POINT('Ctrl Pts',(0.127119040336103,-0.0977061228092429,
2.4));
#10736=CARTESIAN_POINT('Ctrl Pts',(0.132655068544743,-0.0885287317385256,
2.4));
#10737=CARTESIAN_POINT('Ctrl Pts',(0.13725573814533,-0.0788453760087664,
2.4));
#10738=CARTESIAN_POINT('Ctrl Pts',(0.140775482942457,-0.0687522252708787,
2.4));
#10739=CARTESIAN_POINT('Ctrl Pts',(0.141790390598368,-0.0658418961002798,
2.4));
#10740=CARTESIAN_POINT('Ctrl Pts',(0.142715102613091,-0.0628974577303924,
2.4));
#10741=CARTESIAN_POINT('Ctrl Pts',(0.143545299885864,-0.0599211930845618,
2.4));
#10742=CARTESIAN_POINT('Ctrl Pts',(-0.195373070919361,0.000178101583232409,
2.39241303078758));
#10743=CARTESIAN_POINT('Ctrl Pts',(-0.194995765056209,-0.044191626196564,
2.39494202052505));
#10744=CARTESIAN_POINT('Ctrl Pts',(-0.17967283890898,-0.0888121436870032,
2.39747101026252));
#10745=CARTESIAN_POINT('Ctrl Pts',(-0.152022961461301,-0.123275749177746,
2.4));
#10746=CARTESIAN_POINT('',(-0.0903606778650279,-0.126612599672279,0.));
#10747=CARTESIAN_POINT('Ctrl Pts',(-0.0905547187627355,-0.126790994435269,
1.73472347597681E-18));
#10748=CARTESIAN_POINT('Ctrl Pts',(-0.0937786982673177,-0.125067385071004,
2.04138089632303E-18));
#10749=CARTESIAN_POINT('Ctrl Pts',(-0.0969317870940273,-0.123225562125392,
4.55088741215883E-19));
#10750=CARTESIAN_POINT('Ctrl Pts',(-0.100006715605072,-0.121266986978485,
-4.55364912443912E-18));
#10751=CARTESIAN_POINT('Ctrl Pts',(-0.107443591426499,-0.116530070298256,
-1.67607735186196E-17));
#10752=CARTESIAN_POINT('Ctrl Pts',(-0.114423960357848,-0.111111926712958,
-1.67652824684633E-17));
#10753=CARTESIAN_POINT('Ctrl Pts',(-0.120920626723682,-0.105114084706666,
1.90819582357449E-17));
#10754=CARTESIAN_POINT('Ctrl Pts',(-0.123989218118145,-0.102281104632047,
3.60138011450046E-17));
#10755=CARTESIAN_POINT('Ctrl Pts',(-0.126949571175365,-0.0993181071661729,
-2.80225227290868E-17));
#10756=CARTESIAN_POINT('Ctrl Pts',(-0.129788621846087,-0.0962459886237453,
-2.73218947466347E-17));
#10757=CARTESIAN_POINT('Ctrl Pts',(-0.135122303451826,-0.0904744459283742,
-2.60056355403416E-17));
#10758=CARTESIAN_POINT('Ctrl Pts',(-0.140037740247948,-0.0843101296795999,
-2.18057762441945E-17));
#10759=CARTESIAN_POINT('Ctrl Pts',(-0.144515198029218,-0.0778188929962127,
-1.12757025938492E-17));
#10760=CARTESIAN_POINT('Ctrl Pts',(-0.14680932318637,-0.0744929633942239,
-5.88038497210284E-18));
#10761=CARTESIAN_POINT('Ctrl Pts',(-0.148989224672256,-0.0710795596597342,
1.31303430263246E-17));
#10762=CARTESIAN_POINT('Ctrl Pts',(-0.151048822309793,-0.0675910768160332,
1.12757025938492E-17));
#10763=CARTESIAN_POINT('Ctrl Pts',(-0.156978439475454,-0.0575476744664053,
5.93616076096574E-18));
#10764=CARTESIAN_POINT('Ctrl Pts',(-0.161879094027928,-0.0469447472885605,
1.60901821933146E-17));
#10765=CARTESIAN_POINT('Ctrl Pts',(-0.165691488986893,-0.0359818104818786,
3.46944695195361E-18));
#10766=CARTESIAN_POINT('Ctrl Pts',(-0.168615156166144,-0.0275745025101442,
-6.20920119451492E-18));
#10767=CARTESIAN_POINT('Ctrl Pts',(-0.170898487612157,-0.0189541362718905,
7.18953415028294E-18));
#10768=CARTESIAN_POINT('Ctrl Pts',(-0.172499257712041,-0.0101976684652424,
5.20417042793042E-18));
#10769=CARTESIAN_POINT('Ctrl Pts',(-0.173128740734504,-0.00675429591510353,
4.42345072512973E-18));
#10770=CARTESIAN_POINT('Ctrl Pts',(-0.173652109787855,-0.00329034195238573,
-8.72241236130908E-18));
#10771=CARTESIAN_POINT('Ctrl Pts',(-0.174065393356307,0.000176078536121731,
-8.67361737988404E-18));
#10772=CARTESIAN_POINT('Ctrl Pts',(-0.174874448648527,0.0069620387227214,
-8.57809498081156E-18));
#10773=CARTESIAN_POINT('Ctrl Pts',(-0.17526451573988,0.0137702403350294,
-1.47546100136584E-17));
#10774=CARTESIAN_POINT('Ctrl Pts',(-0.17522174425039,0.020564792502022,
-1.04083408558608E-17));
#10775=CARTESIAN_POINT('Ctrl Pts',(-0.175173289109206,0.028262232747164,
-7.43567664424826E-18));
#10776=CARTESIAN_POINT('Ctrl Pts',(-0.174569669212428,0.0359422811365838,
-3.66078693759541E-17));
#10777=CARTESIAN_POINT('Ctrl Pts',(-0.173446373975917,0.0435656717636881,
-4.5102810375397E-17));
#10778=CARTESIAN_POINT('Ctrl Pts',(-0.17276034872808,0.0482214721929289,
-5.02908889989642E-17));
#10779=CARTESIAN_POINT('Ctrl Pts',(-0.171880287491841,0.0528561871195019,
-2.94043840421531E-18));
#10780=CARTESIAN_POINT('Ctrl Pts',(-0.170812464892208,0.0574609818532008,
-6.93889390390723E-18));
#10781=CARTESIAN_POINT('Ctrl Pts',(-0.170006933705219,0.0609346915957652,
-9.95520073792165E-18));
#10782=CARTESIAN_POINT('Ctrl Pts',(-0.169094445764795,0.0643905438353253,
-1.22076013790627E-17));
#10783=CARTESIAN_POINT('Ctrl Pts',(-0.168081936099544,0.0678120165229409,
-1.38777878078145E-17));
#10784=CARTESIAN_POINT('Ctrl Pts',(-0.164824625672852,0.0788191200030298,
-1.92508877945114E-17));
#10785=CARTESIAN_POINT('Ctrl Pts',(-0.160527857603151,0.0895048987030934,
-1.40762953787734E-17));
#10786=CARTESIAN_POINT('Ctrl Pts',(-0.15530139184747,0.0997465174632775,
-6.93889390390723E-18));
#10787=CARTESIAN_POINT('Ctrl Pts',(-0.152082958509342,0.106053258728798,
-2.54371522520859E-18));
#10788=CARTESIAN_POINT('Ctrl Pts',(-0.148511119845249,0.112191703210516,
-2.81380830112988E-17));
#10789=CARTESIAN_POINT('Ctrl Pts',(-0.144604138031713,0.118132165785462,
-2.42861286636753E-17));
#10790=CARTESIAN_POINT('Ctrl Pts',(-0.141699683152471,0.122548312656426,
-2.14225812673671E-17));
#10791=CARTESIAN_POINT('Ctrl Pts',(-0.138605937056638,0.126859392699012,
-1.20788926485952E-17));
#10792=CARTESIAN_POINT('Ctrl Pts',(-0.135350387038284,0.131026597701989,
-1.38777878078145E-17));
#10793=CARTESIAN_POINT('Ctrl Pts',(-0.127454964434828,0.141132983531803,
-1.82405029930444E-17));
#10794=CARTESIAN_POINT('Ctrl Pts',(-0.118596896875794,0.150421116028237,
3.19066915871575E-18));
#10795=CARTESIAN_POINT('Ctrl Pts',(-0.108893943796901,0.158727847366355,
1.73472347597681E-17));
#10796=CARTESIAN_POINT('Ctrl Pts',(-0.101760675780719,0.164834662527825,
2.77546412266345E-17));
#10797=CARTESIAN_POINT('Ctrl Pts',(-0.0941695959020444,0.170411093356264,
-5.23705385272153E-18));
#10798=CARTESIAN_POINT('Ctrl Pts',(-0.0861525859670525,0.175382131162755,
-6.93889390390723E-18));
#10799=CARTESIAN_POINT('Ctrl Pts',(-0.090554718762734,-0.12679099443527,
1.38750773023832E-16));
#10800=CARTESIAN_POINT('Ctrl Pts',(-0.0514132965269827,-0.154438798808553,
0.00344557680604053));
#10801=CARTESIAN_POINT('Ctrl Pts',(0.0585934425206843,-0.172181219813116,
0.0105960579060063));
#10802=CARTESIAN_POINT('Ctrl Pts',(0.177419525591119,-0.0482168938798953,
0.0214514432998975));
#10803=CARTESIAN_POINT('Ctrl Pts',(0.13670630608002,0.122966787890628,0.0325661561816737));
#10804=CARTESIAN_POINT('Ctrl Pts',(-0.0291762440449378,0.181518694867924,
0.0436808690634499));
#10805=CARTESIAN_POINT('Ctrl Pts',(-0.141190839714012,0.0949193830602739,
0.0526273578563488));
#10806=CARTESIAN_POINT('Ctrl Pts',(-0.155411338149369,0.021598754870737,
0.0578689423553222));
#10807=CARTESIAN_POINT('Ctrl Pts',(-0.155324515707295,7.08434145518418E-5,
0.0594056225603703));
#10808=CARTESIAN_POINT('Origin',(0.,0.,-0.129405622560373));
#10809=CARTESIAN_POINT('',(0.090360677865021,-0.126612599672283,0.));
#10810=CARTESIAN_POINT('Origin',(0.,0.,0.));
#10811=CARTESIAN_POINT('Ctrl Pts',(0.0903606778650135,-0.126612599672289,
0.));
#10812=CARTESIAN_POINT('Ctrl Pts',(0.132465879166514,-0.0965630268723143,
0.0037049042939254));
#10813=CARTESIAN_POINT('Ctrl Pts',(0.183615222457176,0.00832016090824247,
0.0111147128817762));
#10814=CARTESIAN_POINT('Ctrl Pts',(0.0924018852348323,0.159092396164803,
0.0222294257635523));
#10815=CARTESIAN_POINT('Ctrl Pts',(-0.0834773491744035,0.163753054047276,
0.0333441386453285));
#10816=CARTESIAN_POINT('Ctrl Pts',(-0.153142789995597,0.0621407336789083,
0.0411324558706874));
#10817=CARTESIAN_POINT('Ctrl Pts',(-0.155773969573712,0.00536683624356025,
0.0452158688021209));
#10818=CARTESIAN_POINT('Ctrl Pts',(-0.155737693224454,0.000100603112028588,
0.045594377439629));
#10819=CARTESIAN_POINT('Ctrl Pts',(0.113509973994375,-0.15904919303095,
-0.0230074082272066));
#10820=CARTESIAN_POINT('Ctrl Pts',(0.166402010859132,-0.121301288658623,
-0.0193025039332812));
#10821=CARTESIAN_POINT('Ctrl Pts',(0.230655187837557,0.0104516839696087,
-0.0118926953454304));
#10822=CARTESIAN_POINT('Ctrl Pts',(0.116074113628315,0.199849914565114,
-0.000777982463654263));
#10823=CARTESIAN_POINT('Ctrl Pts',(-0.104863221013695,0.2057045757688,0.010336730418122));
#10824=CARTESIAN_POINT('Ctrl Pts',(-0.229752900032261,0.0235435225184469,
0.0214514432998981));
#10825=CARTESIAN_POINT('Ctrl Pts',(-0.144341709283358,-0.180324797442481,
0.0325661561816743));
#10826=CARTESIAN_POINT('Ctrl Pts',(0.0732211700541786,-0.219033718527301,
0.0436808690634505));
#10827=CARTESIAN_POINT('Ctrl Pts',(0.223746334253748,-0.0572705996896121,
0.0547955819452267));
#10828=CARTESIAN_POINT('Ctrl Pts',(0.169446625860147,0.156943281339981,
0.0659102948270027));
#10829=CARTESIAN_POINT('Ctrl Pts',(-0.0399751411601898,0.227471578691002,
0.0770250077087791));
#10830=CARTESIAN_POINT('Ctrl Pts',(-0.212800571019475,0.0897670413771846,
0.088139720590555));
#10831=CARTESIAN_POINT('Ctrl Pts',(-0.190818134346944,-0.13011804196319,
0.0992544334723316));
#10832=CARTESIAN_POINT('Ctrl Pts',(0.00584918801334432,-0.230884768458966,
0.110369146354107));
#10833=CARTESIAN_POINT('Ctrl Pts',(0.197161712231628,-0.120288773936248,
0.121483859235884));
#10834=CARTESIAN_POINT('Ctrl Pts',(0.207982494406915,0.100426132144772,
0.13259857211766));
#10835=CARTESIAN_POINT('Ctrl Pts',(0.0284055178284121,0.229205619323633,
0.143713284999436));
#10836=CARTESIAN_POINT('Ctrl Pts',(-0.177175286844647,0.148158796784502,
0.154827997881212));
#10837=CARTESIAN_POINT('Ctrl Pts',(-0.220560866541884,-0.068520165527927,
0.165942710762988));
#10838=CARTESIAN_POINT('Ctrl Pts',(-0.0620338447715747,-0.222472259699958,
0.177057423644765));
#10839=CARTESIAN_POINT('Ctrl Pts',(0.153282099103901,-0.172761991393912,
0.188172136526541));
#10840=CARTESIAN_POINT('Ctrl Pts',(0.228275842850265,0.0351033693558483,
0.199286849408317));
#10841=CARTESIAN_POINT('Ctrl Pts',(0.0942943101399089,0.210833321528243,
0.210401562290093));
#10842=CARTESIAN_POINT('Ctrl Pts',(-0.126009012428097,0.193555768902392,
0.221516275171869));
#10843=CARTESIAN_POINT('Ctrl Pts',(-0.230957299139034,-0.000912545418766224,
0.232630988053646));
#10844=CARTESIAN_POINT('Ctrl Pts',(-0.124475569182979,-0.194545468655793,
0.243745700935422));
#10845=CARTESIAN_POINT('Ctrl Pts',(0.0959574051494835,-0.210081610730679,
0.254860413817198));
#10846=CARTESIAN_POINT('Ctrl Pts',(0.228546107728123,-0.0332983992076444,
0.265975126698974));
#10847=CARTESIAN_POINT('Ctrl Pts',(0.151912120568595,0.173967854400789,
0.277089839580751));
#10848=CARTESIAN_POINT('Ctrl Pts',(-0.0637899206477135,0.221975117467028,
0.288204552462526));
#10849=CARTESIAN_POINT('Ctrl Pts',(-0.221095435638538,0.0667751082861117,
0.299319265344303));
#10850=CARTESIAN_POINT('Ctrl Pts',(-0.175998983737975,-0.149554219162863,
0.310433978226078));
#10851=CARTESIAN_POINT('Ctrl Pts',(0.0302158574941517,-0.22897403499859,
0.321548691107855));
#10852=CARTESIAN_POINT('Ctrl Pts',(0.208769571438822,-0.0987794148000734,
0.332663403989631));
#10853=CARTESIAN_POINT('Ctrl Pts',(0.196205039257046,0.121842887839669,
0.343778116871407));
#10854=CARTESIAN_POINT('Ctrl Pts',(0.0040244704784676,0.230924035961029,
0.354892829753183));
#10855=CARTESIAN_POINT('Ctrl Pts',(-0.191840302536165,0.12860561834497,
0.366007542634959));
#10856=CARTESIAN_POINT('Ctrl Pts',(-0.212084740152647,-0.0914449000297386,
0.377122255516736));
#10857=CARTESIAN_POINT('Ctrl Pts',(-0.038176058189903,-0.227782122494658,
0.388236968398511));
#10858=CARTESIAN_POINT('Ctrl Pts',(0.170680922200525,-0.155596046041835,
0.399351681280289));
#10859=CARTESIAN_POINT('Ctrl Pts',(0.223287936308385,0.0590305365571002,
0.410466394162064));
#10860=CARTESIAN_POINT('Ctrl Pts',(0.071485857298635,0.21961757432719,0.421581107043841));
#10861=CARTESIAN_POINT('Ctrl Pts',(-0.145757998381792,0.179155554350991,
0.432695819925616));
#10862=CARTESIAN_POINT('Ctrl Pts',(-0.2295675953358,-0.0253145396722107,
0.443810532807393));
#10863=CARTESIAN_POINT('Ctrl Pts',(-0.103219381045708,-0.206610421139929,
0.454925245689169));
#10864=CARTESIAN_POINT('Ctrl Pts',(0.117621085806451,-0.198764652090831,
0.466039958570945));
#10865=CARTESIAN_POINT('Ctrl Pts',(0.230785249680916,-0.00895964713562851,
0.477154671452722));
#10866=CARTESIAN_POINT('Ctrl Pts',(0.132676899813103,0.189047472881977,
0.488269384334497));
#10867=CARTESIAN_POINT('Ctrl Pts',(-0.0868906082019593,0.213990955307395,
0.499384097216274));
#10868=CARTESIAN_POINT('Ctrl Pts',(-0.226914049857475,0.0430362721940153,
0.51049881009805));
#10869=CARTESIAN_POINT('Ctrl Pts',(-0.159208870281294,-0.167315995561787,
0.521613522979826));
#10870=CARTESIAN_POINT('Ctrl Pts',(0.0542441778475903,-0.224498721414436,
0.532728235861603));
#10871=CARTESIAN_POINT('Ctrl Pts',(0.218039356482698,-0.0761639401008682,
0.543842948743378));
#10872=CARTESIAN_POINT('Ctrl Pts',(0.182230257970378,0.14189517196553,0.554957661625155));
#10873=CARTESIAN_POINT('Ctrl Pts',(-0.0204016541079569,0.230056252374799,
0.566072374506931));
#10874=CARTESIAN_POINT('Ctrl Pts',(-0.204356858061106,0.107612180121354,
0.577187087388706));
#10875=CARTESIAN_POINT('Ctrl Pts',(-0.201233437350254,-0.113345535594831,
0.588301800270484));
#10876=CARTESIAN_POINT('Ctrl Pts',(-0.0138907295889131,-0.2305410036817,
0.599416513152259));
#10877=CARTESIAN_POINT('Ctrl Pts',(0.186168256019567,-0.136687553192347,
0.610531226034036));
#10878=CARTESIAN_POINT('Ctrl Pts',(0.21579938507027,0.0822966108073177,
0.621645938915812));
#10879=CARTESIAN_POINT('Ctrl Pts',(0.0478768203261135,0.225942286486038,
0.632760651797588));
#10880=CARTESIAN_POINT('Ctrl Pts',(-0.163874612139314,0.162748942372192,
0.643875364679364));
#10881=CARTESIAN_POINT('Ctrl Pts',(-0.225606919495652,-0.0494330316970348,
0.654990077561141));
#10882=CARTESIAN_POINT('Ctrl Pts',(-0.0808072189988052,-0.216361503287338,
0.666104790442916));
#10883=CARTESIAN_POINT('Ctrl Pts',(0.137967505075176,-0.185221689578757,
0.677219503324693));
#10884=CARTESIAN_POINT('Ctrl Pts',(0.230439782817408,0.0154794457957462,
0.688334216206469));
#10885=CARTESIAN_POINT('Ctrl Pts',(0.111955804692462,0.20200991199132,0.699448929088245));
#10886=CARTESIAN_POINT('Ctrl Pts',(-0.109018190962282,0.203610266898281,
0.710563641970021));
#10887=CARTESIAN_POINT('Ctrl Pts',(-0.230191409573946,0.0188154645288922,
0.721678354851798));
#10888=CARTESIAN_POINT('Ctrl Pts',(-0.140635745773037,-0.183203967637002,
0.732793067733573));
#10889=CARTESIAN_POINT('Ctrl Pts',(0.0776650071207401,-0.217509203060499,
0.74390778061535));
#10890=CARTESIAN_POINT('Ctrl Pts',(0.224867276437698,-0.0526954906473946,
0.755022493497126));
#10891=CARTESIAN_POINT('Ctrl Pts',(0.166214644641793,0.160358344509041,
0.766137206378902));
#10892=CARTESIAN_POINT('Ctrl Pts',(-0.044599296608695,0.226612024149398,
0.777251919260677));
#10893=CARTESIAN_POINT('Ctrl Pts',(-0.214584781453568,0.08541357219788,
0.788366632142455));
#10894=CARTESIAN_POINT('Ctrl Pts',(-0.188128482210358,-0.133976792498943,
0.799481345024231));
#10895=CARTESIAN_POINT('Ctrl Pts',(0.0105501639898399,-0.230718011405407,
0.810596057906007));
#10896=CARTESIAN_POINT('Ctrl Pts',(0.19957065539198,-0.116248269894625,
0.821710770787783));
#10897=CARTESIAN_POINT('Ctrl Pts',(0.205894054617937,0.104641029333927,
0.832825483669559));
#10898=CARTESIAN_POINT('Ctrl Pts',(0.0237316015467294,0.229736627108315,
0.843940196551335));
#10899=CARTESIAN_POINT('Ctrl Pts',(-0.180155962296678,0.144519673387521,
0.855054909433111));
#10900=CARTESIAN_POINT('Ctrl Pts',(-0.219119627958972,-0.0729979136016889,
0.866169622314888));
#10901=CARTESIAN_POINT('Ctrl Pts',(-0.0574900812163527,-0.223689510949474,
0.877284335196663));
#10902=CARTESIAN_POINT('Ctrl Pts',(0.15676879946602,-0.16960439340141,0.88839904807844));
#10903=CARTESIAN_POINT('Ctrl Pts',(0.227513576082652,0.0397451814080778,
0.899513760960216));
#10904=CARTESIAN_POINT('Ctrl Pts',(0.0899808947771051,0.212710002872901,
0.910628473841993));
#10905=CARTESIAN_POINT('Ctrl Pts',(-0.129924857834439,0.190949307576065,
0.921743186723768));
#10906=CARTESIAN_POINT('Ctrl Pts',(-0.230890810999347,-0.00561606117680894,
0.932857899605545));
#10907=CARTESIAN_POINT('Ctrl Pts',(-0.120487614241242,-0.197040202906745,
0.943972612487321));
#10908=CARTESIAN_POINT('Ctrl Pts',(0.100216050899275,-0.208083756908682,
0.955087325369097));
#10909=CARTESIAN_POINT('Ctrl Pts',(0.229176864102385,-0.0286368941625087,
0.966202038250873));
#10910=CARTESIAN_POINT('Ctrl Pts',(0.148337561234701,0.177025632816322,
0.97731675113265));
#10911=CARTESIAN_POINT('Ctrl Pts',(-0.0682974629270641,0.220629923865291,
0.988431464014425));
#10912=CARTESIAN_POINT('Ctrl Pts',(-0.22240952821355,0.0622584010949852,
0.999546176896202));
#10913=CARTESIAN_POINT('Ctrl Pts',(-0.17291663967011,-0.153107617290177,
1.01066088977798));
#10914=CARTESIAN_POINT('Ctrl Pts',(0.0348729042335921,-0.228311163321885,
1.02177560265975));
#10915=CARTESIAN_POINT('Ctrl Pts',(0.210738024244903,-0.0945070996509389,
1.03289031554153));
#10916=CARTESIAN_POINT('Ctrl Pts',(0.193682876670397,0.125813552655338,
1.04400502842331));
#10917=CARTESIAN_POINT('Ctrl Pts',(-0.000679392046237043,0.230958102636658,
1.05511974130508));
#10918=CARTESIAN_POINT('Ctrl Pts',(-0.194419710852192,0.124671900519835,
1.06623445418686));
#10919=CARTESIAN_POINT('Ctrl Pts',(-0.210178373163287,-0.095745277698235,
1.07734916706864));
#10920=CARTESIAN_POINT('Ctrl Pts',(-0.0335291008517639,-0.22851237634568,
1.08846387995041));
#10921=CARTESIAN_POINT('Ctrl Pts',(0.173814409632538,-0.152087664691026,
1.09957859283219));
#10922=CARTESIAN_POINT('Ctrl Pts',(0.222039400634039,0.0635658030166745,
1.11069330571397));
#10923=CARTESIAN_POINT('Ctrl Pts',(0.0669982713499448,0.221027913131344,
1.12180801859574));
#10924=CARTESIAN_POINT('Ctrl Pts',(-0.149376470996772,0.176149869882519,
1.13292273147752));
#10925=CARTESIAN_POINT('Ctrl Pts',(-0.229004421401316,-0.0299846915229451,
1.14403744435929));
#10926=CARTESIAN_POINT('Ctrl Pts',(-0.0989901185230116,-0.208669746685709,
1.15515215724107));
#10927=CARTESIAN_POINT('Ctrl Pts',(0.121644755665281,-0.196327940360541,
1.16626687012285));
#10928=CARTESIAN_POINT('Ctrl Pts',(0.230919855567728,-0.00425758753959744,
1.17738158300462));
#10929=CARTESIAN_POINT('Ctrl Pts',(0.12879921667729,0.191710376689407,1.1884962958864));
#10930=CARTESIAN_POINT('Ctrl Pts',(-0.0912307526970952,0.212176946225077,
1.19961100876817));
#10931=CARTESIAN_POINT('Ctrl Pts',(-0.227743467482791,0.0384059860697885,
1.21072572164995));
#10932=CARTESIAN_POINT('Ctrl Pts',(-0.155768270107734,-0.170523760147147,
1.22184043453172));
#10933=CARTESIAN_POINT('Ctrl Pts',(0.0588050960517139,-0.22334741419015,
1.2329551474135));
#10934=CARTESIAN_POINT('Ctrl Pts',(0.219545297046235,-0.071707526048235,
1.24406986029528));
#10935=CARTESIAN_POINT('Ctrl Pts',(0.179302606580475,0.145577065571899,
1.25518457317705));
#10936=CARTESIAN_POINT('Ctrl Pts',(-0.0250827769957638,0.229593033529458,
1.26629928605883));
#10937=CARTESIAN_POINT('Ctrl Pts',(-0.206506115316257,0.103427902831233,
1.27741399894061));
#10938=CARTESIAN_POINT('Ctrl Pts',(-0.198883289957136,-0.1174203718394,
1.28852871182238));
#10939=CARTESIAN_POINT('Ctrl Pts',(-0.00919262157653787,-0.23077608726995,
1.29964342470416));
#10940=CARTESIAN_POINT('Ctrl Pts',(0.188913438476804,-0.132867676693576,
1.31075813758593));
#10941=CARTESIAN_POINT('Ctrl Pts',(0.214078562825313,0.0866745388549966,
1.32187285046771));
#10942=CARTESIAN_POINT('Ctrl Pts',(0.0432653212731772,0.226870488874615,
1.33298756334948));
#10943=CARTESIAN_POINT('Ctrl Pts',(-0.167155188056641,0.159377695593915,
1.34410227623126));
#10944=CARTESIAN_POINT('Ctrl Pts',(-0.224553366823233,-0.0540175174867204,
1.35521698911304));
#10945=CARTESIAN_POINT('Ctrl Pts',(-0.0763840132469668,-0.217962357455055,
1.36633170199482));
#10946=CARTESIAN_POINT('Ctrl Pts',(0.141711137193365,-0.182373409088171,
1.37744641487659));
#10947=CARTESIAN_POINT('Ctrl Pts',(0.230076730733878,0.020169400632847,
1.38856112775837));
#10948=CARTESIAN_POINT('Ctrl Pts',(0.107818424683935,0.204248118830388,
1.39967584064014));
#10949=CARTESIAN_POINT('Ctrl Pts',(-0.113142331553799,0.201347757766626,
1.41079055352192));
#10950=CARTESIAN_POINT('Ctrl Pts',(-0.230526863439747,0.0141234549494752,
1.4219052664037));
#10951=CARTESIAN_POINT('Ctrl Pts',(-0.136875421443584,-0.186030174304383,
1.43301997928547));
#10952=CARTESIAN_POINT('Ctrl Pts',(0.0820787181812268,-0.215882354000517,
1.44413469216725));
#10953=CARTESIAN_POINT('Ctrl Pts',(0.225893839437804,-0.048104885938183,
1.45524940504902));
#10954=CARTESIAN_POINT('Ctrl Pts',(0.162914291785062,0.163710232665064,
1.4663641179308));
#10955=CARTESIAN_POINT('Ctrl Pts',(-0.0492052550555011,0.225656707460693,
1.47747883081258));
#10956=CARTESIAN_POINT('Ctrl Pts',(-0.21627981769851,0.0810255959766872,
1.48859354369435));
#10957=CARTESIAN_POINT('Ctrl Pts',(-0.185360874170467,-0.137780452437339,
1.49970825657613));
#10958=CARTESIAN_POINT('Ctrl Pts',(0.0152468076526161,-0.230455291984111,
1.51082296945791));
#10959=CARTESIAN_POINT('Ctrl Pts',(0.201896789043082,-0.112159677786499,
1.52193768233968));
#10960=CARTESIAN_POINT('Ctrl Pts',(0.203720217624815,0.108812589703471,
1.53305239522146));
#10961=CARTESIAN_POINT('Ctrl Pts',(0.0190478344628315,0.230172297962536,
1.54416710810323));
#10962=CARTESIAN_POINT('Ctrl Pts',(-0.18306190170968,0.140820619546688,
1.55528182098501));
#10963=CARTESIAN_POINT('Ctrl Pts',(-0.217587495489559,-0.0774453907838218,
1.56639653386679));
#10964=CARTESIAN_POINT('Ctrl Pts',(-0.0529224685754187,-0.224813965462472,
1.57751124674856));
#10965=CARTESIAN_POINT('Ctrl Pts',(0.160190468180596,-0.166376442596779,
1.58862595963034));
#10966=CARTESIAN_POINT('Ctrl Pts',(0.226656931919555,0.0443705077714034,
1.59974067251212));
#10967=CARTESIAN_POINT('Ctrl Pts',(0.0856301532179132,0.214498446630633,
1.61085538539389));
#10968=CARTESIAN_POINT('Ctrl Pts',(-0.133786807471087,0.188263636674139,
1.62197009827567));
#10969=CARTESIAN_POINT('Ctrl Pts',(-0.230728544292657,-0.0103172474851095,
1.63308481115744));
#10970=CARTESIAN_POINT('Ctrl Pts',(-0.116449678358188,-0.199453200418927,
1.64419952403922));
#10971=CARTESIAN_POINT('Ctrl Pts',(0.104433124808968,-0.205999585411506,
1.655314236921));
#10972=CARTESIAN_POINT('Ctrl Pts',(0.229712552860698,-0.0239635098701923,
1.66642894980277));
#10973=CARTESIAN_POINT('Ctrl Pts',(0.144701468203596,0.180009977075721,
1.67754366268455));
#10974=CARTESIAN_POINT('Ctrl Pts',(-0.0727766739099085,0.219193208110308,
1.68865837556633));
#10975=CARTESIAN_POINT('Ctrl Pts',(-0.22363136040826,0.0577158677404108,
1.6997730884481));
#10976=CARTESIAN_POINT('Ctrl Pts',(-0.169762565963256,-0.156597502996213,
1.71088780132988));
#10977=CARTESIAN_POINT('Ctrl Pts',(0.039515484922465,-0.227553583136852,
1.72200251421165));
#10978=CARTESIAN_POINT('Ctrl Pts',(0.212619058267456,-0.0901955808703403,
1.73311722709343));
#10979=CARTESIAN_POINT('Ctrl Pts',(0.191080370151679,0.129732027232196,
1.7442319399752));
#10980=CARTESIAN_POINT('Ctrl Pts',(-0.00538297274409746,0.230896362794034,
1.75534665285698));
#10981=CARTESIAN_POINT('Ctrl Pts',(-0.19691846958115,0.120686466038639,
1.76646136573876));
#10982=CARTESIAN_POINT('Ctrl Pts',(-0.208184819545892,-0.100005938112305,
1.77757607862054));
#10983=CARTESIAN_POINT('Ctrl Pts',(-0.0288682349025721,-0.229147838219538,
1.78869079150231));
#10984=CARTESIAN_POINT('Ctrl Pts',(0.176875795011193,-0.148516194020166,
1.79980550438409));
#10985=CARTESIAN_POINT('Ctrl Pts',(0.220698758115687,0.0680747009781974,
1.81092021726586));
#10986=CARTESIAN_POINT('Ctrl Pts',(0.0624828930395807,0.222346564678841,
1.82203493014764));
#10987=CARTESIAN_POINT('Ctrl Pts',(-0.152932978954706,0.173071114560221,
1.83314964302941));
#10988=CARTESIAN_POINT('Ctrl Pts',(-0.22834625137849,-0.0346424050618476,
1.84426435591119));
#10989=CARTESIAN_POINT('Ctrl Pts',(-0.094719792714343,-0.210642511415027,
1.85537906879297));
#10990=CARTESIAN_POINT('Ctrl Pts',(0.125617964594648,-0.193809787467443,
1.86649378167474));
#10991=CARTESIAN_POINT('Ctrl Pts',(0.230958670801831,0.000446238197717259,
1.87760849455652));
#10992=CARTESIAN_POINT('Ctrl Pts',(0.124868104783677,0.194293754801359,
1.88872320743829));
#10993=CARTESIAN_POINT('Ctrl Pts',(-0.095533052662467,0.210274921462518,
1.89983792032007));
#10994=CARTESIAN_POINT('Ctrl Pts',(-0.228478412091282,0.0337597682948806,
1.91095263320185));
#10995=CARTESIAN_POINT('Ctrl Pts',(-0.152263053817779,-0.17366078771318,
1.92206734608362));
#10996=CARTESIAN_POINT('Ctrl Pts',(0.0633416206041145,-0.222103457528968,
1.9331820589654));
#10997=CARTESIAN_POINT('Ctrl Pts',(0.220960165374983,-0.0672213661311443,
1.94429677184717));
#10998=CARTESIAN_POINT('Ctrl Pts',(0.176300576511988,0.149198570598448,
1.95541148472895));
#10999=CARTESIAN_POINT('Ctrl Pts',(-0.0297534949940769,0.229034574426469,
1.96652619761073));
#11000=CARTESIAN_POINT('Ctrl Pts',(-0.208569709276974,0.0992007213642766,
1.97764091049251));
#11001=CARTESIAN_POINT('Ctrl Pts',(-0.196450641385828,-0.121446499522165,
1.98875562337428));
#11002=CARTESIAN_POINT('Ctrl Pts',(-0.00449070026179651,-0.230915439843731,
1.99987033625606));
#11003=CARTESIAN_POINT('Ctrl Pts',(0.191580255470184,-0.128992683750042,
2.01098504913783));
#11004=CARTESIAN_POINT('Ctrl Pts',(0.212268936067735,0.091016512391074,
2.02209976201961));
#11005=CARTESIAN_POINT('Ctrl Pts',(0.0386358748097637,0.227704580376973,
2.03321447490139));
#11006=CARTESIAN_POINT('Ctrl Pts',(-0.170366424312123,0.155940335430241,
2.04432918778316));
#11007=CARTESIAN_POINT('Ctrl Pts',(-0.223406664459236,-0.05857959561862,
2.05544390066494));
#11008=CARTESIAN_POINT('Ctrl Pts',(-0.0719291217184943,-0.219472796024974,
2.06655861354672));
#11009=CARTESIAN_POINT('Ctrl Pts',(0.145395984400223,-0.179449476084793,
2.07767332642849));
#11010=CARTESIAN_POINT('Ctrl Pts',(0.229618237751902,0.0248509887620852,
2.08878803931027));
#11011=CARTESIAN_POINT('Ctrl Pts',(0.103636319198972,0.20640159903293,2.09990275219204));
#11012=CARTESIAN_POINT('Ctrl Pts',(-0.117219538181985,0.199001725158021,
2.11101746507382));
#11013=CARTESIAN_POINT('Ctrl Pts',(-0.230766689726102,0.00942558661705901,
2.1221321779556));
#11014=CARTESIAN_POINT('Ctrl Pts',(-0.133058318070465,-0.188779211488415,
2.13324689083737));
#11015=CARTESIAN_POINT('Ctrl Pts',(0.0864583809916643,-0.214165952291765,
2.14436160371915));
#11016=CARTESIAN_POINT('Ctrl Pts',(0.22682669704182,-0.043494326039136,
2.15547631660092));
#11017=CARTESIAN_POINT('Ctrl Pts',(0.159546357810628,0.166994209782124,
2.1665910294827));
#11018=CARTESIAN_POINT('Ctrl Pts',(-0.0537908007947409,0.224607784190559,
2.17770574236448));
#11019=CARTESIAN_POINT('Ctrl Pts',(-0.21788513873988,0.0766040070256843,
2.18882045524625));
#11020=CARTESIAN_POINT('Ctrl Pts',(-0.182516369710472,-0.141526955103469,
2.19993516812803));
#11021=CARTESIAN_POINT('Ctrl Pts',(0.0199371177794038,-0.230096980137356,
2.2110498810098));
#11022=CARTESIAN_POINT('Ctrl Pts',(0.204139188235331,-0.108024548875401,
2.22216459389158));
#11023=CARTESIAN_POINT('Ctrl Pts',(0.201461841058376,0.112938992248027,
2.23327930677336));
#11024=CARTESIAN_POINT('Ctrl Pts',(0.0143562266588113,0.230512526239688,
2.24439401965513));
#11025=CARTESIAN_POINT('Ctrl Pts',(-0.185892018555318,0.137063077970044,
2.25550873253691));
#11026=CARTESIAN_POINT('Ctrl Pts',(-0.215964883113702,-0.0818606044959991,
2.26662344541869));
#11027=CARTESIAN_POINT('Ctrl Pts',(-0.0483333206738901,-0.225845423581302,
2.27773815830046));
#11028=CARTESIAN_POINT('Ctrl Pts',(0.16354648179728,-0.163078977908128,
2.28885287118224));
#11029=CARTESIAN_POINT('Ctrl Pts',(0.225704752281254,0.048976482321738,
2.29996758406402));
#11030=CARTESIAN_POINT('Ctrl Pts',(0.0812467689117343,0.216199711180548,
2.31108229694579));
#11031=CARTESIAN_POINT('Ctrl Pts',(-0.137598735282772,0.185496446675884,
2.32219700982757));
#11032=CARTESIAN_POINT('Ctrl Pts',(-0.230460149011143,-0.0150076418454517,
2.33331172270934));
#11033=CARTESIAN_POINT('Ctrl Pts',(-0.112383257382243,-0.201795849986241,
2.34442643559112));
#11034=CARTESIAN_POINT('Ctrl Pts',(0.108644616799776,-0.203806378129441,
2.3555411484729));
#11035=CARTESIAN_POINT('Ctrl Pts',(0.230080867601931,-0.0193251643494075,
2.36665586135467));
#11036=CARTESIAN_POINT('Ctrl Pts',(0.141144990674285,0.18300622889355,2.37777057423645));
#11037=CARTESIAN_POINT('Ctrl Pts',(-0.0775128162224814,0.217492107202628,
2.38888528711823));
#11038=CARTESIAN_POINT('Ctrl Pts',(-0.175202059751607,0.108202911730689,
2.39629509570607));
#11039=CARTESIAN_POINT('Ctrl Pts',(-0.190155688860645,0.0449663651403318,
2.4));
#11040=CARTESIAN_POINT('Ctrl Pts',(0.105793541951255,-0.148236995244729,
-0.0153382721514711));
#11041=CARTESIAN_POINT('Ctrl Pts',(0.155089966961593,-0.11305520139652,
-0.0116333678575457));
#11042=CARTESIAN_POINT('Ctrl Pts',(0.21497519937743,0.00974117628248662,
-0.0042235592696949));
#11043=CARTESIAN_POINT('Ctrl Pts',(0.108183370830488,0.186264075098343,
0.00689115361208128));
#11044=CARTESIAN_POINT('Ctrl Pts',(-0.0977345970672646,0.191720735194958,
0.0180058664938575));
#11045=CARTESIAN_POINT('Ctrl Pts',(-0.214134249288,0.0219430288774403,0.0291205793756336));
#11046=CARTESIAN_POINT('Ctrl Pts',(-0.134529329353402,-0.168066279567892,
0.0402352922574098));
#11047=CARTESIAN_POINT('Ctrl Pts',(0.0682435794252791,-0.204143760009197,
0.0513500051391861));
#11048=CARTESIAN_POINT('Ctrl Pts',(0.208536011121689,-0.0533773322081568,
0.0624647180209621));
#11049=CARTESIAN_POINT('Ctrl Pts',(0.15792760839081,0.146274243875976,0.0735794309027384));
#11050=CARTESIAN_POINT('Ctrl Pts',(-0.0372576226080993,0.212008012654093,
0.0846941437845145));
#11051=CARTESIAN_POINT('Ctrl Pts',(-0.19833434318746,0.083664658915774,
0.0958088566662907));
#11052=CARTESIAN_POINT('Ctrl Pts',(-0.177846277209918,-0.121272589946413,
0.106923569548067));
#11053=CARTESIAN_POINT('Ctrl Pts',(0.00545155897490425,-0.215189173059631,
0.118038282429843));
#11054=CARTESIAN_POINT('Ctrl Pts',(0.183758617328128,-0.112111517639152,
0.129152995311619));
#11055=CARTESIAN_POINT('Ctrl Pts',(0.193843800442202,0.0935991424382365,
0.140267708193395));
#11056=CARTESIAN_POINT('Ctrl Pts',(0.0264745047177667,0.213624172837712,
0.151382421075172));
#11057=CARTESIAN_POINT('Ctrl Pts',(-0.16513087336672,0.138086930438782,
0.162497133956948));
#11058=CARTESIAN_POINT('Ctrl Pts',(-0.205567092178708,-0.0638621501811345,
0.173611846838724));
#11059=CARTESIAN_POINT('Ctrl Pts',(-0.0578167708818694,-0.207348548425574,
0.1847265597205));
#11060=CARTESIAN_POINT('Ctrl Pts',(0.142861949582761,-0.161017594674284,
0.195841272602276));
#11061=CARTESIAN_POINT('Ctrl Pts',(0.212757602765681,0.0327170348815519,
0.206955985484052));
#11062=CARTESIAN_POINT('Ctrl Pts',(0.0878841629903467,0.196500827732778,
0.218070698365829));
#11063=CARTESIAN_POINT('Ctrl Pts',(-0.117442893108306,0.180397806789189,
0.229185411247605));
#11064=CARTESIAN_POINT('Ctrl Pts',(-0.215256773088726,-0.000850510388162502,
0.240300124129381));
#11065=CARTESIAN_POINT('Ctrl Pts',(-0.11601369365937,-0.181320226543997,
0.251414837011157));
#11066=CARTESIAN_POINT('Ctrl Pts',(0.0894342004493663,-0.195800218394246,
0.262529549892933));
#11067=CARTESIAN_POINT('Ctrl Pts',(0.213009494979972,-0.0310347669858385,
0.27364426277471));
#11068=CARTESIAN_POINT('Ctrl Pts',(0.141585102478085,0.16214148285887,0.284758975656486));
#11069=CARTESIAN_POINT('Ctrl Pts',(-0.0594534683484756,0.206885202026802,
0.295873688538262));
#11070=CARTESIAN_POINT('Ctrl Pts',(-0.206065321155091,0.0622357222997597,
0.306988401420038));
#11071=CARTESIAN_POINT('Ctrl Pts',(-0.16403453559407,-0.139387491708681,
0.318103114301814));
#11072=CARTESIAN_POINT('Ctrl Pts',(0.0281617771100779,-0.213408331664074,
0.329217827183591));
#11073=CARTESIAN_POINT('Ctrl Pts',(0.194577371810986,-0.0920643692869703,
0.340332540065367));
#11074=CARTESIAN_POINT('Ctrl Pts',(0.182866979184729,0.113559982550668,
0.351447252947143));
#11075=CARTESIAN_POINT('Ctrl Pts',(0.00375088612404077,0.215225771148598,
0.362561965828919));
#11076=CARTESIAN_POINT('Ctrl Pts',(-0.17879895818941,0.119862981205691,
0.373676678710695));
#11077=CARTESIAN_POINT('Ctrl Pts',(-0.197667174654384,-0.0852284563822003,
0.384791391592471));
#11078=CARTESIAN_POINT('Ctrl Pts',(-0.0355808416787025,-0.212297445624285,
0.395906104474247));
#11079=CARTESIAN_POINT('Ctrl Pts',(0.159077997004871,-0.145018593918386,
0.407020817356024));
#11080=CARTESIAN_POINT('Ctrl Pts',(0.20810877516562,0.0550176281951035,
0.4181355302378));
#11081=CARTESIAN_POINT('Ctrl Pts',(0.0666262335979379,0.204687925168304,
0.429250243119576));
#11082=CARTESIAN_POINT('Ctrl Pts',(-0.135849338819328,0.166976521869098,
0.440364956001352));
#11083=CARTESIAN_POINT('Ctrl Pts',(-0.213961541644003,-0.0235936519104577,
0.451479668883129));
#11084=CARTESIAN_POINT('Ctrl Pts',(-0.0962025056880325,-0.19256500100614,
0.462594381764904));
#11085=CARTESIAN_POINT('Ctrl Pts',(0.109625179512714,-0.185252588996634,
0.473709094646681));
#11086=CARTESIAN_POINT('Ctrl Pts',(0.215096419589165,-0.00835056842810073,
0.484823807528457));
#11087=CARTESIAN_POINT('Ctrl Pts',(0.123657496098414,0.176195985685887,
0.495938520410233));
#11088=CARTESIAN_POINT('Ctrl Pts',(-0.0809837662762514,0.199443804899686,
0.507053233292009));
#11089=CARTESIAN_POINT('Ctrl Pts',(-0.211488384748603,0.0401106573067252,
0.518167946173785));
#11090=CARTESIAN_POINT('Ctrl Pts',(-0.148385817601819,-0.155941818790824,
0.529282659055562));
#11091=CARTESIAN_POINT('Ctrl Pts',(0.0505566471631337,-0.209237250844042,
0.540397371937337));
#11092=CARTESIAN_POINT('Ctrl Pts',(0.203216994906723,-0.0709862993417115,
0.551512084819114));
#11093=CARTESIAN_POINT('Ctrl Pts',(0.169842206486041,0.132249108159955,
0.56262679770089));
#11094=CARTESIAN_POINT('Ctrl Pts',(-0.0190147453460938,0.214416979674124,
0.573741510582666));
#11095=CARTESIAN_POINT('Ctrl Pts',(-0.190464635622116,0.100296681353299,
0.584856223464443));
#11096=CARTESIAN_POINT('Ctrl Pts',(-0.187553545711894,-0.105640282108895,
0.595970936346219));
#11097=CARTESIAN_POINT('Ctrl Pts',(-0.0129464348531298,-0.214868777484641,
0.607085649227995));
#11098=CARTESIAN_POINT('Ctrl Pts',(0.17351249859483,-0.127395504412556,
0.618200362109772));
#11099=CARTESIAN_POINT('Ctrl Pts',(0.20112929722474,0.0767020697962746,
0.629315074991546));
#11100=CARTESIAN_POINT('Ctrl Pts',(0.044622143952873,0.210582682056715,
0.640429787873325));
#11101=CARTESIAN_POINT('Ctrl Pts',(-0.152734381341373,0.15168523484314,
0.651544500755098));
#11102=CARTESIAN_POINT('Ctrl Pts',(-0.210270113385278,-0.0460725637456039,
0.662659213636877));
#11103=CARTESIAN_POINT('Ctrl Pts',(-0.0753139271579653,-0.201653202526504,
0.673773926518651));
#11104=CARTESIAN_POINT('Ctrl Pts',(0.128588444895634,-0.172630279940899,
0.684888639400429));
#11105=CARTESIAN_POINT('Ctrl Pts',(0.214774437636115,0.0144271497961512,
0.696003352282204));
#11106=CARTESIAN_POINT('Ctrl Pts',(0.104345025407248,0.188277235442608,
0.70711806516398));
#11107=CARTESIAN_POINT('Ctrl Pts',(-0.101607111279838,0.189768797884471,
0.718232778045757));
#11108=CARTESIAN_POINT('Ctrl Pts',(-0.214542948858282,0.0175363852701505,
0.729347490927533));
#11109=CARTESIAN_POINT('Ctrl Pts',(-0.131075298026442,-0.170749723163553,
0.740462203809309));
#11110=CARTESIAN_POINT('Ctrl Pts',(0.0723853235080425,-0.202722881426312,
0.751576916691085));
#11111=CARTESIAN_POINT('Ctrl Pts',(0.20958075141886,-0.0491132400464108,
0.762691629572862));
#11112=CARTESIAN_POINT('Ctrl Pts',(0.154915337939347,0.149457150328408,
0.773806342454638));
#11113=CARTESIAN_POINT('Ctrl Pts',(-0.0415674269910586,0.211206890812051,
0.784921055336414));
#11114=CARTESIAN_POINT('Ctrl Pts',(-0.199997262618826,0.0796071394921763,
0.79603576821819));
#11115=CARTESIAN_POINT('Ctrl Pts',(-0.175339468194524,-0.124869021804497,
0.807150481099967));
#11116=CARTESIAN_POINT('Ctrl Pts',(0.00983296161011095,-0.215033752185848,
0.818265193981742));
#11117=CARTESIAN_POINT('Ctrl Pts',(0.186003800022871,-0.108345687916974,
0.829379906863519));
#11118=CARTESIAN_POINT('Ctrl Pts',(0.191897333231851,0.0975275100248876,
0.840494619745294));
#11119=CARTESIAN_POINT('Ctrl Pts',(0.0221183222535954,0.214119082600866,
0.851609332627072));
#11120=CARTESIAN_POINT('Ctrl Pts',(-0.167908921871014,0.134695195420119,
0.862724045508846));
#11121=CARTESIAN_POINT('Ctrl Pts',(-0.204223829299531,-0.0680354999936554,
0.873838758390623));
#11122=CARTESIAN_POINT('Ctrl Pts',(-0.0535818933342823,-0.208483050677661,
0.884953471272399));
#11123=CARTESIAN_POINT('Ctrl Pts',(0.146111623316715,-0.158074650861245,
0.896068184154176));
#11124=CARTESIAN_POINT('Ctrl Pts',(0.212047155054175,0.0370432955685794,
0.907182897035951));
#11125=CARTESIAN_POINT('Ctrl Pts',(0.083863974516331,0.198249931882648,
0.918297609917728));
#11126=CARTESIAN_POINT('Ctrl Pts',(-0.121092538515599,0.177968533255176,
0.929412322799505));
#11127=CARTESIAN_POINT('Ctrl Pts',(-0.21519480482684,-0.00523428015002993,
0.940527035681279));
#11128=CARTESIAN_POINT('Ctrl Pts',(-0.112296840738152,-0.183645368232854,
0.951641748563058));
#11129=CARTESIAN_POINT('Ctrl Pts',(0.0934033425602478,-0.193938179097679,
0.962756461444831));
#11130=CARTESIAN_POINT('Ctrl Pts',(0.213597372402487,-0.0266901520397281,
0.97387117432661));
#11131=CARTESIAN_POINT('Ctrl Pts',(0.138253542443842,0.164991392850898,
0.984985887208384));
#11132=CARTESIAN_POINT('Ctrl Pts',(-0.0636545869501867,0.205631454970663,
0.996100600090161));
#11133=CARTESIAN_POINT('Ctrl Pts',(-0.207290081438881,0.0580260618189137,
1.00721531297194));
#11134=CARTESIAN_POINT('Ctrl Pts',(-0.161161729927952,-0.142699329079643,
1.01833002585371));
#11135=CARTESIAN_POINT('Ctrl Pts',(0.0325022368270573,-0.21279052214417,
1.02944473873549));
#11136=CARTESIAN_POINT('Ctrl Pts',(0.196412008778918,-0.0880824870254049,
1.04055945161727));
#11137=CARTESIAN_POINT('Ctrl Pts',(0.180516273744238,0.117260720732245,
1.05167416449904));
#11138=CARTESIAN_POINT('Ctrl Pts',(-0.000633206831217092,0.215257521964412,
1.06278887738082));
#11139=CARTESIAN_POINT('Ctrl Pts',(-0.181203017782488,0.116196678350416,
1.0739035902626));
#11140=CARTESIAN_POINT('Ctrl Pts',(-0.195890402896217,-0.089236493467125,
1.08501830314437));
#11141=CARTESIAN_POINT('Ctrl Pts',(-0.03124978548339,-0.212978056664043,
1.09613301602615));
#11142=CARTESIAN_POINT('Ctrl Pts',(0.161998469298423,-0.14174871307394,
1.10724772890792));
#11143=CARTESIAN_POINT('Ctrl Pts',(0.206945115210521,0.0592445862814022,
1.1183624417897));
#11144=CARTESIAN_POINT('Ctrl Pts',(0.0624437146913072,0.20600238884222,
1.12947715467148));
#11145=CARTESIAN_POINT('Ctrl Pts',(-0.13922182690052,0.164175164466591,
1.14059186755325));
#11146=CARTESIAN_POINT('Ctrl Pts',(-0.213436652392715,-0.0279463258504929,
1.15170658043503));
#11147=CARTESIAN_POINT('Ctrl Pts',(-0.0922607493262528,-0.194484333165705,
1.1628212933168));
#11148=CARTESIAN_POINT('Ctrl Pts',(0.113375319443406,-0.182981525445211,
1.17393600619858));
#11149=CARTESIAN_POINT('Ctrl Pts',(0.215221874939318,-0.00396815583804349,
1.18505071908036));
#11150=CARTESIAN_POINT('Ctrl Pts',(0.120043418682428,0.178677864729199,
1.19616543196213));
#11151=CARTESIAN_POINT('Ctrl Pts',(-0.0850288668305293,0.197753112538505,
1.20728014484391));
#11152=CARTESIAN_POINT('Ctrl Pts',(-0.212261418388302,0.0357951390126765,
1.21839485772569));
#11153=CARTESIAN_POINT('Ctrl Pts',(-0.145179110155855,-0.158931518861127,
1.22950957060746));
#11154=CARTESIAN_POINT('Ctrl Pts',(0.0548075131829614,-0.208164209728402,
1.24062428348924));
#11155=CARTESIAN_POINT('Ctrl Pts',(0.204620561312197,-0.0668328332590501,
1.25173899637101));
#11156=CARTESIAN_POINT('Ctrl Pts',(0.167113577456916,0.135680705860126,
1.26285370925279));
#11157=CARTESIAN_POINT('Ctrl Pts',(-0.0233776445097808,0.213985250543875,
1.27396842213457));
#11158=CARTESIAN_POINT('Ctrl Pts',(-0.192467785914425,0.0963968521184676,
1.28508313501634));
#11159=CARTESIAN_POINT('Ctrl Pts',(-0.185363161835691,-0.1094381101236,
1.29619784789812));
#11160=CARTESIAN_POINT('Ctrl Pts',(-0.00856770521723566,-0.215087880040835,
1.30731256077989));
#11161=CARTESIAN_POINT('Ctrl Pts',(0.17607106296793,-0.123835303926197,
1.31842727366167));
#11162=CARTESIAN_POINT('Ctrl Pts',(0.199525456840005,0.0807823853692007,
1.32954198654345));
#11163=CARTESIAN_POINT('Ctrl Pts',(0.0403241355810343,0.211447785050572,
1.34065669942522));
#11164=CARTESIAN_POINT('Ctrl Pts',(-0.155791943013894,0.148543166133976,
1.351771412307));
#11165=CARTESIAN_POINT('Ctrl Pts',(-0.209288181446391,-0.0503453952215415,
1.36288612518877));
#11166=CARTESIAN_POINT('Ctrl Pts',(-0.0711914118687858,-0.203145230289267,
1.37400083807055));
#11167=CARTESIAN_POINT('Ctrl Pts',(0.132077584110531,-0.169975626160565,
1.38511555095233));
#11168=CARTESIAN_POINT('Ctrl Pts',(0.214436065910022,0.0187982805113507,
1.39623026383411));
#11169=CARTESIAN_POINT('Ctrl Pts',(0.100488905366888,0.190363288507304,
1.40734497671588));
#11170=CARTESIAN_POINT('Ctrl Pts',(-0.105450891921556,0.187660094602179,
1.41845968959766));
#11171=CARTESIAN_POINT('Ctrl Pts',(-0.214855598499328,0.0131633394944521,
1.42957440247943));
#11172=CARTESIAN_POINT('Ctrl Pts',(-0.127570601340334,-0.173383803703852,
1.44068911536121));
#11173=CARTESIAN_POINT('Ctrl Pts',(0.0764989895569963,-0.201206625909559,
1.45180382824298));
#11174=CARTESIAN_POINT('Ctrl Pts',(0.210537528449068,-0.0448347056163908,
1.46291854112476));
#11175=CARTESIAN_POINT('Ctrl Pts',(0.151839343767946,0.152581176418554,
1.47403325400654));
#11176=CARTESIAN_POINT('Ctrl Pts',(-0.0458602714083437,0.210316516753924,
1.48514796688831));
#11177=CARTESIAN_POINT('Ctrl Pts',(-0.201577069941283,0.0755174588226969,
1.49626267977009));
#11178=CARTESIAN_POINT('Ctrl Pts',(-0.172760002734623,-0.128414108135685,
1.50737739265187));
#11179=CARTESIAN_POINT('Ctrl Pts',(0.0142103264432017,-0.214788892486386,
1.51849210553364));
#11180=CARTESIAN_POINT('Ctrl Pts',(0.18817180261632,-0.104535039165226,
1.52960681841542));
#11181=CARTESIAN_POINT('Ctrl Pts',(0.189871274137357,0.101415486838092,
1.54072153129719));
#11182=CARTESIAN_POINT('Ctrl Pts',(0.0177529586468273,0.214525136458259,
1.55183624417897));
#11183=CARTESIAN_POINT('Ctrl Pts',(-0.170617314908023,0.131247604041854,
1.56295095706075));
#11184=CARTESIAN_POINT('Ctrl Pts',(-0.202795851519484,-0.0721806367361637,
1.57406566994252));
#11185=CARTESIAN_POINT('Ctrl Pts',(-0.049324787966875,-0.209531064535007,
1.5851803828243));
#11186=CARTESIAN_POINT('Ctrl Pts',(0.149300686268282,-0.155066136835127,
1.59629509570608));
#11187=CARTESIAN_POINT('Ctrl Pts',(0.211248745742492,0.0413541912673223,
1.60740980858785));
#11188=CARTESIAN_POINT('Ctrl Pts',(0.0798089972886537,0.199916796855417,
1.61852452146963));
#11189=CARTESIAN_POINT('Ctrl Pts',(-0.124691951999022,0.175465434829268,
1.6296392343514));
#11190=CARTESIAN_POINT('Ctrl Pts',(-0.215043569045195,-0.00961587881864149,
1.64075394723318));
#11191=CARTESIAN_POINT('Ctrl Pts',(-0.108533404590579,-0.185894329663731,
1.65186866011496));
#11192=CARTESIAN_POINT('Ctrl Pts',(0.0973337388935138,-0.19199569001975,
1.66298337299673));
#11193=CARTESIAN_POINT('Ctrl Pts',(0.214096644925695,-0.0223344654001731,
1.67409808587851));
#11194=CARTESIAN_POINT('Ctrl Pts',(0.134864631786142,0.167772860756258,
1.68521279876028));
#11195=CARTESIAN_POINT('Ctrl Pts',(-0.0678293002229216,0.204292407456614,
1.69632751164206));
#11196=CARTESIAN_POINT('Ctrl Pts',(-0.208428853222539,0.0537923308426739,
1.70744222452384));
#11197=CARTESIAN_POINT('Ctrl Pts',(-0.158222070818878,-0.14595197161716,
1.71855693740561));
#11198=CARTESIAN_POINT('Ctrl Pts',(0.0368292138986469,-0.212084442420368,
1.72967165028739));
#11199=CARTESIAN_POINT('Ctrl Pts',(0.198165169710719,-0.0840640662035352,
1.74078636316916));
#11200=CARTESIAN_POINT('Ctrl Pts',(0.178090686169176,0.120912816578486,
1.75190107605094));
#11201=CARTESIAN_POINT('Ctrl Pts',(-0.00501703711827952,0.215199979209349,
1.76301578893272));
#11202=CARTESIAN_POINT('Ctrl Pts',(-0.183531910364484,0.112482174548297,
1.77413050181449));
#11203=CARTESIAN_POINT('Ctrl Pts',(-0.194032371475433,-0.0932075132849812,
1.78524521469627));
#11204=CARTESIAN_POINT('Ctrl Pts',(-0.0269057661873462,-0.213570319705296,
1.79635992757805));
#11205=CARTESIAN_POINT('Ctrl Pts',(0.164851741051457,-0.138420031734765,
1.80747464045982));
#11206=CARTESIAN_POINT('Ctrl Pts',(0.205695609854155,0.0634469684057254,
1.8185893533416));
#11207=CARTESIAN_POINT('Ctrl Pts',(0.0582352927536283,0.207231398178581,
1.82970406622338));
#11208=CARTESIAN_POINT('Ctrl Pts',(-0.142536562695159,0.161305703582358,
1.84081877910515));
#11209=CARTESIAN_POINT('Ctrl Pts',(-0.212823224907265,-0.0322874070377658,
1.85193349198693));
#11210=CARTESIAN_POINT('Ctrl Pts',(-0.0882807211693674,-0.196322988931421,
1.8630482048687));
#11211=CARTESIAN_POINT('Ctrl Pts',(0.117078428789294,-0.180634557118456,
1.87416291775048));
#11212=CARTESIAN_POINT('Ctrl Pts',(0.215258051505596,0.000415902830639266,
1.88527763063225));
#11213=CARTESIAN_POINT('Ctrl Pts',(0.116379544606898,0.181085624250633,
1.89639234351403));
#11214=CARTESIAN_POINT('Ctrl Pts',(-0.0890386955341811,0.195980387821644,
1.90750705639581));
#11215=CARTESIAN_POINT('Ctrl Pts',(-0.212946401306843,0.0314647721049302,
1.91862176927758));
#11216=CARTESIAN_POINT('Ctrl Pts',(-0.141912179210756,-0.16185529062964,
1.92973648215936));
#11217=CARTESIAN_POINT('Ctrl Pts',(0.0590356438366701,-0.207004817504183,
1.94085119504114));
#11218=CARTESIAN_POINT('Ctrl Pts',(0.205939246592667,-0.062651643442089,
1.95196590792291));
#11219=CARTESIAN_POINT('Ctrl Pts',(0.16431562602751,0.139056020208906,1.96308062080469));
#11220=CARTESIAN_POINT('Ctrl Pts',(-0.0277308461105627,0.213464755608839,
1.97419533368647));
#11221=CARTESIAN_POINT('Ctrl Pts',(-0.194391096321177,0.092457035341819,
1.98531004656824));
#11222=CARTESIAN_POINT('Ctrl Pts',(-0.183095885228843,-0.113190540794836,
1.99642475945002));
#11223=CARTESIAN_POINT('Ctrl Pts',(-0.00418542150807707,-0.215217759397172,
2.00753947233179));
#11224=CARTESIAN_POINT('Ctrl Pts',(0.178556589177984,-0.12022373382265,
2.01865418521357));
#11225=CARTESIAN_POINT('Ctrl Pts',(0.1978388488922,0.0848291906258296,2.02976889809535));
#11226=CARTESIAN_POINT('Ctrl Pts',(0.0360093998674796,0.212225174836164,
2.04088361097712));
#11227=CARTESIAN_POINT('Ctrl Pts',(-0.158784878749449,0.145339478441341,
2.0519983238589));
#11228=CARTESIAN_POINT('Ctrl Pts',(-0.208219432151661,-0.0545973423170097,
2.06311303674067));
#11229=CARTESIAN_POINT('Ctrl Pts',(-0.0670393648087706,-0.204552988925698,
2.07422774962245));
#11230=CARTESIAN_POINT('Ctrl Pts',(0.135511934624805,-0.167250462741263,
2.08534246250422));
#11231=CARTESIAN_POINT('Ctrl Pts',(0.214008741377946,0.0231616132892584,
2.09645717538601));
#11232=CARTESIAN_POINT('Ctrl Pts',(0.0965911002974415,0.192370374670147,
2.10757188826778));
#11233=CARTESIAN_POINT('Ctrl Pts',(-0.109250929180699,0.185473545786568,
2.11868660114956));
#11234=CARTESIAN_POINT('Ctrl Pts',(-0.215079121344005,0.00878483324502261,
2.12980131403133));
#11235=CARTESIAN_POINT('Ctrl Pts',(-0.124012985461959,-0.175945960758605,
2.14091602691311));
#11236=CARTESIAN_POINT('Ctrl Pts',(0.0805809219631423,-0.199606905552042,
2.15203073979489));
#11237=CARTESIAN_POINT('Ctrl Pts',(0.211406970195834,-0.0405375725545616,
2.16314545267666));
#11238=CARTESIAN_POINT('Ctrl Pts',(0.14870036265752,0.15564190807653,2.17426016555844));
#11239=CARTESIAN_POINT('Ctrl Pts',(-0.0501340907782409,0.209338899509574,
2.18537487844021));
#11240=CARTESIAN_POINT('Ctrl Pts',(-0.203073260918684,0.0713964504238905,
2.19648959132199));
#11241=CARTESIAN_POINT('Ctrl Pts',(-0.170108868289522,-0.131905922758067,
2.20760430420376));
#11242=CARTESIAN_POINT('Ctrl Pts',(0.0185817882954204,-0.214454938754768,
2.21871901708554));
#11243=CARTESIAN_POINT('Ctrl Pts',(0.190261763037141,-0.100681017192216,
2.22983372996732));
#11244=CARTESIAN_POINT('Ctrl Pts',(0.187766422487623,0.105261375664803,
2.24094844284909));
#11245=CARTESIAN_POINT('Ctrl Pts',(0.0133802873337488,0.214842235945161,
2.25206315573087));
#11246=CARTESIAN_POINT('Ctrl Pts',(-0.173255039811833,0.12774550093643,
2.26317786861264));
#11247=CARTESIAN_POINT('Ctrl Pts',(-0.201283544676172,-0.0762957032862286,
2.27429258149442));
#11248=CARTESIAN_POINT('Ctrl Pts',(-0.0450476113104433,-0.210492403912733,
2.2854072943762));
#11249=CARTESIAN_POINT('Ctrl Pts',(0.152428557369401,-0.15199283449353,
2.29652200725797));
#11250=CARTESIAN_POINT('Ctrl Pts',(0.21036129547742,0.0456470506934145,
2.30763672013975));
#11251=CARTESIAN_POINT('Ctrl Pts',(0.0757235963748345,0.201502409081358,
2.31875143302153));
#11252=CARTESIAN_POINT('Ctrl Pts',(-0.128244744151725,0.172886358992444,
2.3298661459033));
#11253=CARTESIAN_POINT('Ctrl Pts',(-0.214793419331693,-0.0139874191781991,
2.34098085878508));
#11254=CARTESIAN_POINT('Ctrl Pts',(-0.104743419772758,-0.188077725417916,
2.35209557166686));
#11255=CARTESIAN_POINT('Ctrl Pts',(0.101258932767922,-0.189951577432652,
2.36321028454863));
#11256=CARTESIAN_POINT('Ctrl Pts',(0.214439921552908,-0.0180114355890496,
2.37432499743041));
#11257=CARTESIAN_POINT('Ctrl Pts',(0.131549924351581,0.170565426741709,
2.38543971031219));
#11258=CARTESIAN_POINT('Ctrl Pts',(-0.0722434785792406,0.202706947748475,
2.39655442319396));
#11259=CARTESIAN_POINT('Ctrl Pts',(-0.163291786668867,0.100847254902872,
2.40396423178181));
#11260=CARTESIAN_POINT('Ctrl Pts',(-0.177228864907903,0.0419095421262742,
2.40766913607574));
#11261=CARTESIAN_POINT('Ctrl Pts',(0.0980771099081341,-0.137424797458509,
-0.00766913607573553));
#11262=CARTESIAN_POINT('Ctrl Pts',(0.143777923064053,-0.104809114134417,
-0.00396423178181014));
#11263=CARTESIAN_POINT('Ctrl Pts',(0.199295210917303,0.00903066859536452,
0.00344557680604064));
#11264=CARTESIAN_POINT('Ctrl Pts',(0.10029262803266,0.172678235631573,0.0145602896878168));
#11265=CARTESIAN_POINT('Ctrl Pts',(-0.090605973120834,0.177736894621117,
0.025675002569593));
#11266=CARTESIAN_POINT('Ctrl Pts',(-0.198515598543739,0.0203425352364337,
0.0367897154513692));
#11267=CARTESIAN_POINT('Ctrl Pts',(-0.124716949423446,-0.155807761693303,
0.0479044283331453));
#11268=CARTESIAN_POINT('Ctrl Pts',(0.0632659887963794,-0.189253801491094,
0.0590191412149216));
#11269=CARTESIAN_POINT('Ctrl Pts',(0.193325687989632,-0.0494840647267017,
0.0701338540966976));
#11270=CARTESIAN_POINT('Ctrl Pts',(0.146408590921473,0.135605206411971,
0.081248566978474));
#11271=CARTESIAN_POINT('Ctrl Pts',(-0.0345401040560084,0.196544446617184,
0.0923632798602499));
#11272=CARTESIAN_POINT('Ctrl Pts',(-0.183868115355446,0.0775622764543633,
0.103477992742026));
#11273=CARTESIAN_POINT('Ctrl Pts',(-0.164874420072892,-0.112427137929636,
0.114592705623802));
#11274=CARTESIAN_POINT('Ctrl Pts',(0.00505392993646349,-0.199493577660297,
0.125707418505579));
#11275=CARTESIAN_POINT('Ctrl Pts',(0.170355522424629,-0.103934261342056,
0.136822131387355));
#11276=CARTESIAN_POINT('Ctrl Pts',(0.179705106477489,0.0867721527317011,
0.147936844269131));
#11277=CARTESIAN_POINT('Ctrl Pts',(0.0245434916071218,0.19804272635179,
0.159051557150907));
#11278=CARTESIAN_POINT('Ctrl Pts',(-0.153086459888794,0.128015064093063,
0.170166270032684));
#11279=CARTESIAN_POINT('Ctrl Pts',(-0.190573317815533,-0.0592041348343418,
0.181280982914459));
#11280=CARTESIAN_POINT('Ctrl Pts',(-0.0535996969921641,-0.19222483715119,
0.192395695796236));
#11281=CARTESIAN_POINT('Ctrl Pts',(0.132441800061622,-0.149273197954655,
0.203510408678012));
#11282=CARTESIAN_POINT('Ctrl Pts',(0.197239362681098,0.0303307004072554,
0.214625121559788));
#11283=CARTESIAN_POINT('Ctrl Pts',(0.0814740158407841,0.182168333937314,
0.225739834441564));
#11284=CARTESIAN_POINT('Ctrl Pts',(-0.108876773788515,0.167239844675987,
0.23685454732334));
#11285=CARTESIAN_POINT('Ctrl Pts',(-0.199556247038418,-0.000788475357558915,
0.247969260205116));
#11286=CARTESIAN_POINT('Ctrl Pts',(-0.10755181813576,-0.168094984432202,
0.259083973086893));
#11287=CARTESIAN_POINT('Ctrl Pts',(0.0829109957492487,-0.181518826057814,
0.270198685968668));
#11288=CARTESIAN_POINT('Ctrl Pts',(0.197472882231822,-0.0287711347640326,
0.281313398850446));
#11289=CARTESIAN_POINT('Ctrl Pts',(0.131258084387575,0.150315111316951,
0.292428111732221));
#11290=CARTESIAN_POINT('Ctrl Pts',(-0.0551170160492373,0.191795286586576,
0.303542824613998));
#11291=CARTESIAN_POINT('Ctrl Pts',(-0.191035206671645,0.0576963363134077,
0.314657537495773));
#11292=CARTESIAN_POINT('Ctrl Pts',(-0.152070087450166,-0.129220764254499,
0.32577225037755));
#11293=CARTESIAN_POINT('Ctrl Pts',(0.0261076967260043,-0.197842628329557,
0.336886963259326));
#11294=CARTESIAN_POINT('Ctrl Pts',(0.180385172183149,-0.0853493237738671,
0.348001676141102));
#11295=CARTESIAN_POINT('Ctrl Pts',(0.169528919112412,0.105277077261666,
0.359116389022878));
#11296=CARTESIAN_POINT('Ctrl Pts',(0.00347730176961437,0.199527506336167,
0.370231101904654));
#11297=CARTESIAN_POINT('Ctrl Pts',(-0.165757613842657,0.111120344066412,
0.381345814786431));
#11298=CARTESIAN_POINT('Ctrl Pts',(-0.18324960915612,-0.079012012734662,
0.392460527668206));
#11299=CARTESIAN_POINT('Ctrl Pts',(-0.0329856251675023,-0.196812768753913,
0.403575240549983));
#11300=CARTESIAN_POINT('Ctrl Pts',(0.147475071809217,-0.134441141794937,
0.414689953431759));
#11301=CARTESIAN_POINT('Ctrl Pts',(0.192929614022855,0.0510047198331068,
0.425804666313535));
#11302=CARTESIAN_POINT('Ctrl Pts',(0.0617666098972408,0.189758276009417,
0.436919379195312));
#11303=CARTESIAN_POINT('Ctrl Pts',(-0.125940679256865,0.154797489387205,
0.448034092077088));
#11304=CARTESIAN_POINT('Ctrl Pts',(-0.198355487952206,-0.0218727641487044,
0.459148804958864));
#11305=CARTESIAN_POINT('Ctrl Pts',(-0.0891856303303566,-0.178519580872352,
0.47026351784064));
#11306=CARTESIAN_POINT('Ctrl Pts',(0.101629273218976,-0.171740525902436,
0.481378230722416));
#11307=CARTESIAN_POINT('Ctrl Pts',(0.199407589497414,-0.00774148972057319,
0.492492943604193));
#11308=CARTESIAN_POINT('Ctrl Pts',(0.114638092383726,0.163344498489797,
0.503607656485968));
#11309=CARTESIAN_POINT('Ctrl Pts',(-0.0750769243505434,0.184896654491977,
0.514722369367745));
#11310=CARTESIAN_POINT('Ctrl Pts',(-0.196062719639731,0.037185042419435,
0.525837082249521));
#11311=CARTESIAN_POINT('Ctrl Pts',(-0.137562764922345,-0.144567642019861,
0.536951795131298));
#11312=CARTESIAN_POINT('Ctrl Pts',(0.046869116478677,-0.193975780273649,
0.548066508013073));
#11313=CARTESIAN_POINT('Ctrl Pts',(0.188394633330749,-0.0658086585825549,
0.559181220894849));
#11314=CARTESIAN_POINT('Ctrl Pts',(0.157454155001704,0.12260304435438,0.570295933776627));
#11315=CARTESIAN_POINT('Ctrl Pts',(-0.0176278365842307,0.198777706973449,
0.581410646658401));
#11316=CARTESIAN_POINT('Ctrl Pts',(-0.176572413183126,0.0929811825852432,
0.592525359540179));
#11317=CARTESIAN_POINT('Ctrl Pts',(-0.173873654073534,-0.0979350286229587,
0.603640072421953));
#11318=CARTESIAN_POINT('Ctrl Pts',(-0.0120021401173466,-0.199196551287582,
0.614754785303731));
#11319=CARTESIAN_POINT('Ctrl Pts',(0.160856741170093,-0.118103455632765,
0.625869498185506));
#11320=CARTESIAN_POINT('Ctrl Pts',(0.186459209379211,0.0711075287852313,
0.636984211067283));
#11321=CARTESIAN_POINT('Ctrl Pts',(0.0413674675796324,0.195223077627392,
0.648098923949059));
#11322=CARTESIAN_POINT('Ctrl Pts',(-0.141594150543432,0.140621527314088,
0.659213636830835));
#11323=CARTESIAN_POINT('Ctrl Pts',(-0.194933307274904,-0.0427120957941727,
0.670328349712612));
#11324=CARTESIAN_POINT('Ctrl Pts',(-0.0698206353171251,-0.18694490176567,
0.681443062594386));
#11325=CARTESIAN_POINT('Ctrl Pts',(0.119209384716092,-0.160038870303041,
0.692557775476165));
#11326=CARTESIAN_POINT('Ctrl Pts',(0.199109092454823,0.0133748537965563,
0.703672488357939));
#11327=CARTESIAN_POINT('Ctrl Pts',(0.0967342461220328,0.174544558893895,
0.714787201239717));
#11328=CARTESIAN_POINT('Ctrl Pts',(-0.0941960315973934,0.175927328870661,
0.725901914121491));
#11329=CARTESIAN_POINT('Ctrl Pts',(-0.198894488142619,0.016257306011409,
0.73701662700327));
#11330=CARTESIAN_POINT('Ctrl Pts',(-0.121514850279847,-0.158295478690104,
0.748131339885044));
#11331=CARTESIAN_POINT('Ctrl Pts',(0.0671056398953447,-0.187936559792125,
0.759246052766821));
#11332=CARTESIAN_POINT('Ctrl Pts',(0.194294226400023,-0.0455309894454271,
0.770360765648596));
#11333=CARTESIAN_POINT('Ctrl Pts',(0.143616031236901,0.138555956147776,
0.781475478530374));
#11334=CARTESIAN_POINT('Ctrl Pts',(-0.0385355573734222,0.195801757474703,
0.792590191412148));
#11335=CARTESIAN_POINT('Ctrl Pts',(-0.185409743784085,0.0738007067864724,
0.803704904293926));
#11336=CARTESIAN_POINT('Ctrl Pts',(-0.162550454178691,-0.11576125111005,
0.814819617175701));
#11337=CARTESIAN_POINT('Ctrl Pts',(0.00911575923038187,-0.199349492966289,
0.825934330057478));
#11338=CARTESIAN_POINT('Ctrl Pts',(0.172436944653762,-0.100443105939323,
0.837049042939254));
#11339=CARTESIAN_POINT('Ctrl Pts',(0.177900611845764,0.0904139907158485,
0.84816375582103));
#11340=CARTESIAN_POINT('Ctrl Pts',(0.0205050429604615,0.198501538093417,
0.859278468702807));
#11341=CARTESIAN_POINT('Ctrl Pts',(-0.155661881445351,0.124870717452717,
0.870393181584582));
#11342=CARTESIAN_POINT('Ctrl Pts',(-0.18932803064009,-0.063073086385622,
0.881507894466359));
#11343=CARTESIAN_POINT('Ctrl Pts',(-0.0496737054522119,-0.193276590405847,
0.892622607348134));
#11344=CARTESIAN_POINT('Ctrl Pts',(0.13545444716741,-0.14654490832108,0.903737320229911));
#11345=CARTESIAN_POINT('Ctrl Pts',(0.196580734025697,0.0343414097290811,
0.914852033111688));
#11346=CARTESIAN_POINT('Ctrl Pts',(0.0777470542555572,0.183789860892396,
0.925966745993463));
#11347=CARTESIAN_POINT('Ctrl Pts',(-0.112260219196759,0.164987758934287,
0.93708145887524));
#11348=CARTESIAN_POINT('Ctrl Pts',(-0.199498798654332,-0.00485249912325078,
0.948196171757015));
#11349=CARTESIAN_POINT('Ctrl Pts',(-0.104106067235061,-0.170250533558963,
0.959310884638792));
#11350=CARTESIAN_POINT('Ctrl Pts',(0.0865906342212202,-0.179792601286676,
0.970425597520567));
#11351=CARTESIAN_POINT('Ctrl Pts',(0.198017880702589,-0.0247434099169477,
0.981540310402345));
#11352=CARTESIAN_POINT('Ctrl Pts',(0.128169523652984,0.152957152885473,
0.992655023284119));
#11353=CARTESIAN_POINT('Ctrl Pts',(-0.0590117109733095,0.190632986076034,
1.0037697361659));
#11354=CARTESIAN_POINT('Ctrl Pts',(-0.192170634664213,0.0537937225428421,
1.01488444904767));
#11355=CARTESIAN_POINT('Ctrl Pts',(-0.149406820185795,-0.132291040869109,
1.02599916192945));
#11356=CARTESIAN_POINT('Ctrl Pts',(0.0301315694205225,-0.197269880966454,
1.03711387481122));
#11357=CARTESIAN_POINT('Ctrl Pts',(0.182085993312934,-0.0816578743998708,
1.048228587693));
#11358=CARTESIAN_POINT('Ctrl Pts',(0.16734967081808,0.108707888809153,1.05934330057478));
#11359=CARTESIAN_POINT('Ctrl Pts',(-0.000587021616197327,0.199556941292166,
1.07045801345656));
#11360=CARTESIAN_POINT('Ctrl Pts',(-0.167986324712783,0.107721456180996,
1.08157272633833));
#11361=CARTESIAN_POINT('Ctrl Pts',(-0.181602432629148,-0.0827277092360154,
1.09268743922011));
#11362=CARTESIAN_POINT('Ctrl Pts',(-0.0289704701150162,-0.197443736982406,
1.10380215210188));
#11363=CARTESIAN_POINT('Ctrl Pts',(0.150182528964309,-0.131409761456854,
1.11491686498366));
#11364=CARTESIAN_POINT('Ctrl Pts',(0.191850829787004,0.0549233695461304,
1.12603157786543));
#11365=CARTESIAN_POINT('Ctrl Pts',(0.0578891580326697,0.190976864553096,
1.13714629074721));
#11366=CARTESIAN_POINT('Ctrl Pts',(-0.129067182804268,0.152200459050663,
1.14826100362899));
#11367=CARTESIAN_POINT('Ctrl Pts',(-0.197868883384114,-0.025907960178041,
1.15937571651076));
#11368=CARTESIAN_POINT('Ctrl Pts',(-0.0855313801294934,-0.180298919645701,
1.17049042939254));
#11369=CARTESIAN_POINT('Ctrl Pts',(0.10510588322153,-0.169635110529881,
1.18160514227432));
#11370=CARTESIAN_POINT('Ctrl Pts',(0.199523894310908,-0.00367872413648953,
1.19271985515609));
#11371=CARTESIAN_POINT('Ctrl Pts',(0.111287620687565,0.165645352768991,
1.20383456803787));
#11372=CARTESIAN_POINT('Ctrl Pts',(-0.0788269809639628,0.183329278851933,
1.21494928091964));
#11373=CARTESIAN_POINT('Ctrl Pts',(-0.196779369293813,0.0331842919555645,
1.22606399380142));
#11374=CARTESIAN_POINT('Ctrl Pts',(-0.134589950203975,-0.147339277575106,
1.2371787066832));
#11375=CARTESIAN_POINT('Ctrl Pts',(0.0508099303142088,-0.192981005266653,
1.24829341956497));
#11376=CARTESIAN_POINT('Ctrl Pts',(0.189695825578159,-0.0619581404698651,
1.25940813244675));
#11377=CARTESIAN_POINT('Ctrl Pts',(0.154924548333356,0.125784346148352,
1.27052284532852));
#11378=CARTESIAN_POINT('Ctrl Pts',(-0.021672512023798,0.198377467558292,
1.2816375582103));
#11379=CARTESIAN_POINT('Ctrl Pts',(-0.178429456512593,0.089365801405703,
1.29275227109208));
#11380=CARTESIAN_POINT('Ctrl Pts',(-0.171843033714247,-0.101455848407801,
1.30386698397385));
#11381=CARTESIAN_POINT('Ctrl Pts',(-0.00794278885793319,-0.199399672811719,
1.31498169685563));
#11382=CARTESIAN_POINT('Ctrl Pts',(0.163228687459056,-0.114802931158818,
1.32609640973741));
#11383=CARTESIAN_POINT('Ctrl Pts',(0.184972350854696,0.0748902318834049,
1.33721112261918));
#11384=CARTESIAN_POINT('Ctrl Pts',(0.0373829498888915,0.196025081226529,
1.34832583550096));
#11385=CARTESIAN_POINT('Ctrl Pts',(-0.144428697971146,0.137708636674038,
1.35944054838274));
#11386=CARTESIAN_POINT('Ctrl Pts',(-0.194022996069548,-0.0466732729563628,
1.37055526126451));
#11387=CARTESIAN_POINT('Ctrl Pts',(-0.0659988104906048,-0.18832810312348,
1.38166997414629));
#11388=CARTESIAN_POINT('Ctrl Pts',(0.122444031027697,-0.157577843232959,
1.39278468702806));
#11389=CARTESIAN_POINT('Ctrl Pts',(0.198795401086165,0.0174271603898547,
1.40389939990984));
#11390=CARTESIAN_POINT('Ctrl Pts',(0.0931593860498409,0.17647845818422,
1.41501411279162));
#11391=CARTESIAN_POINT('Ctrl Pts',(-0.0977594522893137,0.173972431437732,
1.42612882567339));
#11392=CARTESIAN_POINT('Ctrl Pts',(-0.199184333558908,0.0122032240394291,
1.43724353855517));
#11393=CARTESIAN_POINT('Ctrl Pts',(-0.118265781237084,-0.160737433103322,
1.44835825143694));
#11394=CARTESIAN_POINT('Ctrl Pts',(0.070919260932766,-0.1865308978186,1.45947296431872));
#11395=CARTESIAN_POINT('Ctrl Pts',(0.195181217460332,-0.0415645252945986,
1.47058767720049));
#11396=CARTESIAN_POINT('Ctrl Pts',(0.140764395750831,0.141452120172044,
1.48170239008227));
#11397=CARTESIAN_POINT('Ctrl Pts',(-0.042515287761186,0.194976326047155,
1.49281710296405));
#11398=CARTESIAN_POINT('Ctrl Pts',(-0.186874322184056,0.0700093216687068,
1.50393181584582));
#11399=CARTESIAN_POINT('Ctrl Pts',(-0.160159131298779,-0.119047763834031,
1.5150465287276));
#11400=CARTESIAN_POINT('Ctrl Pts',(0.0131738452337871,-0.19912249298866,
1.52616124160938));
#11401=CARTESIAN_POINT('Ctrl Pts',(0.174446816189558,-0.0969104005439529,
1.53727595449115));
#11402=CARTESIAN_POINT('Ctrl Pts',(0.176022330649899,0.0940183839727135,
1.54839066737293));
#11403=CARTESIAN_POINT('Ctrl Pts',(0.0164580828308227,0.198877974953982,
1.55950538025471));
#11404=CARTESIAN_POINT('Ctrl Pts',(-0.158172728106364,0.121674588537019,
1.57062009313648));
#11405=CARTESIAN_POINT('Ctrl Pts',(-0.188004207549408,-0.0669158826885055,
1.58173480601826));
#11406=CARTESIAN_POINT('Ctrl Pts',(-0.0457271073583309,-0.194248163607542,
1.59284951890003));
#11407=CARTESIAN_POINT('Ctrl Pts',(0.138410904355969,-0.143755831073476,
1.60396423178181));
#11408=CARTESIAN_POINT('Ctrl Pts',(0.19584055956543,0.038337874763241,1.61507894466359));
#11409=CARTESIAN_POINT('Ctrl Pts',(0.0739878413593942,0.185335147080201,
1.62619365754536));
#11410=CARTESIAN_POINT('Ctrl Pts',(-0.115597096526957,0.162667232984398,
1.63730837042714));
#11411=CARTESIAN_POINT('Ctrl Pts',(-0.199358593797733,-0.00891451015217326,
1.64842308330891));
#11412=CARTESIAN_POINT('Ctrl Pts',(-0.100617130822971,-0.172335458908536,
1.65953779619069));
#11413=CARTESIAN_POINT('Ctrl Pts',(0.0902343529780598,-0.177991794627994,
1.67065250907247));
#11414=CARTESIAN_POINT('Ctrl Pts',(0.198480736990691,-0.0207054209301543,
1.68176722195424));
#11415=CARTESIAN_POINT('Ctrl Pts',(0.125027795368688,0.155535744436796,
1.69288193483602));
#11416=CARTESIAN_POINT('Ctrl Pts',(-0.0628819265359346,0.189391606802921,
1.7039966477178));
#11417=CARTESIAN_POINT('Ctrl Pts',(-0.193226346036818,0.0498687939449371,
1.71511136059957));
#11418=CARTESIAN_POINT('Ctrl Pts',(-0.146681575674501,-0.135306440238108,
1.72622607348135));
#11419=CARTESIAN_POINT('Ctrl Pts',(0.0341429428748287,-0.196615301703883,
1.73734078636313));
#11420=CARTESIAN_POINT('Ctrl Pts',(0.183711281153983,-0.0779325515367303,
1.7484554992449));
#11421=CARTESIAN_POINT('Ctrl Pts',(0.165101002186673,0.112093605924776,
1.75957021212668));
#11422=CARTESIAN_POINT('Ctrl Pts',(-0.00465110149246194,0.199503595624664,
1.77068492500845));
#11423=CARTESIAN_POINT('Ctrl Pts',(-0.170145351147817,0.104277883057956,
1.78179963789023));
#11424=CARTESIAN_POINT('Ctrl Pts',(-0.179879923404974,-0.0864090884576575,
1.79291435077201));
#11425=CARTESIAN_POINT('Ctrl Pts',(-0.0249432974721202,-0.197992801191054,
1.80402906365378));
#11426=CARTESIAN_POINT('Ctrl Pts',(0.152827687091721,-0.128323869449364,
1.81514377653556));
#11427=CARTESIAN_POINT('Ctrl Pts',(0.190692461592625,0.0588192358332533,
1.82625848941733));
#11428=CARTESIAN_POINT('Ctrl Pts',(0.0539876924676758,0.192116231678321,
1.83737320229911));
#11429=CARTESIAN_POINT('Ctrl Pts',(-0.132140146435612,0.149540292604495,
1.84848791518088));
#11430=CARTESIAN_POINT('Ctrl Pts',(-0.197300198436039,-0.0299324090136843,
1.85960262806266));
#11431=CARTESIAN_POINT('Ctrl Pts',(-0.0818416496243918,-0.182003466447815,
1.87071734094444));
#11432=CARTESIAN_POINT('Ctrl Pts',(0.108538892983941,-0.167459326769468,
1.88183205382621));
#11433=CARTESIAN_POINT('Ctrl Pts',(0.199557432209361,0.000385567463561441,
1.89294676670799));
#11434=CARTESIAN_POINT('Ctrl Pts',(0.107890984430119,0.167877493699908,
1.90406147958976));
#11435=CARTESIAN_POINT('Ctrl Pts',(-0.0825443384058951,0.18168585418077,
1.91517619247155));
#11436=CARTESIAN_POINT('Ctrl Pts',(-0.197414390522405,0.0291697759149795,
1.92629090535332));
#11437=CARTESIAN_POINT('Ctrl Pts',(-0.131561304603733,-0.150049793546099,
1.9374056182351));
#11438=CARTESIAN_POINT('Ctrl Pts',(0.0547296670692254,-0.191906177479399,
1.94852033111687));
#11439=CARTESIAN_POINT('Ctrl Pts',(0.190918327810351,-0.0580819207530336,
1.95963504399865));
#11440=CARTESIAN_POINT('Ctrl Pts',(0.152330675543031,0.128913469819363,
1.97074975688042));
#11441=CARTESIAN_POINT('Ctrl Pts',(-0.0257081972270486,0.19789493679121,
1.9818644697622));
#11442=CARTESIAN_POINT('Ctrl Pts',(-0.18021248336538,0.0857133493193614,
1.99297918264398));
#11443=CARTESIAN_POINT('Ctrl Pts',(-0.169741129071859,-0.104934582067508,
2.00409389552575));
#11444=CARTESIAN_POINT('Ctrl Pts',(-0.00388014275435722,-0.199520078950613,
2.01520860840753));
#11445=CARTESIAN_POINT('Ctrl Pts',(0.165532922885783,-0.111454783895257,
2.0263233212893));
#11446=CARTESIAN_POINT('Ctrl Pts',(0.183408761716666,0.0786418688605853,
2.03743803417108));
#11447=CARTESIAN_POINT('Ctrl Pts',(0.0333829249251954,0.196745769295354,
2.04855274705286));
#11448=CARTESIAN_POINT('Ctrl Pts',(-0.147203333186775,0.13473862145244,
2.05966745993463));
#11449=CARTESIAN_POINT('Ctrl Pts',(-0.193032199844087,-0.0506150890153994,
2.07078217281641));
#11450=CARTESIAN_POINT('Ctrl Pts',(-0.0621496078990471,-0.189633181826421,
2.08189688569819));
#11451=CARTESIAN_POINT('Ctrl Pts',(0.125627884849386,-0.155051449397732,
2.09301159857996));
#11452=CARTESIAN_POINT('Ctrl Pts',(0.19839924500399,0.0214722378164315,
2.10412631146174));
#11453=CARTESIAN_POINT('Ctrl Pts',(0.0895458813959111,0.178339150307365,
2.11524102434352));
#11454=CARTESIAN_POINT('Ctrl Pts',(-0.101282320179413,0.171945366415114,
2.12635573722529));
#11455=CARTESIAN_POINT('Ctrl Pts',(-0.199391552961908,0.00814407987298619,
2.13747045010707));
#11456=CARTESIAN_POINT('Ctrl Pts',(-0.114967652853453,-0.163112710028795,
2.14858516298884));
#11457=CARTESIAN_POINT('Ctrl Pts',(0.0747034629346199,-0.185047858812318,
2.15969987587062));
#11458=CARTESIAN_POINT('Ctrl Pts',(0.195987243349849,-0.0375808190699873,
2.17081458875239));
#11459=CARTESIAN_POINT('Ctrl Pts',(0.137854367504411,0.144289606370936,
2.18192930163417));
#11460=CARTESIAN_POINT('Ctrl Pts',(-0.0464773807617405,0.194070014828589,
2.19304401451595));
#11461=CARTESIAN_POINT('Ctrl Pts',(-0.188261383097489,0.0661888938220966,
2.20415872739772));
#11462=CARTESIAN_POINT('Ctrl Pts',(-0.157701366868572,-0.122284890412664,
2.2152734402795));
#11463=CARTESIAN_POINT('Ctrl Pts',(0.0172264588114365,-0.198812897372179,
2.22638815316128));
#11464=CARTESIAN_POINT('Ctrl Pts',(0.176384337838951,-0.0933374855090313,
2.23750286604305));
#11465=CARTESIAN_POINT('Ctrl Pts',(0.174071003916871,0.0975837590815798,
2.24861757892483));
#11466=CARTESIAN_POINT('Ctrl Pts',(0.0124043480086864,0.199171945650634,
2.25973229180661));
#11467=CARTESIAN_POINT('Ctrl Pts',(-0.160618061068349,0.118427923902816,
2.27084700468838));
#11468=CARTESIAN_POINT('Ctrl Pts',(-0.186602206238641,-0.0707308020764581,
2.28196171757016));
#11469=CARTESIAN_POINT('Ctrl Pts',(-0.0417619019469965,-0.195139384244164,
2.29307643045193));
#11470=CARTESIAN_POINT('Ctrl Pts',(0.141310632941521,-0.140906691078931,
2.30419114333371));
#11471=CARTESIAN_POINT('Ctrl Pts',(0.195017838673586,0.0423176190650909,
2.31530585621549));
#11472=CARTESIAN_POINT('Ctrl Pts',(0.0702004238379346,0.186805106982167,
2.32642056909726));
#11473=CARTESIAN_POINT('Ctrl Pts',(-0.118890753020677,0.160276271309004,
2.33753528197904));
#11474=CARTESIAN_POINT('Ctrl Pts',(-0.199126689652242,-0.0129671965109469,
2.34864999486081));
#11475=CARTESIAN_POINT('Ctrl Pts',(-0.0971035821632717,-0.174359600849589,
2.35976470774259));
#11476=CARTESIAN_POINT('Ctrl Pts',(0.0938732487360676,-0.176096776735865,
2.37087942062436));
#11477=CARTESIAN_POINT('Ctrl Pts',(0.198798975503885,-0.0166977068286914,
2.38199413350614));
#11478=CARTESIAN_POINT('Ctrl Pts',(0.121954858028878,0.158124624589868,
2.39310884638792));
#11479=CARTESIAN_POINT('Ctrl Pts',(-0.0669741409359997,0.187921788294323,
2.4042235592697));
#11480=CARTESIAN_POINT('Ctrl Pts',(-0.151381513586126,0.0934915980750552,
2.41163336785755));
#11481=CARTESIAN_POINT('Ctrl Pts',(-0.164302040955162,0.0388527191122167,
2.41533827215147));
#11482=CARTESIAN_POINT('Ctrl Pts',(0.0903606778650135,-0.126612599672289,
0.));
#11483=CARTESIAN_POINT('Ctrl Pts',(0.132465879166514,-0.0965630268723143,
0.0037049042939254));
#11484=CARTESIAN_POINT('Ctrl Pts',(0.183615222457176,0.00832016090824247,
0.0111147128817762));
#11485=CARTESIAN_POINT('Ctrl Pts',(0.0924018852348323,0.159092396164803,
0.0222294257635523));
#11486=CARTESIAN_POINT('Ctrl Pts',(-0.0834773491744035,0.163753054047276,
0.0333441386453285));
#11487=CARTESIAN_POINT('Ctrl Pts',(-0.182896947799478,0.0187420415954273,
0.0444588515271047));
#11488=CARTESIAN_POINT('Ctrl Pts',(-0.11490456949349,-0.143549243818714,
0.0555735644088809));
#11489=CARTESIAN_POINT('Ctrl Pts',(0.0582883981674798,-0.17436384297299,
0.0666882772906571));
#11490=CARTESIAN_POINT('Ctrl Pts',(0.178115364857574,-0.0455907972452466,
0.0778029901724332));
#11491=CARTESIAN_POINT('Ctrl Pts',(0.134889573452136,0.124936168947966,
0.0889177030542095));
#11492=CARTESIAN_POINT('Ctrl Pts',(-0.0318225855039178,0.181080880580275,
0.100032415935985));
#11493=CARTESIAN_POINT('Ctrl Pts',(-0.169401887523431,0.0714598939929528,
0.111147128817762));
#11494=CARTESIAN_POINT('Ctrl Pts',(-0.151902562935867,-0.103581685912858,
0.122261841699538));
#11495=CARTESIAN_POINT('Ctrl Pts',(0.00465630089802304,-0.183797982260963,
0.133376554581314));
#11496=CARTESIAN_POINT('Ctrl Pts',(0.156952427521129,-0.0957570050449602,
0.14449126746309));
#11497=CARTESIAN_POINT('Ctrl Pts',(0.165566412512777,0.0799451630251659,
0.155605980344867));
#11498=CARTESIAN_POINT('Ctrl Pts',(0.0226124784964766,0.182461279865869,
0.166720693226643));
#11499=CARTESIAN_POINT('Ctrl Pts',(-0.141042046410868,0.117943197747344,
0.177835406108419));
#11500=CARTESIAN_POINT('Ctrl Pts',(-0.175579543452357,-0.0545461194875494,
0.188950118990195));
#11501=CARTESIAN_POINT('Ctrl Pts',(-0.0493826231024586,-0.177101125876806,
0.200064831871971));
#11502=CARTESIAN_POINT('Ctrl Pts',(0.122021650540482,-0.137528801235027,
0.211179544753747));
#11503=CARTESIAN_POINT('Ctrl Pts',(0.181721122596515,0.027944365932959,
0.222294257635524));
#11504=CARTESIAN_POINT('Ctrl Pts',(0.0750638686912215,0.167835840141849,
0.2334089705173));
#11505=CARTESIAN_POINT('Ctrl Pts',(-0.100310654468725,0.154081882562785,
0.244523683399076));
#11506=CARTESIAN_POINT('Ctrl Pts',(-0.18385572098811,-0.000726440326955142,
0.255638396280852));
#11507=CARTESIAN_POINT('Ctrl Pts',(-0.0990899426121504,-0.154869742320406,
0.266753109162628));
#11508=CARTESIAN_POINT('Ctrl Pts',(0.0763877910491314,-0.167237433721381,
0.277867822044404));
#11509=CARTESIAN_POINT('Ctrl Pts',(0.181936269483671,-0.0265075025422269,
0.288982534926181));
#11510=CARTESIAN_POINT('Ctrl Pts',(0.120931066297065,0.138488739775033,
0.300097247807957));
#11511=CARTESIAN_POINT('Ctrl Pts',(-0.0507805637499992,0.17670537114635,
0.311211960689733));
#11512=CARTESIAN_POINT('Ctrl Pts',(-0.176005092188198,0.0531569503270556,
0.322326673571509));
#11513=CARTESIAN_POINT('Ctrl Pts',(-0.140105639306261,-0.119054036800316,
0.333441386453286));
#11514=CARTESIAN_POINT('Ctrl Pts',(0.0240536163419306,-0.182276924995041,
0.344556099335061));
#11515=CARTESIAN_POINT('Ctrl Pts',(0.166192972555312,-0.078634278260764,
0.355670812216838));
#11516=CARTESIAN_POINT('Ctrl Pts',(0.156190859040095,0.0969941719726652,
0.366785525098613));
#11517=CARTESIAN_POINT('Ctrl Pts',(0.00320371741518769,0.183829241523736,
0.37790023798039));
#11518=CARTESIAN_POINT('Ctrl Pts',(-0.152716269495902,0.102377706927133,
0.389014950862166));
#11519=CARTESIAN_POINT('Ctrl Pts',(-0.168832043657856,-0.0727955690871238,
0.400129663743942));
#11520=CARTESIAN_POINT('Ctrl Pts',(-0.030390408656302,-0.18132809188354,
0.411244376625719));
#11521=CARTESIAN_POINT('Ctrl Pts',(0.135872146613563,-0.123863689671489,
0.422359089507495));
#11522=CARTESIAN_POINT('Ctrl Pts',(0.177750452880091,0.0469918114711103,
0.433473802389271));
#11523=CARTESIAN_POINT('Ctrl Pts',(0.0569069861965436,0.174828626850531,
0.444588515271047));
#11524=CARTESIAN_POINT('Ctrl Pts',(-0.116032019694402,0.142618456905312,
0.455703228152823));
#11525=CARTESIAN_POINT('Ctrl Pts',(-0.182749434260409,-0.0201518763869515,
0.466817941034599));
#11526=CARTESIAN_POINT('Ctrl Pts',(-0.0821687549726806,-0.164474160738562,
0.477932653916376));
#11527=CARTESIAN_POINT('Ctrl Pts',(0.093633366925239,-0.158228462808239,
0.489047366798152));
#11528=CARTESIAN_POINT('Ctrl Pts',(0.183718759405662,-0.00713241101304534,
0.500162079679928));
#11529=CARTESIAN_POINT('Ctrl Pts',(0.105618688669037,0.150493011293707,
0.511276792561704));
#11530=CARTESIAN_POINT('Ctrl Pts',(-0.0691700824248357,0.170349504084268,
0.52239150544348));
#11531=CARTESIAN_POINT('Ctrl Pts',(-0.180637054530859,0.0342594275321448,
0.533506218325257));
#11532=CARTESIAN_POINT('Ctrl Pts',(-0.12673971224287,-0.133193465248897,
0.544620931207033));
#11533=CARTESIAN_POINT('Ctrl Pts',(0.0431815857942205,-0.178714309703255,
0.555735644088809));
#11534=CARTESIAN_POINT('Ctrl Pts',(0.173572271754774,-0.0606310178233981,
0.566850356970585));
#11535=CARTESIAN_POINT('Ctrl Pts',(0.145066103517367,0.112956980548805,
0.577965069852361));
#11536=CARTESIAN_POINT('Ctrl Pts',(-0.0162409278223676,0.183138434272774,
0.589079782734138));
#11537=CARTESIAN_POINT('Ctrl Pts',(-0.162680190744136,0.0856656838171876,
0.600194495615913));
#11538=CARTESIAN_POINT('Ctrl Pts',(-0.160193762435174,-0.0902297751370224,
0.61130920849769));
#11539=CARTESIAN_POINT('Ctrl Pts',(-0.0110578453815636,-0.183524325090524,
0.622423921379466));
#11540=CARTESIAN_POINT('Ctrl Pts',(0.148200983745356,-0.108811406852975,
0.633538634261242));
#11541=CARTESIAN_POINT('Ctrl Pts',(0.171789121533681,0.0655129877741882,
0.644653347143018));
#11542=CARTESIAN_POINT('Ctrl Pts',(0.0381127912063918,0.179863473198069,
0.655768060024794));
#11543=CARTESIAN_POINT('Ctrl Pts',(-0.130453919745491,0.129557819785036,
0.666882772906571));
#11544=CARTESIAN_POINT('Ctrl Pts',(-0.17959650116453,-0.0393516278427419,
0.677997485788347));
#11545=CARTESIAN_POINT('Ctrl Pts',(-0.0643273434762849,-0.172236601004835,
0.689112198670122));
#11546=CARTESIAN_POINT('Ctrl Pts',(0.10983032453655,-0.147447460665183,
0.7002269115519));
#11547=CARTESIAN_POINT('Ctrl Pts',(0.183443747273531,0.0123225577969614,
0.711341624433675));
#11548=CARTESIAN_POINT('Ctrl Pts',(0.0891234668368183,0.160811882345183,
0.722456337315452));
#11549=CARTESIAN_POINT('Ctrl Pts',(-0.0867849519149494,0.162085859856851,
0.733571050197227));
#11550=CARTESIAN_POINT('Ctrl Pts',(-0.183246027426955,0.0149782267526674,
0.744685763079004));
#11551=CARTESIAN_POINT('Ctrl Pts',(-0.111954402533252,-0.145841234216655,
0.75580047596078));
#11552=CARTESIAN_POINT('Ctrl Pts',(0.0618259562826469,-0.173150238157939,
0.766915188842555));
#11553=CARTESIAN_POINT('Ctrl Pts',(0.179007701381185,-0.0419487388444433,
0.778029901724333));
#11554=CARTESIAN_POINT('Ctrl Pts',(0.132316724534454,0.127654761967143,
0.789144614606108));
#11555=CARTESIAN_POINT('Ctrl Pts',(-0.0355036877557856,0.180396624137356,
0.800259327487885));
#11556=CARTESIAN_POINT('Ctrl Pts',(-0.170822224949343,0.0679942740807686,
0.81137404036966));
#11557=CARTESIAN_POINT('Ctrl Pts',(-0.149761440162857,-0.106653480415604,
0.822488753251438));
#11558=CARTESIAN_POINT('Ctrl Pts',(0.00839855685065273,-0.18366523374673,
0.833603466133212));
#11559=CARTESIAN_POINT('Ctrl Pts',(0.158870089284654,-0.0925405239616719,
0.844718179014991));
#11560=CARTESIAN_POINT('Ctrl Pts',(0.163903890459678,0.0833004714068091,
0.855832891896764));
#11561=CARTESIAN_POINT('Ctrl Pts',(0.0188917636673275,0.182883993585968,
0.866947604778543));
#11562=CARTESIAN_POINT('Ctrl Pts',(-0.143414841019688,0.115046239485315,
0.878062317660317));
#11563=CARTESIAN_POINT('Ctrl Pts',(-0.174432231980648,-0.0581106727775883,
0.889177030542094));
#11564=CARTESIAN_POINT('Ctrl Pts',(-0.0457655175701415,-0.178070130134034,
0.90029174342387));
#11565=CARTESIAN_POINT('Ctrl Pts',(0.124797271018106,-0.135015165780915,
0.911406456305646));
#11566=CARTESIAN_POINT('Ctrl Pts',(0.18111431299722,0.0316395238895826,
0.922521169187422));
#11567=CARTESIAN_POINT('Ctrl Pts',(0.071630133994783,0.169329789902144,
0.933635882069198));
#11568=CARTESIAN_POINT('Ctrl Pts',(-0.103427899877919,0.152006984613398,
0.944750594950975));
#11569=CARTESIAN_POINT('Ctrl Pts',(-0.183802792481824,-0.0044707180964717,
0.95586530783275));
#11570=CARTESIAN_POINT('Ctrl Pts',(-0.0959152937319705,-0.156855698885072,
0.966980020714528));
#11571=CARTESIAN_POINT('Ctrl Pts',(0.0797779258821927,-0.165647023475673,
0.978094733596302));
#11572=CARTESIAN_POINT('Ctrl Pts',(0.182438389002691,-0.0227966677941671,
0.989209446478081));
#11573=CARTESIAN_POINT('Ctrl Pts',(0.118085504862125,0.140922912920049,
1.00032415935986));
#11574=CARTESIAN_POINT('Ctrl Pts',(-0.0543688349964322,0.175634517181406,
1.01143887224163));
#11575=CARTESIAN_POINT('Ctrl Pts',(-0.177051187889545,0.0495613832667703,
1.02255358512341));
#11576=CARTESIAN_POINT('Ctrl Pts',(-0.137651910443638,-0.121882752658575,
1.03366829800518));
#11577=CARTESIAN_POINT('Ctrl Pts',(0.0277609020139879,-0.181749239788739,
1.04478301088696));
#11578=CARTESIAN_POINT('Ctrl Pts',(0.167759977846949,-0.0752332617743367,
1.05589772376874));
#11579=CARTESIAN_POINT('Ctrl Pts',(0.154183067891921,0.10015505688606,1.06701243665051));
#11580=CARTESIAN_POINT('Ctrl Pts',(-0.000540836401177662,0.183856360619919,
1.07812714953229));
#11581=CARTESIAN_POINT('Ctrl Pts',(-0.154769631643078,0.0992462340115768,
1.08924186241407));
#11582=CARTESIAN_POINT('Ctrl Pts',(-0.167314462362078,-0.0762189250049056,
1.10035657529584));
#11583=CARTESIAN_POINT('Ctrl Pts',(-0.0266911547466422,-0.181909417300769,
1.11147128817762));
#11584=CARTESIAN_POINT('Ctrl Pts',(0.138366588630194,-0.121070809839768,
1.12258600105939));
#11585=CARTESIAN_POINT('Ctrl Pts',(0.176756544363487,0.0506021528108583,
1.13370071394117));
#11586=CARTESIAN_POINT('Ctrl Pts',(0.053334601374032,0.175951340263971,
1.14481542682295));
#11587=CARTESIAN_POINT('Ctrl Pts',(-0.118912538708016,0.140225753634735,
1.15593013970472));
#11588=CARTESIAN_POINT('Ctrl Pts',(-0.182301114375512,-0.0238695945055889,
1.1670448525865));
#11589=CARTESIAN_POINT('Ctrl Pts',(-0.0788020109327346,-0.166113506125697,
1.17815956546827));
#11590=CARTESIAN_POINT('Ctrl Pts',(0.0968364469996555,-0.156288695614551,
1.18927427835005));
#11591=CARTESIAN_POINT('Ctrl Pts',(0.183825913682498,-0.00338929243493567,
1.20038899123183));
#11592=CARTESIAN_POINT('Ctrl Pts',(0.102531822692703,0.152612840808782,
1.2115037041136));
#11593=CARTESIAN_POINT('Ctrl Pts',(-0.0726250950973966,0.168905445165361,
1.22261841699538));
#11594=CARTESIAN_POINT('Ctrl Pts',(-0.181297320199323,0.0305734448984526,
1.23373312987716));
#11595=CARTESIAN_POINT('Ctrl Pts',(-0.124000790252096,-0.135747036289086,
1.24484784275893));
#11596=CARTESIAN_POINT('Ctrl Pts',(0.0468123474454561,-0.177797800804905,
1.25596255564071));
#11597=CARTESIAN_POINT('Ctrl Pts',(0.174771089844121,-0.0570834476806803,
1.26707726852248));
#11598=CARTESIAN_POINT('Ctrl Pts',(0.142735519209796,0.115887986436578,
1.27819198140426));
#11599=CARTESIAN_POINT('Ctrl Pts',(-0.0199673795378149,0.182769684572709,
1.28930669428604));
#11600=CARTESIAN_POINT('Ctrl Pts',(-0.164391127110762,0.082334750692938,
1.30042140716781));
#11601=CARTESIAN_POINT('Ctrl Pts',(-0.158322905592802,-0.0934735866920008,
1.31153612004959));
#11602=CARTESIAN_POINT('Ctrl Pts',(-0.00731787249863105,-0.183711465582603,
1.32265083293137));
#11603=CARTESIAN_POINT('Ctrl Pts',(0.150386311950183,-0.10577055839144,
1.33376554581314));
#11604=CARTESIAN_POINT('Ctrl Pts',(0.170419244869387,0.0689980783976093,
1.34488025869492));
#11605=CARTESIAN_POINT('Ctrl Pts',(0.0344417641967487,0.180602377402486,
1.35599497157669));
#11606=CARTESIAN_POINT('Ctrl Pts',(-0.133065452928399,0.126874107214099,
1.36710968445847));
#11607=CARTESIAN_POINT('Ctrl Pts',(-0.178757810692705,-0.0430011506911841,
1.37822439734024));
#11608=CARTESIAN_POINT('Ctrl Pts',(-0.0608062091124237,-0.173510975957692,
1.38933911022202));
#11609=CARTESIAN_POINT('Ctrl Pts',(0.112810477944863,-0.145180060305354,
1.4004538231038));
#11610=CARTESIAN_POINT('Ctrl Pts',(0.183154736262308,0.0160560402683587,
1.41156853598558));
#11611=CARTESIAN_POINT('Ctrl Pts',(0.0858298667327937,0.162593627861136,
1.42268324886735));
#11612=CARTESIAN_POINT('Ctrl Pts',(-0.0900680126570708,0.160284768273284,
1.43379796174913));
#11613=CARTESIAN_POINT('Ctrl Pts',(-0.183513068618488,0.0112431085844059,
1.44491267463091));
#11614=CARTESIAN_POINT('Ctrl Pts',(-0.108960961133834,-0.148091062502792,
1.45602738751268));
#11615=CARTESIAN_POINT('Ctrl Pts',(0.0653395323085358,-0.171855169727642,
1.46714210039446));
#11616=CARTESIAN_POINT('Ctrl Pts',(0.179824906471596,-0.0382943449728064,
1.47825681327623));
#11617=CARTESIAN_POINT('Ctrl Pts',(0.129689447733715,0.130323063925534,
1.48937152615801));
#11618=CARTESIAN_POINT('Ctrl Pts',(-0.0391703041140288,0.179636135340385,
1.50048623903978));
#11619=CARTESIAN_POINT('Ctrl Pts',(-0.172171574426829,0.0645011845147166,
1.51160095192156));
#11620=CARTESIAN_POINT('Ctrl Pts',(-0.147558259862935,-0.109681419532377,
1.52271566480334));
#11621=CARTESIAN_POINT('Ctrl Pts',(0.0121373640243727,-0.183456093490935,
1.53383037768511));
#11622=CARTESIAN_POINT('Ctrl Pts',(0.160721829762796,-0.0892857619226799,
1.54494509056689));
#11623=CARTESIAN_POINT('Ctrl Pts',(0.162173387162441,0.0866212811073344,
1.55605980344866));
#11624=CARTESIAN_POINT('Ctrl Pts',(0.0151632070148183,0.183230813449705,
1.56717451633044));
#11625=CARTESIAN_POINT('Ctrl Pts',(-0.145728141304706,0.112101573032185,
1.57828922921222));
#11626=CARTESIAN_POINT('Ctrl Pts',(-0.173212563579333,-0.0616511286408472,
1.58940394209399));
#11627=CARTESIAN_POINT('Ctrl Pts',(-0.042129426749787,-0.178965262680077,
1.60051865497577));
#11628=CARTESIAN_POINT('Ctrl Pts',(0.127521122443655,-0.132445525311824,
1.61163336785754));
#11629=CARTESIAN_POINT('Ctrl Pts',(0.180432373388368,0.0353215582591597,
1.62274808073932));
#11630=CARTESIAN_POINT('Ctrl Pts',(0.0681666854301347,0.170753497304986,
1.6338627936211));
#11631=CARTESIAN_POINT('Ctrl Pts',(-0.106502241054892,0.149869031139527,
1.64497750650287));
#11632=CARTESIAN_POINT('Ctrl Pts',(-0.183673618550271,-0.00821314148570485,
1.65609221938465));
#11633=CARTESIAN_POINT('Ctrl Pts',(-0.0927008570553628,-0.158776588153342,
1.66720693226643));
#11634=CARTESIAN_POINT('Ctrl Pts',(0.0831349670626055,-0.163987899236237,
1.6783216451482));
#11635=CARTESIAN_POINT('Ctrl Pts',(0.182864829055688,-0.0190763764601355,
1.68943635802998));
#11636=CARTESIAN_POINT('Ctrl Pts',(0.115190958951233,0.143298628117334,
1.70055107091176));
#11637=CARTESIAN_POINT('Ctrl Pts',(-0.0579345528489473,0.174490806149227,
1.71166578379353));
#11638=CARTESIAN_POINT('Ctrl Pts',(-0.178023838851097,0.0459452570472002,
1.72278049667531));
#11639=CARTESIAN_POINT('Ctrl Pts',(-0.135141080530122,-0.124660908859055,
1.73389520955708));
#11640=CARTESIAN_POINT('Ctrl Pts',(0.0314566718510104,-0.181146160987399,
1.74500992243886));
#11641=CARTESIAN_POINT('Ctrl Pts',(0.169257392597246,-0.071801036869925,
1.75612463532064));
#11642=CARTESIAN_POINT('Ctrl Pts',(0.15211131820417,0.103274395271066,1.76723934820241));
#11643=CARTESIAN_POINT('Ctrl Pts',(-0.00428516586664415,0.18380721203998,
1.77835406108419));
#11644=CARTESIAN_POINT('Ctrl Pts',(-0.156758791931151,0.0960735915676151,
1.78946877396597));
#11645=CARTESIAN_POINT('Ctrl Pts',(-0.165727475334516,-0.0796106636303336,
1.80058348684774));
#11646=CARTESIAN_POINT('Ctrl Pts',(-0.0229808287568944,-0.182415282676811,
1.81169819972952));
#11647=CARTESIAN_POINT('Ctrl Pts',(0.140803633131985,-0.118227707163963,
1.82281291261129));
#11648=CARTESIAN_POINT('Ctrl Pts',(0.175689313331093,0.0541915032607811,
1.83392762549307));
#11649=CARTESIAN_POINT('Ctrl Pts',(0.0497400921817236,0.177001065178062,
1.84504233837485));
#11650=CARTESIAN_POINT('Ctrl Pts',(-0.121743730176064,0.137774881626631,
1.85615705125662));
#11651=CARTESIAN_POINT('Ctrl Pts',(-0.181777171964813,-0.0275774109896026,
1.8672717641384));
#11652=CARTESIAN_POINT('Ctrl Pts',(-0.0754025780794165,-0.16768394396421,
1.87838647702017));
#11653=CARTESIAN_POINT('Ctrl Pts',(0.0999993571785868,-0.154284096420481,
1.88950118990195));
#11654=CARTESIAN_POINT('Ctrl Pts',(0.183856812913126,0.000355232096483363,
1.90061590278373));
#11655=CARTESIAN_POINT('Ctrl Pts',(0.0994024242533403,0.154669363149183,
1.9117306156655));
#11656=CARTESIAN_POINT('Ctrl Pts',(-0.0760499812776094,0.167391320539895,
1.92284532854728));
#11657=CARTESIAN_POINT('Ctrl Pts',(-0.181882379737966,0.0268747797250293,
1.93396004142905));
#11658=CARTESIAN_POINT('Ctrl Pts',(-0.121210429996709,-0.138244296462558,
1.94507475431083));
#11659=CARTESIAN_POINT('Ctrl Pts',(0.050423690301781,-0.176807537454614,
1.95618946719261));
#11660=CARTESIAN_POINT('Ctrl Pts',(0.175897409028035,-0.0535121980639788,
1.96730418007439));
#11661=CARTESIAN_POINT('Ctrl Pts',(0.140345725058553,0.118770919429821,
1.97841889295616));
#11662=CARTESIAN_POINT('Ctrl Pts',(-0.0236855483435345,0.18232511797358,
1.98953360583794));
#11663=CARTESIAN_POINT('Ctrl Pts',(-0.166033870409582,0.0789696632969042,
2.00064831871971));
#11664=CARTESIAN_POINT('Ctrl Pts',(-0.156386372914875,-0.0966786233401791,
2.01176303160149));
#11665=CARTESIAN_POINT('Ctrl Pts',(-0.00357486400063734,-0.183822398504055,
2.02287774448326));
#11666=CARTESIAN_POINT('Ctrl Pts',(0.152509256593582,-0.102685833967865,
2.03399245736504));
#11667=CARTESIAN_POINT('Ctrl Pts',(0.168978674541131,0.072454547095341,
2.04510717024682));
#11668=CARTESIAN_POINT('Ctrl Pts',(0.0307564499829109,0.181266363754544,
2.05622188312859));
#11669=CARTESIAN_POINT('Ctrl Pts',(-0.135621787624101,0.124137764463539,
2.06733659601037));
#11670=CARTESIAN_POINT('Ctrl Pts',(-0.177844967536513,-0.046632835713789,
2.07845130889214));
#11671=CARTESIAN_POINT('Ctrl Pts',(-0.0572598509893232,-0.174713374727145,
2.08956602177392));
#11672=CARTESIAN_POINT('Ctrl Pts',(0.115743835073967,-0.142852436054201,
2.10068073465569));
#11673=CARTESIAN_POINT('Ctrl Pts',(0.182789748630034,0.0197828623436046,
2.11179544753748));
#11674=CARTESIAN_POINT('Ctrl Pts',(0.0825006624943804,0.164307925944582,
2.12291016041925));
#11675=CARTESIAN_POINT('Ctrl Pts',(-0.0933137111781269,0.15841718704366,
2.13402487330103));
#11676=CARTESIAN_POINT('Ctrl Pts',(-0.183703984579811,0.00750332650094965,
2.1451395861828));
#11677=CARTESIAN_POINT('Ctrl Pts',(-0.105922320244947,-0.150279459298985,
2.15625429906458));
#11678=CARTESIAN_POINT('Ctrl Pts',(0.0688260039060977,-0.170488812072594,
2.16736901194635));
#11679=CARTESIAN_POINT('Ctrl Pts',(0.180567516503863,-0.0346240655854127,
2.17848372482813));
#11680=CARTESIAN_POINT('Ctrl Pts',(0.127008372351303,0.132937304665343,
2.18959843770991));
#11681=CARTESIAN_POINT('Ctrl Pts',(-0.0428206707452402,0.178801130147604,
2.20071315059168));
#11682=CARTESIAN_POINT('Ctrl Pts',(-0.173449505276293,0.0609813372203028,
2.21182786347346));
#11683=CARTESIAN_POINT('Ctrl Pts',(-0.145293865447621,-0.112663858067262,
2.22294257635523));
#11684=CARTESIAN_POINT('Ctrl Pts',(0.0158711293274525,-0.18317085598959,
2.23405728923701));
#11685=CARTESIAN_POINT('Ctrl Pts',(0.162506912640762,-0.0859939538258468,
2.24517200211879));
#11686=CARTESIAN_POINT('Ctrl Pts',(0.160375585346118,0.0899061424983564,
2.25628671500056));
#11687=CARTESIAN_POINT('Ctrl Pts',(0.011428408683624,0.183501655356106,
2.26740142788234));
#11688=CARTESIAN_POINT('Ctrl Pts',(-0.147981082324864,0.109110346869202,
2.27851614076412));
#11689=CARTESIAN_POINT('Ctrl Pts',(-0.171920867801111,-0.0651659008666877,
2.28963085364589));
#11690=CARTESIAN_POINT('Ctrl Pts',(-0.0384761925835495,-0.179786364575594,
2.30074556652767));
#11691=CARTESIAN_POINT('Ctrl Pts',(0.130192708513641,-0.129820547664333,
2.31186027940944));
#11692=CARTESIAN_POINT('Ctrl Pts',(0.179674381869752,0.0389881874367674,
2.32297499229122));
#11693=CARTESIAN_POINT('Ctrl Pts',(0.0646772513010348,0.172107804882976,
2.33408970517299));
#11694=CARTESIAN_POINT('Ctrl Pts',(-0.109536761889629,0.147666183625563,
2.34520441805478));
#11695=CARTESIAN_POINT('Ctrl Pts',(-0.183459959972792,-0.0119469738436946,
2.35631913093654));
#11696=CARTESIAN_POINT('Ctrl Pts',(-0.0894637445537859,-0.160641476281263,
2.36743384381833));
#11697=CARTESIAN_POINT('Ctrl Pts',(0.0864875647042136,-0.162241976039076,
2.3785485567001));
#11698=CARTESIAN_POINT('Ctrl Pts',(0.183158029454863,-0.0153839780683336,
2.38966326958188));
#11699=CARTESIAN_POINT('Ctrl Pts',(0.112359791706175,0.145683822438027,
2.40077798246366));
#11700=CARTESIAN_POINT('Ctrl Pts',(-0.0617048032927588,0.173136628840171,
2.41189269534543));
#11701=CARTESIAN_POINT('Ctrl Pts',(-0.139471240503386,0.0861359412472379,
2.41930250393328));
#11702=CARTESIAN_POINT('Ctrl Pts',(-0.15137521700242,0.0357958960981592,
2.42300740822721));
#11703=CARTESIAN_POINT('Ctrl Pts',(0.103461767481305,0.116497970106856,
2.4));
#11704=CARTESIAN_POINT('Ctrl Pts',(0.101062838412544,0.119258880418799,
2.4));
#11705=CARTESIAN_POINT('Ctrl Pts',(0.0985654514169239,0.121922998634947,
2.4));
#11706=CARTESIAN_POINT('Ctrl Pts',(0.0959729906474675,0.124483778490476,
2.4));
#11707=CARTESIAN_POINT('Ctrl Pts',(0.0883686915733725,0.131995149969571,
2.4));
#11708=CARTESIAN_POINT('Ctrl Pts',(0.0799499756415848,0.138619651568493,
2.4));
#11709=CARTESIAN_POINT('Ctrl Pts',(0.0709074190314827,0.144354628951697,
2.4));
#11710=CARTESIAN_POINT('Ctrl Pts',(0.0663081210711623,0.147271599330582,
2.4));
#11711=CARTESIAN_POINT('Ctrl Pts',(0.0615466559749117,0.149958011111103,
2.4));
#11712=CARTESIAN_POINT('Ctrl Pts',(0.0566442332600693,0.152410331606476,
2.4));
#11713=CARTESIAN_POINT('Ctrl Pts',(0.0538846120488591,0.153790766556572,
2.4));
#11714=CARTESIAN_POINT('Ctrl Pts',(0.0510823344409583,0.155095773985438,
2.4));
#11715=CARTESIAN_POINT('Ctrl Pts',(0.0482496499195413,0.156321567055163,
2.4));
#11716=CARTESIAN_POINT('Ctrl Pts',(0.0376888807059046,0.160891549209958,
2.4));
#11717=CARTESIAN_POINT('Ctrl Pts',(0.026677561630956,0.164379337372229,
2.4));
#11718=CARTESIAN_POINT('Ctrl Pts',(0.0154207238187948,0.166770147581746,
2.4));
#11719=CARTESIAN_POINT('Ctrl Pts',(0.00969748088526884,0.167985692112577,
2.4));
#11720=CARTESIAN_POINT('Ctrl Pts',(0.00391012467736534,0.168917061289908,
2.4));
#11721=CARTESIAN_POINT('Ctrl Pts',(-0.00191715667191961,0.169557978194554,
2.4));
#11722=CARTESIAN_POINT('Ctrl Pts',(-0.00616200194240661,0.170024849953164,
2.4));
#11723=CARTESIAN_POINT('Ctrl Pts',(-0.0104304763189531,0.170337222982092,
2.4));
#11724=CARTESIAN_POINT('Ctrl Pts',(-0.0146899072891042,0.170491883891854,
2.4));
#11725=CARTESIAN_POINT('Ctrl Pts',(-0.0266165983220355,0.170924944762785,
2.4));
#11726=CARTESIAN_POINT('Ctrl Pts',(-0.0385088145683558,0.170130732075648,
2.4));
#11727=CARTESIAN_POINT('Ctrl Pts',(-0.0501623159300862,0.168075457674568,
2.4));
#11728=CARTESIAN_POINT('Ctrl Pts',(-0.0531380387349214,0.167550643138949,
2.4));
#11729=CARTESIAN_POINT('Ctrl Pts',(-0.056098276264386,0.166943351080139,
2.4));
#11730=CARTESIAN_POINT('Ctrl Pts',(-0.0590397244743148,0.166252475819097,
2.4));
#11731=CARTESIAN_POINT('Ctrl Pts',(-0.0636086044060329,0.165179356086839,
2.4));
#11732=CARTESIAN_POINT('Ctrl Pts',(-0.0681321698191967,0.163904647115538,
2.4));
#11733=CARTESIAN_POINT('Ctrl Pts',(-0.0726033638424945,0.16243676026702,
2.4));
#11734=CARTESIAN_POINT('Ctrl Pts',(-0.0761928889181732,0.161258324121428,
2.4));
#11735=CARTESIAN_POINT('Ctrl Pts',(-0.0797406633513067,0.159957854461999,
2.4));
#11736=CARTESIAN_POINT('Ctrl Pts',(-0.0832382631684214,0.158543149031954,
2.4));
#11737=CARTESIAN_POINT('Ctrl Pts',(-0.0942712060188925,0.154080556117935,
2.4));
#11738=CARTESIAN_POINT('Ctrl Pts',(-0.104821070590689,0.148480110064895,
2.4));
#11739=CARTESIAN_POINT('Ctrl Pts',(-0.114778874587596,0.14189890553014,
2.4));
#11740=CARTESIAN_POINT('Ctrl Pts',(-0.119667974430172,0.13866765433612,
2.4));
#11741=CARTESIAN_POINT('Ctrl Pts',(-0.124414280597228,0.135199161922686,
2.4));
#11742=CARTESIAN_POINT('Ctrl Pts',(-0.129003727534357,0.131507805861248,
2.4));
#11743=CARTESIAN_POINT('Ctrl Pts',(-0.132789110117922,0.128463169952799,
2.4));
#11744=CARTESIAN_POINT('Ctrl Pts',(-0.136469556648549,0.125264639778438,
2.4));
#11745=CARTESIAN_POINT('Ctrl Pts',(-0.140019314144638,0.121936802656766,
2.4));
#11746=CARTESIAN_POINT('Ctrl Pts',(-0.146223653031234,0.116120340747751,
2.4));
#11747=CARTESIAN_POINT('Ctrl Pts',(-0.152041126912371,0.109900559216443,
2.4));
#11748=CARTESIAN_POINT('Ctrl Pts',(-0.157432164500961,0.103324206966413,
2.4));
#11749=CARTESIAN_POINT('Ctrl Pts',(-0.160741343411017,0.0992874467299484,
2.4));
#11750=CARTESIAN_POINT('Ctrl Pts',(-0.163889774361174,0.0951161328995282,
2.4));
#11751=CARTESIAN_POINT('Ctrl Pts',(-0.166867208569052,0.0908194395900732,
2.4));
#11752=CARTESIAN_POINT('Ctrl Pts',(-0.16945817546063,0.0870804518137491,
2.4));
#11753=CARTESIAN_POINT('Ctrl Pts',(-0.171914118235205,0.0832543718370342,
2.4));
#11754=CARTESIAN_POINT('Ctrl Pts',(-0.17422826794027,0.0793498140525304,
2.4));
#11755=CARTESIAN_POINT('Ctrl Pts',(-0.180683508174901,0.0684581857132719,
2.4));
#11756=CARTESIAN_POINT('Ctrl Pts',(-0.186040971013606,0.0569542137720182,
2.4));
#11757=CARTESIAN_POINT('Ctrl Pts',(-0.190155688860645,0.0449663651403318,
2.4));
#11758=CARTESIAN_POINT('Ctrl Pts',(0.0863566694936597,0.175642871684081,
0.));
#11759=CARTESIAN_POINT('Ctrl Pts',(0.0902251377602554,0.173267020623209,
-1.48058408815148E-18));
#11760=CARTESIAN_POINT('Ctrl Pts',(0.0939991325874577,0.170750246590702,
-3.18714891677109E-17));
#11761=CARTESIAN_POINT('Ctrl Pts',(0.0976698484646397,0.168092084222829,
-2.37440275774325E-17));
#11762=CARTESIAN_POINT('Ctrl Pts',(0.104809934079732,0.162921565032443,
-6.47830459115438E-18));
#11763=CARTESIAN_POINT('Ctrl Pts',(0.11155987158375,0.157216438110753,-1.30821889653785E-17));
#11764=CARTESIAN_POINT('Ctrl Pts',(0.117888926389013,0.151039119528356,
-2.51534904016637E-17));
#11765=CARTESIAN_POINT('Ctrl Pts',(0.12275959422371,0.146285223749331,-3.4443234516339E-17));
#11766=CARTESIAN_POINT('Ctrl Pts',(0.127384674495468,0.141245910799109,
-5.49491509124901E-17));
#11767=CARTESIAN_POINT('Ctrl Pts',(0.131724318639059,0.135976688450155,
-4.46691295064028E-17));
#11768=CARTESIAN_POINT('Ctrl Pts',(0.13624098258323,0.130492527581232,-3.39697724868313E-17));
#11769=CARTESIAN_POINT('Ctrl Pts',(0.140453276997769,0.124755769602575,
2.19954579643677E-17));
#11770=CARTESIAN_POINT('Ctrl Pts',(0.144343923096435,0.11879886899313,2.34187669256869E-17));
#11771=CARTESIAN_POINT('Ctrl Pts',(0.14782723598055,0.113465629187694,2.46930618158692E-17));
#11772=CARTESIAN_POINT('Ctrl Pts',(0.151052683365278,0.107955843865382,
-2.41963381637405E-17));
#11773=CARTESIAN_POINT('Ctrl Pts',(0.154004429688849,0.102292097260694,
-2.77555756156289E-17));
#11774=CARTESIAN_POINT('Ctrl Pts',(0.155739361180546,0.098963148472989,
-2.98475687833339E-17));
#11775=CARTESIAN_POINT('Ctrl Pts',(0.157375218128347,0.0955895675179438,
-1.47300813205832E-17));
#11776=CARTESIAN_POINT('Ctrl Pts',(0.158909878065559,0.0921763188170318,
-1.38777878078145E-17));
#11777=CARTESIAN_POINT('Ctrl Pts',(0.163914736043458,0.0810449765716888,
-1.10982743250791E-17));
#11778=CARTESIAN_POINT('Ctrl Pts',(0.167847252202745,0.0694917728439882,
9.78508137823812E-19));
#11779=CARTESIAN_POINT('Ctrl Pts',(0.170602677001,0.0576812257767674,-6.93889390390723E-18));
#11780=CARTESIAN_POINT('Ctrl Pts',(0.171991086671603,0.051730100645855,
-1.0928332326523E-17));
#11781=CARTESIAN_POINT('Ctrl Pts',(0.173079837921644,0.045713571791822,
2.82966050020454E-17));
#11782=CARTESIAN_POINT('Ctrl Pts',(0.173850319068363,0.0396534029415724,
3.12250225675825E-17));
#11783=CARTESIAN_POINT('Ctrl Pts',(0.174328221535971,0.0358944924737595,
3.30414174095796E-17));
#11784=CARTESIAN_POINT('Ctrl Pts',(0.17468335594369,0.0321178316076463,
1.10401303661207E-17));
#11785=CARTESIAN_POINT('Ctrl Pts',(0.174910473855443,0.0283454744478527,
1.04083408558608E-17));
#11786=CARTESIAN_POINT('Ctrl Pts',(0.175316978609887,0.0215935581895444,
9.277538631825E-18));
#11787=CARTESIAN_POINT('Ctrl Pts',(0.175315699739124,0.0148427717406492,
1.46103290560722E-17));
#11788=CARTESIAN_POINT('Ctrl Pts',(0.174886275518905,0.00812263339345144,
8.67361737988404E-18));
#11789=CARTESIAN_POINT('Ctrl Pts',(0.174132950249562,-0.00366629185126618,
-1.74096734056434E-18));
#11790=CARTESIAN_POINT('Ctrl Pts',(0.172064162512452,-0.015362891267024,
2.05614309001684E-17));
#11791=CARTESIAN_POINT('Ctrl Pts',(0.168769206728486,-0.0267893073475998,
3.29597460435593E-17));
#11792=CARTESIAN_POINT('Ctrl Pts',(0.16774389460927,-0.0303449371207288,
3.68178077620904E-17));
#11793=CARTESIAN_POINT('Ctrl Pts',(0.166598934891851,-0.0338750081296103,
-1.14228928110452E-17));
#11794=CARTESIAN_POINT('Ctrl Pts',(0.165342739336206,-0.0373581457979936,
-1.21430643318376E-17));
#11795=CARTESIAN_POINT('Ctrl Pts',(0.161971436695734,-0.0467059827377018,
-1.40758176668829E-17));
#11796=CARTESIAN_POINT('Ctrl Pts',(0.15779349911764,-0.0557446055141624,
4.46068520704283E-18));
#11797=CARTESIAN_POINT('Ctrl Pts',(0.152869055079828,-0.0643699094100016,
3.46944695195361E-17));
#11798=CARTESIAN_POINT('Ctrl Pts',(0.150138152047912,-0.0691531637996316,
5.14609374926382E-17));
#11799=CARTESIAN_POINT('Ctrl Pts',(0.147177244350092,-0.0738090201013192,
-1.50318967518465E-18));
#11800=CARTESIAN_POINT('Ctrl Pts',(0.143994070896324,-0.0783167975121378,
-6.93889390390723E-18));
#11801=CARTESIAN_POINT('Ctrl Pts',(0.14200814232103,-0.0811291242989852,
-1.03301386825709E-17));
#11802=CARTESIAN_POINT('Ctrl Pts',(0.139935669748527,-0.0838837680603148,
1.78075490207948E-17));
#11803=CARTESIAN_POINT('Ctrl Pts',(0.137778285309418,-0.0865751700254918,
2.08166817117217E-17));
#11804=CARTESIAN_POINT('Ctrl Pts',(0.135528080086737,-0.0893823687095031,
2.39552813855276E-17));
#11805=CARTESIAN_POINT('Ctrl Pts',(0.133190359351591,-0.0921145253789638,
2.01371011364845E-17));
#11806=CARTESIAN_POINT('Ctrl Pts',(0.130771621045583,-0.0947623052516935,
1.73472347597681E-17));
#11807=CARTESIAN_POINT('Ctrl Pts',(0.123528051428705,-0.102691802126427,
8.99222120938157E-18));
#11808=CARTESIAN_POINT('Ctrl Pts',(0.11554930715408,-0.109880506845132,
-2.43949043573933E-17));
#11809=CARTESIAN_POINT('Ctrl Pts',(0.106897890251738,-0.116170853237509,
-6.93889390390723E-18));
#11810=CARTESIAN_POINT('Ctrl Pts',(0.101631397195622,-0.120000060172047,
3.68733748437521E-18));
#11811=CARTESIAN_POINT('Ctrl Pts',(0.0961151553280942,-0.12349557915736,
2.54302973394793E-18));
#11812=CARTESIAN_POINT('Ctrl Pts',(0.0903606778650135,-0.126612599672289,
0.));
#11813=CARTESIAN_POINT('Origin',(0.,0.,0.));
#11814=CARTESIAN_POINT('Origin',(0.,0.,2.4));
#11815=CARTESIAN_POINT('Origin',(-0.0866025403784439,-0.15,-0.3));
#11816=CARTESIAN_POINT('',(-0.0866025403784439,-0.15,-0.3));
#11817=CARTESIAN_POINT('',(0.0866025403784439,-0.15,-0.3));
#11818=CARTESIAN_POINT('',(-0.043301270189222,-0.15,-0.3));
#11819=CARTESIAN_POINT('',(-0.0866025403784439,-0.15,-0.1));
#11820=CARTESIAN_POINT('',(-0.0866025403784439,-0.15,-0.3));
#11821=CARTESIAN_POINT('',(0.0866025403784439,-0.15,-0.1));
#11822=CARTESIAN_POINT('',(-0.0866025403784439,-0.15,-0.1));
#11823=CARTESIAN_POINT('',(0.0866025403784439,-0.15,-0.3));
#11824=CARTESIAN_POINT('Origin',(-0.173205080756888,2.12115047744981E-17,
-0.3));
#11825=CARTESIAN_POINT('',(-0.173205080756888,2.12115047744981E-17,-0.3));
#11826=CARTESIAN_POINT('',(-0.151554445662277,-0.0375,-0.3));
#11827=CARTESIAN_POINT('',(-0.173205080756888,2.77555756156289E-17,-0.1));
#11828=CARTESIAN_POINT('',(-0.173205080756888,2.12115047744981E-17,-0.3));
#11829=CARTESIAN_POINT('',(-0.173205080756888,2.12115047744981E-17,-0.1));
#11830=CARTESIAN_POINT('Origin',(-0.0866025403784438,0.15,-0.3));
#11831=CARTESIAN_POINT('',(-0.0866025403784438,0.15,-0.3));
#11832=CARTESIAN_POINT('',(-0.108253175473055,0.1125,-0.3));
#11833=CARTESIAN_POINT('',(-0.0866025403784438,0.15,-0.1));
#11834=CARTESIAN_POINT('',(-0.0866025403784438,0.15,-0.3));
#11835=CARTESIAN_POINT('',(-0.0866025403784438,0.15,-0.1));
#11836=CARTESIAN_POINT('Origin',(0.0866025403784439,0.15,-0.3));
#11837=CARTESIAN_POINT('',(0.0866025403784439,0.15,-0.3));
#11838=CARTESIAN_POINT('',(0.043301270189222,0.15,-0.3));
#11839=CARTESIAN_POINT('',(0.0866025403784439,0.15,-0.1));
#11840=CARTESIAN_POINT('',(0.0866025403784439,0.15,-0.3));
#11841=CARTESIAN_POINT('',(0.0866025403784439,0.15,-0.1));
#11842=CARTESIAN_POINT('Origin',(0.173205080756888,0.,-0.3));
#11843=CARTESIAN_POINT('',(0.173205080756888,0.,-0.3));
#11844=CARTESIAN_POINT('',(0.151554445662277,0.0375,-0.3));
#11845=CARTESIAN_POINT('',(0.173205080756888,0.,-0.1));
#11846=CARTESIAN_POINT('',(0.173205080756888,0.,-0.3));
#11847=CARTESIAN_POINT('',(0.173205080756888,0.,-0.1));
#11848=CARTESIAN_POINT('Origin',(0.0866025403784439,-0.15,-0.3));
#11849=CARTESIAN_POINT('',(0.108253175473055,-0.1125,-0.3));
#11850=CARTESIAN_POINT('',(0.0866025403784439,-0.15,-0.1));
#11851=CARTESIAN_POINT('Origin',(0.,2.77555756156289E-17,-0.1));
#11852=CARTESIAN_POINT('Origin',(0.,0.,0.));
#11853=CARTESIAN_POINT('',(-0.4,-4.89858719658941E-17,0.));
#11854=CARTESIAN_POINT('Origin',(0.,0.,0.));
#11855=CARTESIAN_POINT('Origin',(0.,0.,-0.3));
#11856=CARTESIAN_POINT('',(-0.4,-4.89858719658941E-17,-0.3));
#11857=CARTESIAN_POINT('',(-0.4,-4.89858719658941E-17,-0.3));
#11858=CARTESIAN_POINT('Origin',(0.,0.,-0.3));
#11859=CARTESIAN_POINT('Origin',(0.,0.,-0.3));
#11860=CARTESIAN_POINT('Origin',(0.,0.,2.4));
#12946=UNCERTAINTY_MEASURE_WITH_UNIT(LENGTH_MEASURE(0.001),#12964,
'DISTANCE_ACCURACY_VALUE',
'Maximum model space distance between geometric entities at asserted c
onnectivities');
#12949=UNCERTAINTY_MEASURE_WITH_UNIT(LENGTH_MEASURE(0.001),#12964,
'DISTANCE_ACCURACY_VALUE',
'Maximum model space distance between geometric entities at asserted c
onnectivities');
#12960=(
GEOMETRIC_REPRESENTATION_CONTEXT(3)
GLOBAL_UNCERTAINTY_ASSIGNED_CONTEXT((#12946))
GLOBAL_UNIT_ASSIGNED_CONTEXT((#12964,#12966,#12967))
REPRESENTATION_CONTEXT('','3D')
);
#12963=(
GEOMETRIC_REPRESENTATION_CONTEXT(3)
GLOBAL_UNCERTAINTY_ASSIGNED_CONTEXT((#12949))
GLOBAL_UNIT_ASSIGNED_CONTEXT((#12964,#12966,#12967))
REPRESENTATION_CONTEXT('','3D')
);
#12964=(
LENGTH_UNIT()
NAMED_UNIT(*)
SI_UNIT(.CENTI.,.METRE.)
);
#12966=(
NAMED_UNIT(*)
PLANE_ANGLE_UNIT()
SI_UNIT($,.RADIAN.)
);
#12967=(
NAMED_UNIT(*)
SI_UNIT($,.STERADIAN.)
SOLID_ANGLE_UNIT()
);
#12978=SHAPE_DEFINITION_REPRESENTATION(#12991,#13044);
#12991=PRODUCT_DEFINITION_SHAPE('',$,#13058);
#13044=SHAPE_REPRESENTATION('',(#5177),#12960);
#13047=PRODUCT_DEFINITION_CONTEXT('part definition',#13088,'design');
#13058=PRODUCT_DEFINITION('Socket head screw M4x24',
'Socket head screw M4x24',#13071,#13047);
#13071=PRODUCT_DEFINITION_FORMATION('',$,#13100);
#13088=APPLICATION_CONTEXT(
'Core Data for Automotive Mechanical Design Process');
#13089=PRODUCT_CONTEXT('part definition',#13088,'mechanical');
#13100=PRODUCT('Socket head screw M4x24','Socket head screw M4x24',$,(#13089));
#13113=PRESENTATION_STYLE_ASSIGNMENT((#13126));
#13126=SURFACE_STYLE_USAGE(.BOTH.,#13139);
#13139=SURFACE_SIDE_STYLE('',(#13152));
#13152=SURFACE_STYLE_FILL_AREA(#13165);
#13165=FILL_AREA_STYLE('Socket head screw M4x24 finish',(#13178));
#13178=FILL_AREA_STYLE_COLOUR('Socket head screw M4x24 finish',#13191);
#13191=COLOUR_RGB('Socket head screw M4x24 finish',0.607843137254902,0.647058823529412,
0.701960784313725);
ENDSEC;
END-ISO-10303-21;
